ISO-10303-21;
HEADER;
FILE_DESCRIPTION (('STEP AP214'),
    '1' );
FILE_NAME ('upper roller_ISO - Spur gear 0.4M 35T 20PA 20FW ---S35A75H50L5.0N.step',
    '2026-10-03T20:08:58',
    ( '' ),
    ( '' ),
    'SwSTEP 2.0',
    'SolidWorks 2026',
    '' );
FILE_SCHEMA (( 'AUTOMOTIVE_DESIGN' ));
ENDSEC;

DATA;
#3=ORIENTED_EDGE ( 'NONE', *, *, #5317, .F. ) ;
#5=ORIENTED_EDGE ( 'NONE', *, *, #5789, .T. ) ;
#7=AXIS2_PLACEMENT_3D ( 'NONE', #1534, #4440, #9440 ) ;
#11=ADVANCED_FACE ( 'NONE', ( #11750 ), #8898, .T. ) ;
#12=CARTESIAN_POINT ( 'NONE',  ( 19.99999999999997868, 5.670261409740700920, -3.175710400084609475 ) ) ;
#13=CARTESIAN_POINT ( 'NONE',  ( 9.999999999999994671, -7.399010254356641170, 0.1210258481698957278 ) ) ;
#14=FACE_OUTER_BOUND ( 'NONE', #4864, .T. ) ;
#18=DIRECTION ( 'NONE',  ( 1.140150527077241873E-30, 0.000000000000000000, -1.000000000000000000 ) ) ;
#19=FACE_OUTER_BOUND ( 'NONE', #8393, .T. ) ;
#21=ORIENTED_EDGE ( 'NONE', *, *, #12558, .T. ) ;
#22=DIRECTION ( 'NONE',  ( -1.000000000000000000, 1.010728034814421376E-30, 1.090846720500930387E-30 ) ) ;
#23=EDGE_CURVE ( 'NONE', #11067, #11603, #10115, .T. ) ;
#26=DIRECTION ( 'NONE',  ( 0.000000000000000000, 0.000000000000000000, 1.000000000000000000 ) ) ;
#27=ADVANCED_FACE ( 'NONE', ( #3005 ), #10828, .T. ) ;
#28=CARTESIAN_POINT ( 'NONE',  ( 19.99999999999999645, 0.000000000000000000, 0.000000000000000000 ) ) ;
#31=CARTESIAN_POINT ( 'NONE',  ( 0.000000000000000000, -6.884685972239682705, 2.713134545806031195 ) ) ;
#35=VERTEX_POINT ( 'NONE', #4203 ) ;
#41=VERTEX_POINT ( 'NONE', #145 ) ;
#49=CARTESIAN_POINT ( 'NONE',  ( 19.99999999999999645, -6.484265599627176968, 1.105616797298907716 ) ) ;
#51=ORIENTED_EDGE ( 'NONE', *, *, #132, .F. ) ;
#52=AXIS2_PLACEMENT_3D ( 'NONE', #7977, #7092, #2061 ) ;
#54=DIRECTION ( 'NONE',  ( 7.272311470006191196E-31, 0.3513748240813434620, -0.9362348706397368714 ) ) ;
#57=CARTESIAN_POINT ( 'NONE',  ( 19.99999999999999645, 0.000000000000000000, 0.000000000000000000 ) ) ;
#59=EDGE_CURVE ( 'NONE', #992, #4885, #7267, .T. ) ;
#64=DIRECTION ( 'NONE',  ( -1.000000000000000000, 1.010728034814421376E-30, 1.090846720500930387E-30 ) ) ;
#65=EDGE_CURVE ( 'NONE', #6211, #2771, #7241, .T. ) ;
#67=DIRECTION ( 'NONE',  ( -1.000000000000000000, 1.010728034814421376E-30, 1.090846720500930387E-30 ) ) ;
#68=CIRCLE ( 'NONE', #2542, 6.499000000000009436 ) ;
#69=ORIENTED_EDGE ( 'NONE', *, *, #11638, .T. ) ;
#70=DIRECTION ( 'NONE',  ( 0.000000000000000000, 0.000000000000000000, 1.000000000000000000 ) ) ;
#73=CARTESIAN_POINT ( 'NONE',  ( 19.99999999999999645, -2.385831757338583881, 6.045230171438861433 ) ) ;
#74=VECTOR ( 'NONE', #10959, 1000.000000000000000 ) ;
#78=CARTESIAN_POINT ( 'NONE',  ( 19.99999999999997868, -2.171317488608451196, -7.074275960383738848 ) ) ;
#81=AXIS2_PLACEMENT_3D ( 'NONE', #653, #10630, #1876 ) ;
#82=ORIENTED_EDGE ( 'NONE', *, *, #340, .T. ) ;
#86=LINE ( 'NONE', #3133, #9986 ) ;
#87=VERTEX_POINT ( 'NONE', #3260 ) ;
#88=AXIS2_PLACEMENT_3D ( 'NONE', #6205, #12269, #12210 ) ;
#90=FACE_OUTER_BOUND ( 'NONE', #10199, .T. ) ;
#94=ORIENTED_EDGE ( 'NONE', *, *, #6721, .T. ) ;
#97=AXIS2_PLACEMENT_3D ( 'NONE', #1483, #11545, #8437 ) ;
#100=DIRECTION ( 'NONE',  ( 0.000000000000000000, -0.9909497617679331460, -0.1342332658176667304 ) ) ;
#102=DIRECTION ( 'NONE',  ( -1.000000000000000000, 1.010728034814421376E-30, 1.090846720500930387E-30 ) ) ;
#105=CARTESIAN_POINT ( 'NONE',  ( 9.999999999999994671, -7.301715115245761112, -1.202063382601588959 ) ) ;
#108=ORIENTED_EDGE ( 'NONE', *, *, #10644, .F. ) ;
#109=ADVANCED_FACE ( 'NONE', ( #2146 ), #3325, .T. ) ;
#111=EDGE_CURVE ( 'NONE', #3787, #7514, #12202, .T. ) ;
#113=ORIENTED_EDGE ( 'NONE', *, *, #3942, .T. ) ;
#114=DIRECTION ( 'NONE',  ( -1.000000000000000000, 1.010728034814421376E-30, 1.090846720500930387E-30 ) ) ;
#116=ORIENTED_EDGE ( 'NONE', *, *, #9811, .T. ) ;
#117=AXIS2_PLACEMENT_3D ( 'NONE', #8062, #12074, #12010 ) ;
#122=CARTESIAN_POINT ( 'NONE',  ( 19.99999999999999645, -5.610543508060446882, 3.433640984893234549 ) ) ;
#123=CARTESIAN_POINT ( 'NONE',  ( 19.99999999999999645, -4.155687294075553595, -5.098857909653601084 ) ) ;
#125=VERTEX_POINT ( 'NONE', #8190 ) ;
#128=CARTESIAN_POINT ( 'NONE',  ( 19.99999999999999645, 0.000000000000000000, 0.000000000000000000 ) ) ;
#129=CARTESIAN_POINT ( 'NONE',  ( 9.999999999999998224, 7.100173756228433497, 2.085073771204572157 ) ) ;
#130=CIRCLE ( 'NONE', #8361, 7.400000000000011902 ) ;
#132=EDGE_CURVE ( 'NONE', #3832, #6132, #1903, .T. ) ;
#133=CIRCLE ( 'NONE', #4662, 7.400000000000011902 ) ;
#134=CARTESIAN_POINT ( 'NONE',  ( 0.000000000000000000, 4.192831774278975132, 4.965597920955404199 ) ) ;
#137=DIRECTION ( 'NONE',  ( 1.000000000000000000, -1.010728034814421376E-30, -1.090846720500930387E-30 ) ) ;
#143=EDGE_CURVE ( 'NONE', #5907, #8271, #10318, .T. ) ;
#145=CARTESIAN_POINT ( 'NONE',  ( 19.99999999999997868, 0.6915992404090851586, -6.462096524400249287 ) ) ;
#146=CARTESIAN_POINT ( 'NONE',  ( 0.000000000000000000, 4.772487208025128602, 4.411390579991361527 ) ) ;
#147=CARTESIAN_POINT ( 'NONE',  ( 19.99999999999999645, -5.651611091574833878, 4.776954267060571802 ) ) ;
#150=ORIENTED_EDGE ( 'NONE', *, *, #8938, .F. ) ;
#151=CIRCLE ( 'NONE', #11268, 2.800000000000003375 ) ;
#156=VERTEX_POINT ( 'NONE', #5173 ) ;
#162=ORIENTED_EDGE ( 'NONE', *, *, #10787, .F. ) ;
#167=CARTESIAN_POINT ( 'NONE',  ( 0.000000000000000000, 4.772487208025201433, -4.411390579991299354 ) ) ;
#168=DIRECTION ( 'NONE',  ( -1.000000000000000000, 1.010728034814421376E-30, 1.090846720500930387E-30 ) ) ;
#174=ORIENTED_EDGE ( 'NONE', *, *, #9059, .T. ) ;
#175=VERTEX_POINT ( 'NONE', #5295 ) ;
#178=ORIENTED_EDGE ( 'NONE', *, *, #3075, .F. ) ;
#179=FACE_OUTER_BOUND ( 'NONE', #3393, .T. ) ;
#184=ADVANCED_FACE ( 'NONE', ( #12327 ), #9395, .T. ) ;
#186=AXIS2_PLACEMENT_3D ( 'NONE', #11743, #4909, #6785 ) ;
#188=FACE_OUTER_BOUND ( 'NONE', #3903, .T. ) ;
#190=FACE_OUTER_BOUND ( 'NONE', #6817, .T. ) ;
#195=AXIS2_PLACEMENT_3D ( 'NONE', #7539, #2660, #4452 ) ;
#197=CIRCLE ( 'NONE', #2043, 2.800000000000002931 ) ;
#202=DIRECTION ( 'NONE',  ( -1.000000000000000000, 1.010728034814421376E-30, 1.090846720500930387E-30 ) ) ;
#204=CIRCLE ( 'NONE', #7, 6.499000000000010324 ) ;
#206=CARTESIAN_POINT ( 'NONE',  ( 0.000000000000000000, -1.623118704078857499, -6.293050665016890477 ) ) ;
#215=ORIENTED_EDGE ( 'NONE', *, *, #9401, .F. ) ;
#221=DIRECTION ( 'NONE',  ( 0.000000000000000000, 0.000000000000000000, 1.000000000000000000 ) ) ;
#226=ORIENTED_EDGE ( 'NONE', *, *, #11853, .T. ) ;
#228=CARTESIAN_POINT ( 'NONE',  ( 19.99999999999997868, 6.146182963951697609, -2.112211157443803611 ) ) ;
#229=VERTEX_POINT ( 'NONE', #7547 ) ;
#230=CARTESIAN_POINT ( 'NONE',  ( 9.999999999999980460, -5.492355906873422455, 4.959236492871922586 ) ) ;
#232=DIRECTION ( 'NONE',  ( 1.158639454543359513E-30, -0.1785568947986227173, -0.9839295885986321100 ) ) ;
#236=ORIENTED_EDGE ( 'NONE', *, *, #12303, .F. ) ;
#241=AXIS2_PLACEMENT_3D ( 'NONE', #12258, #11351, #9391 ) ;
#242=CARTESIAN_POINT ( 'NONE',  ( 0.000000000000000000, 0.000000000000000000, 0.000000000000000000 ) ) ;
#244=CARTESIAN_POINT ( 'NONE',  ( -10.00000000000000178, 0.000000000000000000, 0.000000000000000000 ) ) ;
#245=VERTEX_POINT ( 'NONE', #10303 ) ;
#246=CARTESIAN_POINT ( 'NONE',  ( 19.99999999999999645, -4.155687294075553595, -5.098857909653601084 ) ) ;
#247=AXIS2_PLACEMENT_3D ( 'NONE', #6312, #11214, #8436 ) ;
#248=CARTESIAN_POINT ( 'NONE',  ( 0.000000000000000000, 0.000000000000000000, 0.000000000000000000 ) ) ;
#249=LINE ( 'NONE', #7281, #6377 ) ;
#250=ORIENTED_EDGE ( 'NONE', *, *, #9565, .F. ) ;
#252=ORIENTED_EDGE ( 'NONE', *, *, #804, .T. ) ;
#253=CARTESIAN_POINT ( 'NONE',  ( 0.000000000000000000, 0.000000000000000000, 0.000000000000000000 ) ) ;
#254=EDGE_CURVE ( 'NONE', #6132, #11730, #871, .T. ) ;
#257=CARTESIAN_POINT ( 'NONE',  ( 0.000000000000000000, -0.4733669331951463888, -6.481737787550307495 ) ) ;
#262=CIRCLE ( 'NONE', #8491, 7.400000000000009237 ) ;
#267=DIRECTION ( 'NONE',  ( -1.000000000000000000, 1.010728034814421376E-30, 1.090846720500930387E-30 ) ) ;
#272=DIRECTION ( 'NONE',  ( 0.000000000000000000, 0.9195277725514489076, 0.3930250316539277144 ) ) ;
#275=CYLINDRICAL_SURFACE ( 'NONE', #8773, 2.800000000000003819 ) ;
#276=VERTEX_POINT ( 'NONE', #717 ) ;
#284=ORIENTED_EDGE ( 'NONE', *, *, #4561, .F. ) ;
#285=ORIENTED_EDGE ( 'NONE', *, *, #3237, .F. ) ;
#286=DIRECTION ( 'NONE',  ( -1.000000000000000000, 1.010728034814421376E-30, 1.090846720500930387E-30 ) ) ;
#287=ORIENTED_EDGE ( 'NONE', *, *, #3604, .F. ) ;
#290=DIRECTION ( 'NONE',  ( 1.000000000000000000, -1.010728034814421376E-30, -1.090846720500930387E-30 ) ) ;
#291=VERTEX_POINT ( 'NONE', #5614 ) ;
#293=CARTESIAN_POINT ( 'NONE',  ( 9.999999999999998224, 3.019282868015183752, -6.756029230465944835 ) ) ;
#296=EDGE_CURVE ( 'NONE', #2105, #6027, #1281, .T. ) ;
#299=AXIS2_PLACEMENT_3D ( 'NONE', #10361, #5481, #9387 ) ;
#310=ORIENTED_EDGE ( 'NONE', *, *, #2739, .F. ) ;
#311=VECTOR ( 'NONE', #12495, 1000.000000000000000 ) ;
#317=EDGE_CURVE ( 'NONE', #3010, #5117, #3561, .T. ) ;
#319=ORIENTED_EDGE ( 'NONE', *, *, #10446, .F. ) ;
#320=AXIS2_PLACEMENT_3D ( 'NONE', #11362, #2607, #1756 ) ;
#323=EDGE_CURVE ( 'NONE', #2041, #8095, #6021, .T. ) ;
#325=CYLINDRICAL_SURFACE ( 'NONE', #7247, 2.800000000000003819 ) ;
#327=CYLINDRICAL_SURFACE ( 'NONE', #7553, 6.499000000000010324 ) ;
#329=DIRECTION ( 'NONE',  ( 2.218671295934092637E-31, -0.8345732537213080837, 0.5508969814520944253 ) ) ;
#330=CYLINDRICAL_SURFACE ( 'NONE', #9243, 2.800000000000003819 ) ;
#332=AXIS2_PLACEMENT_3D ( 'NONE', #551, #4484, #8402 ) ;
#334=AXIS2_PLACEMENT_3D ( 'NONE', #8900, #11752, #2944 ) ;
#337=CARTESIAN_POINT ( 'NONE',  ( 0.000000000000000000, 6.557268578288196537, 0.5199208220222142351 ) ) ;
#338=DIRECTION ( 'NONE',  ( 0.000000000000000000, 0.000000000000000000, 1.000000000000000000 ) ) ;
#339=CARTESIAN_POINT ( 'NONE',  ( 19.99999999999999645, 6.018220532833773007, 2.453165835849278942 ) ) ;
#340=EDGE_CURVE ( 'NONE', #9694, #2491, #8482, .T. ) ;
#343=CIRCLE ( 'NONE', #6939, 6.499000000000008548 ) ;
#346=ORIENTED_EDGE ( 'NONE', *, *, #1046, .T. ) ;
#350=VECTOR ( 'NONE', #4831, 1000.000000000000000 ) ;
#351=ORIENTED_EDGE ( 'NONE', *, *, #8169, .F. ) ;
#353=CARTESIAN_POINT ( 'NONE',  ( 0.000000000000000000, 2.649444137877595473, 6.020675595748707032 ) ) ;
#355=DIRECTION ( 'NONE',  ( -1.000000000000000000, 1.010728034814421376E-30, 1.090846720500930387E-30 ) ) ;
#356=DIRECTION ( 'NONE',  ( -1.000000000000000000, 1.010728034814421376E-30, 1.090846720500930387E-30 ) ) ;
#362=ORIENTED_EDGE ( 'NONE', *, *, #10996, .F. ) ;
#363=VERTEX_POINT ( 'NONE', #5799 ) ;
#365=EDGE_LOOP ( 'NONE', ( #4634, #310, #4264, #5091 ) ) ;
#368=EDGE_CURVE ( 'NONE', #6626, #7571, #10720, .T. ) ;
#372=EDGE_LOOP ( 'NONE', ( #7956, #11236, #11285, #3395 ) ) ;
#374=DIRECTION ( 'NONE',  ( -1.000000000000000000, 1.010728034814421376E-30, 1.090846720500930387E-30 ) ) ;
#375=EDGE_CURVE ( 'NONE', #9475, #4011, #6203, .T. ) ;
#379=ORIENTED_EDGE ( 'NONE', *, *, #2110, .T. ) ;
#386=DIRECTION ( 'NONE',  ( 0.000000000000000000, -0.9909497617679332571, -0.1342332658176667859 ) ) ;
#388=AXIS2_PLACEMENT_3D ( 'NONE', #12442, #3619, #6573 ) ;
#390=CARTESIAN_POINT ( 'NONE',  ( 0.000000000000000000, 6.718789039999997215, -3.101269713516732196 ) ) ;
#397=AXIS2_PLACEMENT_3D ( 'NONE', #3147, #6392, #6023 ) ;
#401=DIRECTION ( 'NONE',  ( -1.000000000000000000, 1.010728034814421376E-30, 1.090846720500930387E-30 ) ) ;
#403=FACE_OUTER_BOUND ( 'NONE', #8812, .T. ) ;
#405=CIRCLE ( 'NONE', #4524, 2.800000000000003375 ) ;
#410=ORIENTED_EDGE ( 'NONE', *, *, #7161, .T. ) ;
#414=EDGE_CURVE ( 'NONE', #9874, #11663, #6658, .T. ) ;
#418=CIRCLE ( 'NONE', #12362, 2.800000000000002931 ) ;
#420=FACE_OUTER_BOUND ( 'NONE', #1460, .T. ) ;
#422=CARTESIAN_POINT ( 'NONE',  ( 19.99999999999999645, 0.000000000000000000, 0.000000000000000000 ) ) ;
#429=ORIENTED_EDGE ( 'NONE', *, *, #2954, .F. ) ;
#432=ADVANCED_FACE ( 'NONE', ( #10629 ), #7678, .T. ) ;
#435=ORIENTED_EDGE ( 'NONE', *, *, #843, .T. ) ;
#437=ORIENTED_EDGE ( 'NONE', *, *, #10607, .F. ) ;
#440=DIRECTION ( 'NONE',  ( -1.000000000000000000, 1.010728034814421376E-30, 1.090846720500930387E-30 ) ) ;
#442=EDGE_LOOP ( 'NONE', ( #11196, #8941, #10732, #3335 ) ) ;
#443=CIRCLE ( 'NONE', #3735, 7.400000000000009237 ) ;
#445=EDGE_CURVE ( 'NONE', #3047, #865, #7801, .T. ) ;
#448=EDGE_CURVE ( 'NONE', #992, #6318, #11736, .T. ) ;
#452=AXIS2_PLACEMENT_3D ( 'NONE', #4456, #11224, #9272 ) ;
#454=EDGE_CURVE ( 'NONE', #1459, #9808, #2931, .T. ) ;
#459=CARTESIAN_POINT ( 'NONE',  ( 19.99999999999997868, -3.055252325922143797, -5.825248672282175910 ) ) ;
#462=ADVANCED_FACE ( 'NONE', ( #3998 ), #9588, .T. ) ;
#465=CARTESIAN_POINT ( 'NONE',  ( 19.99999999999999645, 0.000000000000000000, 0.000000000000000000 ) ) ;
#466=DIRECTION ( 'NONE',  ( -1.380506584136768733E-30, 0.4338837391175524583, 0.9009688679024216995 ) ) ;
#468=AXIS2_PLACEMENT_3D ( 'NONE', #1619, #6323, #10228 ) ;
#470=CIRCLE ( 'NONE', #9303, 2.800000000000003819 ) ;
#477=VERTEX_POINT ( 'NONE', #10690 ) ;
#479=VERTEX_POINT ( 'NONE', #10750 ) ;
#482=CARTESIAN_POINT ( 'NONE',  ( 0.000000000000000000, 0.6915992404090791634, -6.462096524400238629 ) ) ;
#483=DIRECTION ( 'NONE',  ( -9.614242282381067365E-31, -0.08963930890344089242, 0.9959742939952382912 ) ) ;
#485=DIRECTION ( 'NONE',  ( -1.000000000000000000, 1.010728034814421376E-30, 1.090846720500930387E-30 ) ) ;
#486=ORIENTED_EDGE ( 'NONE', *, *, #4954, .F. ) ;
#490=VERTEX_POINT ( 'NONE', #12059 ) ;
#491=ORIENTED_EDGE ( 'NONE', *, *, #11638, .F. ) ;
#493=ORIENTED_EDGE ( 'NONE', *, *, #2028, .F. ) ;
#495=LINE ( 'NONE', #10139, #8704 ) ;
#498=DIRECTION ( 'NONE',  ( -1.000000000000000000, 1.010728034814421376E-30, -1.140150527077241873E-30 ) ) ;
#503=CIRCLE ( 'NONE', #12641, 2.500000000000003553 ) ;
#504=ADVANCED_FACE ( 'NONE', ( #4128 ), #325, .T. ) ;
#510=ORIENTED_EDGE ( 'NONE', *, *, #6287, .F. ) ;
#512=CIRCLE ( 'NONE', #11620, 6.499000000000008548 ) ;
#513=ADVANCED_FACE ( 'NONE', ( #2068 ), #7979, .T. ) ;
#514=CIRCLE ( 'NONE', #2164, 2.800000000000003375 ) ;
#515=FACE_OUTER_BOUND ( 'NONE', #12425, .T. ) ;
#516=CARTESIAN_POINT ( 'NONE',  ( 19.99999999999999645, 1.395418990828201533, 6.428133065596412621 ) ) ;
#519=CYLINDRICAL_SURFACE ( 'NONE', #97, 6.499000000000010324 ) ;
#520=AXIS2_PLACEMENT_3D ( 'NONE', #4632, #11202, #6301 ) ;
#521=AXIS2_PLACEMENT_3D ( 'NONE', #8664, #3774, #5821 ) ;
#523=ORIENTED_EDGE ( 'NONE', *, *, #7970, .F. ) ;
#525=CYLINDRICAL_SURFACE ( 'NONE', #241, 6.499000000000010324 ) ;
#528=DIRECTION ( 'NONE',  ( -1.000000000000000000, 1.010728034814421376E-30, 1.090846720500930387E-30 ) ) ;
#530=CIRCLE ( 'NONE', #8546, 2.800000000000003819 ) ;
#533=CARTESIAN_POINT ( 'NONE',  ( 19.99999999999999645, -5.682309657208315379, -3.313524683562055984 ) ) ;
#537=EDGE_CURVE ( 'NONE', #41, #2105, #8074, .T. ) ;
#541=AXIS2_PLACEMENT_3D ( 'NONE', #8358, #12429, #3605 ) ;
#542=CIRCLE ( 'NONE', #1350, 2.800000000000002931 ) ;
#543=FACE_OUTER_BOUND ( 'NONE', #7089, .T. ) ;
#544=ORIENTED_EDGE ( 'NONE', *, *, #9595, .F. ) ;
#545=ORIENTED_EDGE ( 'NONE', *, *, #8383, .T. ) ;
#547=DIRECTION ( 'NONE',  ( 0.000000000000000000, 0.9909497617679351444, -0.1342332658176521309 ) ) ;
#551=CARTESIAN_POINT ( 'NONE',  ( 19.99999999999999645, 0.000000000000000000, 0.000000000000000000 ) ) ;
#552=ORIENTED_EDGE ( 'NONE', *, *, #4771, .F. ) ;
#564=EDGE_CURVE ( 'NONE', #7155, #8095, #3349, .T. ) ;
#566=FACE_OUTER_BOUND ( 'NONE', #2032, .T. ) ;
#568=VERTEX_POINT ( 'NONE', #6186 ) ;
#583=CIRCLE ( 'NONE', #10028, 2.800000000000003819 ) ;
#584=CARTESIAN_POINT ( 'NONE',  ( 19.99999999999999645, 0.000000000000000000, 0.000000000000000000 ) ) ;
#585=CARTESIAN_POINT ( 'NONE',  ( 19.99999999999999645, 7.358375340956981425, 0.7837807994561900582 ) ) ;
#586=DIRECTION ( 'NONE',  ( -1.000000000000000000, 1.010728034814421376E-30, 1.090846720500930387E-30 ) ) ;
#589=DIRECTION ( 'NONE',  ( 1.232595164407829545E-30, -0.9510565162951502005, -0.3090169943749582204 ) ) ;
#590=VECTOR ( 'NONE', #4280, 1000.000000000000000 ) ;
#591=CARTESIAN_POINT ( 'NONE',  ( 19.99999999999997868, -7.399010254356644722, -0.1210258481700032807 ) ) ;
#592=CARTESIAN_POINT ( 'NONE',  ( 9.999999999999980460, -4.707829255731252438, 5.709320773864527965 ) ) ;
#593=DIRECTION ( 'NONE',  ( -1.000000000000000000, 1.010728034814421376E-30, 1.090846720500930387E-30 ) ) ;
#594=DIRECTION ( 'NONE',  ( -1.000000000000000000, 1.010728034814421376E-30, 1.090846720500930387E-30 ) ) ;
#596=CIRCLE ( 'NONE', #5947, 6.499000000000006771 ) ;
#600=ORIENTED_EDGE ( 'NONE', *, *, #3946, .T. ) ;
#601=CIRCLE ( 'NONE', #2631, 2.800000000000003819 ) ;
#603=EDGE_CURVE ( 'NONE', #9871, #1141, #5181, .T. ) ;
#605=CARTESIAN_POINT ( 'NONE',  ( 0.000000000000000000, 0.000000000000000000, 0.000000000000000000 ) ) ;
#608=LINE ( 'NONE', #7632, #1578 ) ;
#611=AXIS2_PLACEMENT_3D ( 'NONE', #6625, #6815, #10596 ) ;
#612=CARTESIAN_POINT ( 'NONE',  ( 9.999999999999998224, 6.718789040000002544, -3.101269713516732196 ) ) ;
#618=ORIENTED_EDGE ( 'NONE', *, *, #11395, .T. ) ;
#620=ORIENTED_EDGE ( 'NONE', *, *, #4486, .F. ) ;
#626=EDGE_LOOP ( 'NONE', ( #2632, #9006, #9669, #2831 ) ) ;
#627=CARTESIAN_POINT ( 'NONE',  ( 0.000000000000000000, -5.774092856145738750, 2.982759240804853107 ) ) ;
#629=ORIENTED_EDGE ( 'NONE', *, *, #3742, .F. ) ;
#630=DIRECTION ( 'NONE',  ( 2.218671295934092637E-31, -0.8345732537213078617, 0.5508969814520944253 ) ) ;
#634=CARTESIAN_POINT ( 'NONE',  ( 0.000000000000000000, -6.182645281642508372, 2.245659411033100294 ) ) ;
#635=CARTESIAN_POINT ( 'NONE',  ( 0.000000000000000000, 0.000000000000000000, 0.000000000000000000 ) ) ;
#637=ORIENTED_EDGE ( 'NONE', *, *, #11083, .T. ) ;
#639=( GEOMETRIC_REPRESENTATION_CONTEXT ( 3 ) GLOBAL_UNCERTAINTY_ASSIGNED_CONTEXT ( ( #2646 ) ) GLOBAL_UNIT_ASSIGNED_CONTEXT ( ( #12452, #11860, #2199 ) ) REPRESENTATION_CONTEXT ( 'NONE', 'WORKASPACE' ) );
#640=VERTEX_POINT ( 'NONE', #9383 ) ;
#645=CARTESIAN_POINT ( 'NONE',  ( 19.99999999999999645, 0.000000000000000000, 0.000000000000000000 ) ) ;
#646=EDGE_CURVE ( 'NONE', #2961, #11067, #5786, .T. ) ;
#647=ORIENTED_EDGE ( 'NONE', *, *, #2202, .T. ) ;
#648=DIRECTION ( 'NONE',  ( -1.000000000000000000, 1.010728034814421376E-30, 1.090846720500930387E-30 ) ) ;
#649=DIRECTION ( 'NONE',  ( 1.000000000000000000, -1.010728034814421376E-30, -1.090846720500930387E-30 ) ) ;
#650=CARTESIAN_POINT ( 'NONE',  ( 19.99999999999997868, 6.359534927042319374, -1.339147681075104845 ) ) ;
#651=ORIENTED_EDGE ( 'NONE', *, *, #537, .F. ) ;
#653=CARTESIAN_POINT ( 'NONE',  ( -10.00000000000000178, 0.000000000000000000, 0.000000000000000000 ) ) ;
#654=CARTESIAN_POINT ( 'NONE',  ( 19.99999999999997868, -3.055252325922143797, -5.825248672282175910 ) ) ;
#656=CARTESIAN_POINT ( 'NONE',  ( 19.99999999999999645, -6.453973581750240385, 0.7636923504068631186 ) ) ;
#657=CARTESIAN_POINT ( 'NONE',  ( 19.99999999999999645, -4.907279493584704610, -4.380262188593404105 ) ) ;
#659=AXIS2_PLACEMENT_3D ( 'NONE', #128, #5987, #1992 ) ;
#664=LINE ( 'NONE', #7811, #3937 ) ;
#667=ORIENTED_EDGE ( 'NONE', *, *, #12742, .T. ) ;
#668=ORIENTED_EDGE ( 'NONE', *, *, #10011, .T. ) ;
#669=AXIS2_PLACEMENT_3D ( 'NONE', #3194, #5107, #7170 ) ;
#670=DIRECTION ( 'NONE',  ( 0.000000000000000000, 0.000000000000000000, 1.000000000000000000 ) ) ;
#674=LINE ( 'NONE', #10390, #9169 ) ;
#675=ORIENTED_EDGE ( 'NONE', *, *, #4358, .T. ) ;
#677=DIRECTION ( 'NONE',  ( -1.000000000000000000, 1.010728034814421376E-30, 1.090846720500930387E-30 ) ) ;
#678=ORIENTED_EDGE ( 'NONE', *, *, #5317, .T. ) ;
#679=VECTOR ( 'NONE', #1002, 1000.000000000000000 ) ;
#683=ORIENTED_EDGE ( 'NONE', *, *, #10659, .F. ) ;
#685=ORIENTED_EDGE ( 'NONE', *, *, #8630, .F. ) ;
#686=CARTESIAN_POINT ( 'NONE',  ( 0.000000000000000000, 0.000000000000000000, 0.000000000000000000 ) ) ;
#687=EDGE_CURVE ( 'NONE', #1778, #3832, #1883, .T. ) ;
#689=ORIENTED_EDGE ( 'NONE', *, *, #4230, .F. ) ;
#701=VERTEX_POINT ( 'NONE', #1411 ) ;
#704=CARTESIAN_POINT ( 'NONE',  ( 19.99999999999999645, 0.000000000000000000, 0.000000000000000000 ) ) ;
#706=EDGE_CURVE ( 'NONE', #2862, #4036, #4572, .T. ) ;
#709=DIRECTION ( 'NONE',  ( -1.000000000000000000, 1.010728034814421376E-30, 1.090846720500930387E-30 ) ) ;
#714=EDGE_CURVE ( 'NONE', #1261, #7962, #3815, .T. ) ;
#716=CARTESIAN_POINT ( 'NONE',  ( 19.99999999999997868, 0.4528593230175830819, -7.386130139224213131 ) ) ;
#717=CARTESIAN_POINT ( 'NONE',  ( 0.000000000000000000, 5.200656487704347519, -5.264330166022919144 ) ) ;
#719=CIRCLE ( 'NONE', #8935, 7.400000000000009237 ) ;
#723=CARTESIAN_POINT ( 'NONE',  ( 0.000000000000000000, 6.544726022087268724, -0.6592800351836389794 ) ) ;
#731=ORIENTED_EDGE ( 'NONE', *, *, #143, .T. ) ;
#732=ADVANCED_FACE ( 'NONE', ( #12312 ), #11410, .T. ) ;
#739=FACE_OUTER_BOUND ( 'NONE', #4229, .T. ) ;
#741=FACE_OUTER_BOUND ( 'NONE', #4025, .T. ) ;
#742=VERTEX_POINT ( 'NONE', #12444 ) ;
#743=ORIENTED_EDGE ( 'NONE', *, *, #7941, .T. ) ;
#745=EDGE_LOOP ( 'NONE', ( #5637, #3870, #2752, #943 ) ) ;
#747=FACE_OUTER_BOUND ( 'NONE', #12689, .T. ) ;
#752=CARTESIAN_POINT ( 'NONE',  ( 19.99999999999999645, -2.720702104307051172, 5.902099716170436494 ) ) ;
#753=VERTEX_POINT ( 'NONE', #6513 ) ;
#754=EDGE_CURVE ( 'NONE', #5455, #175, #6337, .T. ) ;
#755=CARTESIAN_POINT ( 'NONE',  ( 0.000000000000000000, -2.720702104306971236, -5.902099716170491561 ) ) ;
#756=CARTESIAN_POINT ( 'NONE',  ( 19.99999999999997868, 3.238809497145301197, -5.634457741540144227 ) ) ;
#759=CIRCLE ( 'NONE', #7352, 6.499000000000009436 ) ;
#760=ORIENTED_EDGE ( 'NONE', *, *, #8868, .F. ) ;
#765=CARTESIAN_POINT ( 'NONE',  ( 0.000000000000000000, 0.000000000000000000, 0.000000000000000000 ) ) ;
#776=DIRECTION ( 'NONE',  ( 4.606824426974261154E-31, 0.5128992774059070170, -0.8584487936018656562 ) ) ;
#778=DIRECTION ( 'NONE',  ( -1.000000000000000000, 1.010728034814421376E-30, 1.090846720500930387E-30 ) ) ;
#780=DIRECTION ( 'NONE',  ( -1.000000000000000000, 1.010728034814421376E-30, 1.090846720500930387E-30 ) ) ;
#781=DIRECTION ( 'NONE',  ( 0.000000000000000000, 0.000000000000000000, 1.000000000000000000 ) ) ;
#783=AXIS2_PLACEMENT_3D ( 'NONE', #10673, #11597, #12572 ) ;
#788=ORIENTED_EDGE ( 'NONE', *, *, #3741, .F. ) ;
#792=DIRECTION ( 'NONE',  ( 1.140150527077241873E-30, 0.000000000000000000, -1.000000000000000000 ) ) ;
#796=ORIENTED_EDGE ( 'NONE', *, *, #6469, .F. ) ;
#797=FACE_OUTER_BOUND ( 'NONE', #626, .T. ) ;
#798=CIRCLE ( 'NONE', #8573, 2.800000000000003375 ) ;
#802=VERTEX_POINT ( 'NONE', #8984 ) ;
#804=EDGE_CURVE ( 'NONE', #4951, #2162, #7730, .T. ) ;
#806=ORIENTED_EDGE ( 'NONE', *, *, #12168, .T. ) ;
#807=ORIENTED_EDGE ( 'NONE', *, *, #3273, .F. ) ;
#809=FACE_OUTER_BOUND ( 'NONE', #856, .T. ) ;
#812=AXIS2_PLACEMENT_3D ( 'NONE', #8077, #11046, #4086 ) ;
#814=CARTESIAN_POINT ( 'NONE',  ( 19.99999999999997868, 6.359055127044386246, 1.682410996215993881 ) ) ;
#820=AXIS2_PLACEMENT_3D ( 'NONE', #3748, #648, #8441 ) ;
#823=ORIENTED_EDGE ( 'NONE', *, *, #7750, .T. ) ;
#825=VERTEX_POINT ( 'NONE', #167 ) ;
#826=APPLICATION_CONTEXT ( 'automotive_design' ) ;
#827=DIRECTION ( 'NONE',  ( 0.000000000000000000, -0.7818314824680222541, -0.6234898018587429203 ) ) ;
#831=AXIS2_PLACEMENT_3D ( 'NONE', #8362, #6370, #6441 ) ;
#832=FACE_OUTER_BOUND ( 'NONE', #3271, .T. ) ;
#839=CARTESIAN_POINT ( 'NONE',  ( 0.000000000000000000, 5.914787828628604416, -4.446941076999666009 ) ) ;
#842=DIRECTION ( 'NONE',  ( -1.000000000000000000, 1.010728034814421376E-30, 1.090846720500930387E-30 ) ) ;
#843=EDGE_CURVE ( 'NONE', #245, #9681, #6582, .T. ) ;
#844=CARTESIAN_POINT ( 'NONE',  ( 19.99999999999997868, 4.192831774279055068, -4.965597920955358902 ) ) ;
#846=CARTESIAN_POINT ( 'NONE',  ( 19.99999999999999645, 0.000000000000000000, 0.000000000000000000 ) ) ;
#849=CARTESIAN_POINT ( 'NONE',  ( 0.000000000000000000, -0.8135880386782442519, -6.527339685683426929 ) ) ;
#856=EDGE_LOOP ( 'NONE', ( #6670, #8268, #11592, #5004 ) ) ;
#857=ORIENTED_EDGE ( 'NONE', *, *, #6520, .F. ) ;
#858=CARTESIAN_POINT ( 'NONE',  ( 19.99999999999999645, -0.4733669331952357062, 6.481737787550290619 ) ) ;
#859=DIRECTION ( 'NONE',  ( 1.000000000000000000, -1.010728034814421376E-30, -1.090846720500930387E-30 ) ) ;
#864=CARTESIAN_POINT ( 'NONE',  ( 19.99999999999999645, -4.707829255731172502, -5.709320773864600795 ) ) ;
#865=VERTEX_POINT ( 'NONE', #8021 ) ;
#867=CYLINDRICAL_SURFACE ( 'NONE', #7181, 2.800000000000003819 ) ;
#869=ORIENTED_EDGE ( 'NONE', *, *, #6126, .F. ) ;
#871=CIRCLE ( 'NONE', #8061, 7.400000000000011902 ) ;
#874=LINE ( 'NONE', #3908, #9431 ) ;
#882=AXIS2_PLACEMENT_3D ( 'NONE', #6214, #8019, #11052 ) ;
#883=VECTOR ( 'NONE', #7862, 1000.000000000000000 ) ;
#885=ORIENTED_EDGE ( 'NONE', *, *, #5888, .F. ) ;
#887=ORIENTED_EDGE ( 'NONE', *, *, #8327, .T. ) ;
#891=SHAPE_REPRESENTATION ( 'upper roller_ISO - Spur gear 0.4M 35T 20PA 20FW ---S35A75H50L5.0N', ( #12422 ), #639 ) ;
#892=ORIENTED_EDGE ( 'NONE', *, *, #6007, .F. ) ;
#894=EDGE_CURVE ( 'NONE', #2378, #9789, #4768, .T. ) ;
#897=CARTESIAN_POINT ( 'NONE',  ( 19.99999999999999645, 0.000000000000000000, 0.000000000000000000 ) ) ;
#901=CYLINDRICAL_SURFACE ( 'NONE', #2276, 2.800000000000003819 ) ;
#904=CIRCLE ( 'NONE', #1315, 2.800000000000002931 ) ;
#905=DIRECTION ( 'NONE',  ( -1.000000000000000000, 1.010728034814421376E-30, 1.090846720500930387E-30 ) ) ;
#906=AXIS2_PLACEMENT_3D ( 'NONE', #814, #3973, #10600 ) ;
#908=DIRECTION ( 'NONE',  ( -1.000000000000000000, 1.010728034814421376E-30, 1.090846720500930387E-30 ) ) ;
#909=ADVANCED_FACE ( 'NONE', ( #832 ), #12633, .T. ) ;
#914=DIRECTION ( 'NONE',  ( 0.000000000000000000, 0.000000000000000000, 1.000000000000000000 ) ) ;
#916=EDGE_CURVE ( 'NONE', #1397, #12171, #5951, .T. ) ;
#918=AXIS2_PLACEMENT_3D ( 'NONE', #8549, #2515, #3424 ) ;
#920=VECTOR ( 'NONE', #986, 1000.000000000000000 ) ;
#921=ORIENTED_EDGE ( 'NONE', *, *, #4079, .T. ) ;
#929=EDGE_CURVE ( 'NONE', #2828, #7514, #2471, .T. ) ;
#932=CARTESIAN_POINT ( 'NONE',  ( 19.99999999999999645, -6.577476285968329783, 0.06996125000489905599 ) ) ;
#933=EDGE_LOOP ( 'NONE', ( #2197, #5461, #5972, #6284 ) ) ;
#934=VECTOR ( 'NONE', #593, 1000.000000000000000 ) ;
#936=DIRECTION ( 'NONE',  ( 0.000000000000000000, 0.000000000000000000, 1.000000000000000000 ) ) ;
#940=ORIENTED_EDGE ( 'NONE', *, *, #11784, .F. ) ;
#942=LINE ( 'NONE', #12743, #3570 ) ;
#943=ORIENTED_EDGE ( 'NONE', *, *, #1608, .T. ) ;
#944=VECTOR ( 'NONE', #3056, 1000.000000000000000 ) ;
#949=ORIENTED_EDGE ( 'NONE', *, *, #6883, .T. ) ;
#955=VERTEX_POINT ( 'NONE', #8214 ) ;
#956=CIRCLE ( 'NONE', #8157, 2.800000000000003819 ) ;
#957=CIRCLE ( 'NONE', #334, 2.800000000000003819 ) ;
#967=VECTOR ( 'NONE', #3055, 1000.000000000000000 ) ;
#968=AXIS2_PLACEMENT_3D ( 'NONE', #6719, #5802, #8710 ) ;
#969=DIRECTION ( 'NONE',  ( -1.000000000000000000, 1.010728034814421376E-30, 1.090846720500930387E-30 ) ) ;
#972=DIRECTION ( 'NONE',  ( -1.000000000000000000, 1.010728034814421376E-30, 1.090846720500930387E-30 ) ) ;
#976=CARTESIAN_POINT ( 'NONE',  ( 19.99999999999997868, 6.557268578288205418, -0.5199208220221240850 ) ) ;
#977=DIRECTION ( 'NONE',  ( 1.140150527077241873E-30, 0.000000000000000000, -1.000000000000000000 ) ) ;
#978=EDGE_CURVE ( 'NONE', #3412, #10716, #5341, .T. ) ;
#981=FACE_OUTER_BOUND ( 'NONE', #3039, .T. ) ;
#983=DIRECTION ( 'NONE',  ( -1.000000000000000000, 1.010728034814421376E-30, 1.090846720500930387E-30 ) ) ;
#984=DIRECTION ( 'NONE',  ( 0.000000000000000000, 0.4338837391175524583, 0.9009688679024216995 ) ) ;
#985=ORIENTED_EDGE ( 'NONE', *, *, #1695, .T. ) ;
#986=DIRECTION ( 'NONE',  ( -1.000000000000000000, 1.010728034814421376E-30, 1.090846720500930387E-30 ) ) ;
#987=FACE_OUTER_BOUND ( 'NONE', #6274, .T. ) ;
#988=DIRECTION ( 'NONE',  ( -1.000000000000000000, 1.010728034814421376E-30, 1.090846720500930387E-30 ) ) ;
#992=VERTEX_POINT ( 'NONE', #3280 ) ;
#994=ORIENTED_EDGE ( 'NONE', *, *, #11737, .T. ) ;
#999=ORIENTED_EDGE ( 'NONE', *, *, #8325, .F. ) ;
#1002=DIRECTION ( 'NONE',  ( -1.000000000000000000, 1.010728034814421376E-30, 1.090846720500930387E-30 ) ) ;
#1003=ORIENTED_EDGE ( 'NONE', *, *, #4683, .T. ) ;
#1006=EDGE_CURVE ( 'NONE', #7962, #2242, #4285, .T. ) ;
#1007=DIRECTION ( 'NONE',  ( -1.000000000000000000, 1.010728034814421376E-30, 1.090846720500930387E-30 ) ) ;
#1009=ORIENTED_EDGE ( 'NONE', *, *, #2005, .F. ) ;
#1010=CIRCLE ( 'NONE', #1830, 7.400000000000011902 ) ;
#1012=ORIENTED_EDGE ( 'NONE', *, *, #3749, .F. ) ;
#1014=CARTESIAN_POINT ( 'NONE',  ( 0.000000000000000000, 0.000000000000000000, 0.000000000000000000 ) ) ;
#1015=AXIS2_PLACEMENT_3D ( 'NONE', #1478, #5410, #7534 ) ;
#1017=DIRECTION ( 'NONE',  ( -1.000000000000000000, 1.010728034814421376E-30, 1.090846720500930387E-30 ) ) ;
#1020=CIRCLE ( 'NONE', #12562, 2.800000000000003819 ) ;
#1024=ORIENTED_EDGE ( 'NONE', *, *, #8317, .T. ) ;
#1025=CYLINDRICAL_SURFACE ( 'NONE', #12746, 2.800000000000003819 ) ;
#1027=FACE_OUTER_BOUND ( 'NONE', #9727, .T. ) ;
#1029=AXIS2_PLACEMENT_3D ( 'NONE', #9712, #905, #5865 ) ;
#1030=DIRECTION ( 'NONE',  ( 0.000000000000000000, 0.000000000000000000, 1.000000000000000000 ) ) ;
#1032=CYLINDRICAL_SURFACE ( 'NONE', #7953, 6.499000000000010324 ) ;
#1041=CARTESIAN_POINT ( 'NONE',  ( 19.99999999999999645, -1.623118704078951202, 6.293050665016855838 ) ) ;
#1044=DIRECTION ( 'NONE',  ( -1.000000000000000000, 1.010728034814421376E-30, 1.090846720500930387E-30 ) ) ;
#1046=EDGE_CURVE ( 'NONE', #3737, #8175, #12317, .T. ) ;
#1047=DIRECTION ( 'NONE',  ( 1.000000000000000000, -1.010728034814421376E-30, -1.090846720500930387E-30 ) ) ;
#1050=DIRECTION ( 'NONE',  ( -1.140150527077241873E-30, 0.000000000000000000, 1.000000000000000000 ) ) ;
#1051=CIRCLE ( 'NONE', #7650, 2.800000000000002931 ) ;
#1056=ORIENTED_EDGE ( 'NONE', *, *, #12288, .F. ) ;
#1059=ADVANCED_FACE ( 'NONE', ( #5313 ), #9230, .T. ) ;
#1061=ORIENTED_EDGE ( 'NONE', *, *, #2666, .T. ) ;
#1063=DIRECTION ( 'NONE',  ( 0.000000000000000000, -0.9989930665413151445, 0.04486483035050446017 ) ) ;
#1064=AXIS2_PLACEMENT_3D ( 'NONE', #8443, #3323, #10225 ) ;
#1066=CARTESIAN_POINT ( 'NONE',  ( 19.99999999999999645, 0.000000000000000000, 0.000000000000000000 ) ) ;
#1068=CARTESIAN_POINT ( 'NONE',  ( 19.99999999999999645, -6.213893036447794671, -1.903820982021606989 ) ) ;
#1070=ORIENTED_EDGE ( 'NONE', *, *, #3986, .T. ) ;
#1073=ORIENTED_EDGE ( 'NONE', *, *, #12643, .F. ) ;
#1074=CARTESIAN_POINT ( 'NONE',  ( 19.99999999999997868, 6.424561140605097087, -0.9808237102696195642 ) ) ;
#1076=DIRECTION ( 'NONE',  ( 1.380506584136768733E-30, -0.5128992774058948045, -0.8584487936018728726 ) ) ;
#1080=DIRECTION ( 'NONE',  ( 0.000000000000000000, 0.08963930890342672320, 0.9959742939952396235 ) ) ;
#1084=ADVANCED_FACE ( 'NONE', ( #3710 ), #10322, .T. ) ;
#1085=CYLINDRICAL_SURFACE ( 'NONE', #3410, 2.800000000000003819 ) ;
#1087=ORIENTED_EDGE ( 'NONE', *, *, #2568, .T. ) ;
#1089=AXIS2_PLACEMENT_3D ( 'NONE', #12158, #10982, #8210 ) ;
#1098=LINE ( 'NONE', #2070, #967 ) ;
#1102=CARTESIAN_POINT ( 'NONE',  ( 0.000000000000000000, -7.258495115966566047, -1.440225208600910634 ) ) ;
#1104=VECTOR ( 'NONE', #11982, 1000.000000000000000 ) ;
#1106=CARTESIAN_POINT ( 'NONE',  ( 19.99999999999999645, -6.310777386698697811, -1.552768423021409161 ) ) ;
#1110=CARTESIAN_POINT ( 'NONE',  ( 19.99999999999999645, 0.000000000000000000, 0.000000000000000000 ) ) ;
#1117=ADVANCED_BREP_SHAPE_REPRESENTATION ( '', ( #10152, #12422 ), #639 ) ;
#1121=CARTESIAN_POINT ( 'NONE',  ( 19.99999999999999645, 7.358375340957004518, -0.7837807994560894720 ) ) ;
#1123=AXIS2_PLACEMENT_3D ( 'NONE', #10087, #11984, #5089 ) ;
#1125=PRODUCT_CONTEXT ( 'NONE', #2144, 'mechanical' ) ;
#1128=CARTESIAN_POINT ( 'NONE',  ( -10.00000000000000178, 0.000000000000000000, 0.000000000000000000 ) ) ;
#1130=EDGE_LOOP ( 'NONE', ( #12366, #1473, #8778, #5940 ) ) ;
#1132=DIRECTION ( 'NONE',  ( -1.000000000000000000, 1.010728034814421376E-30, 1.090846720500930387E-30 ) ) ;
#1135=DIRECTION ( 'NONE',  ( -1.000000000000000000, 1.010728034814421376E-30, 1.090846720500930387E-30 ) ) ;
#1136=FACE_OUTER_BOUND ( 'NONE', #9598, .T. ) ;
#1140=ORIENTED_EDGE ( 'NONE', *, *, #9304, .T. ) ;
#1141=VERTEX_POINT ( 'NONE', #1767 ) ;
#1142=EDGE_LOOP ( 'NONE', ( #2486, #10917, #3865, #8337 ) ) ;
#1143=CARTESIAN_POINT ( 'NONE',  ( 9.999999999999994671, -6.289597356626513758, 3.898841506334516094 ) ) ;
#1148=DIRECTION ( 'NONE',  ( -1.000000000000000000, 1.010728034814421376E-30, 1.090846720500930387E-30 ) ) ;
#1149=ORIENTED_EDGE ( 'NONE', *, *, #7544, .T. ) ;
#1150=DIRECTION ( 'NONE',  ( 0.000000000000000000, 0.9510565162951545304, -0.3090169943749445092 ) ) ;
#1151=DIRECTION ( 'NONE',  ( -1.000000000000000000, 1.010728034814421376E-30, 1.090846720500930387E-30 ) ) ;
#1154=FACE_OUTER_BOUND ( 'NONE', #7783, .T. ) ;
#1157=EDGE_CURVE ( 'NONE', #3414, #5639, #2871, .T. ) ;
#1159=EDGE_CURVE ( 'NONE', #8279, #10901, #583, .T. ) ;
#1160=AXIS2_PLACEMENT_3D ( 'NONE', #8965, #8902, #9025 ) ;
#1161=DIRECTION ( 'NONE',  ( -1.140150527077241873E-30, 0.000000000000000000, 1.000000000000000000 ) ) ;
#1164=EDGE_CURVE ( 'NONE', #3630, #11388, #11076, .T. ) ;
#1168=CIRCLE ( 'NONE', #4253, 2.800000000000002931 ) ;
#1169=AXIS2_PLACEMENT_3D ( 'NONE', #8125, #4140, #8057 ) ;
#1173=CARTESIAN_POINT ( 'NONE',  ( 9.999999999999994671, -7.399010254356641170, -0.1210258481700032807 ) ) ;
#1175=CYLINDRICAL_SURFACE ( 'NONE', #11875, 2.800000000000003819 ) ;
#1177=DIRECTION ( 'NONE',  ( 0.000000000000000000, 0.000000000000000000, 1.000000000000000000 ) ) ;
#1180=CARTESIAN_POINT ( 'NONE',  ( 2.727116801252330522E-30, 5.204170427930467826E-15, 2.499999999999999112 ) ) ;
#1183=CARTESIAN_POINT ( 'NONE',  ( 0.000000000000000000, -6.459281472512942379, -1.243290685169453402 ) ) ;
#1185=ORIENTED_EDGE ( 'NONE', *, *, #1164, .F. ) ;
#1187=LINE ( 'NONE', #7949, #12349 ) ;
#1189=LINE ( 'NONE', #9109, #590 ) ;
#1194=CARTESIAN_POINT ( 'NONE',  ( -10.00000000000000178, 0.000000000000000000, 0.000000000000000000 ) ) ;
#1196=AXIS2_PLACEMENT_3D ( 'NONE', #2619, #4610, #1638 ) ;
#1197=ORIENTED_EDGE ( 'NONE', *, *, #9838, .T. ) ;
#1198=ORIENTED_EDGE ( 'NONE', *, *, #1665, .T. ) ;
#1203=EDGE_LOOP ( 'NONE', ( #10273, #6208, #1198, #629 ) ) ;
#1207=CYLINDRICAL_SURFACE ( 'NONE', #10349, 2.800000000000003819 ) ;
#1210=DIRECTION ( 'NONE',  ( 0.000000000000000000, 0.9749279121818227312, 0.2225209339563182231 ) ) ;
#1211=ADVANCED_FACE ( 'NONE', ( #1703 ), #9542, .T. ) ;
#1213=AXIS2_PLACEMENT_3D ( 'NONE', #2855, #6705, #6830 ) ;
#1216=AXIS2_PLACEMENT_3D ( 'NONE', #4875, #3912, #11772 ) ;
#1219=CYLINDRICAL_SURFACE ( 'NONE', #8884, 6.499000000000010324 ) ;
#1221=CIRCLE ( 'NONE', #10053, 7.400000000000011902 ) ;
#1222=DIRECTION ( 'NONE',  ( -1.000000000000000000, 1.010728034814421376E-30, 1.090846720500930387E-30 ) ) ;
#1226=EDGE_CURVE ( 'NONE', #8657, #9126, #12529, .T. ) ;
#1227=CARTESIAN_POINT ( 'NONE',  ( 19.99999999999999645, 0.000000000000000000, 0.000000000000000000 ) ) ;
#1229=CARTESIAN_POINT ( 'NONE',  ( 0.000000000000000000, -2.401522331692820256, -6.999477872697425163 ) ) ;
#1230=CIRCLE ( 'NONE', #8434, 6.499000000000006771 ) ;
#1231=AXIS2_PLACEMENT_3D ( 'NONE', #5096, #3432, #5345 ) ;
#1234=ADVANCED_FACE ( 'NONE', ( #11881 ), #3830, .T. ) ;
#1241=ORIENTED_EDGE ( 'NONE', *, *, #4147, .F. ) ;
#1243=EDGE_CURVE ( 'NONE', #10380, #10576, #4983, .T. ) ;
#1246=DIRECTION ( 'NONE',  ( -1.000000000000000000, 1.010728034814421376E-30, 1.090846720500930387E-30 ) ) ;
#1247=ORIENTED_EDGE ( 'NONE', *, *, #7927, .T. ) ;
#1256=CARTESIAN_POINT ( 'NONE',  ( 19.99999999999999645, 3.238809497145207494, 5.634457741540175313 ) ) ;
#1261=VERTEX_POINT ( 'NONE', #7934 ) ;
#1263=VERTEX_POINT ( 'NONE', #4073 ) ;
#1264=ORIENTED_EDGE ( 'NONE', *, *, #7163, .F. ) ;
#1266=DIRECTION ( 'NONE',  ( -1.000000000000000000, 1.010728034814421376E-30, 1.090846720500930387E-30 ) ) ;
#1270=ORIENTED_EDGE ( 'NONE', *, *, #5502, .T. ) ;
#1273=CARTESIAN_POINT ( 'NONE',  ( 19.99999999999999645, -0.9522442067291300161, 6.508557431545700211 ) ) ;
#1276=FACE_OUTER_BOUND ( 'NONE', #3409, .T. ) ;
#1278=DIRECTION ( 'NONE',  ( 1.000000000000000000, -1.010728034814421376E-30, -1.090846720500930387E-30 ) ) ;
#1281=CIRCLE ( 'NONE', #11371, 7.400000000000011902 ) ;
#1284=AXIS2_PLACEMENT_3D ( 'NONE', #1858, #12691, #3862 ) ;
#1290=CIRCLE ( 'NONE', #3170, 7.400000000000009237 ) ;
#1297=EDGE_LOOP ( 'NONE', ( #2561, #7768, #10724, #11579 ) ) ;
#1299=FACE_OUTER_BOUND ( 'NONE', #4604, .T. ) ;
#1301=CARTESIAN_POINT ( 'NONE',  ( 19.99999999999999645, -0.9522442067291300161, 6.508557431545700211 ) ) ;
#1302=CARTESIAN_POINT ( 'NONE',  ( 19.99999999999997868, -2.385831757338501724, -6.045230171438906730 ) ) ;
#1305=EDGE_CURVE ( 'NONE', #12032, #2862, #9921, .T. ) ;
#1306=CIRCLE ( 'NONE', #1525, 2.800000000000004263 ) ;
#1311=ORIENTED_EDGE ( 'NONE', *, *, #2045, .F. ) ;
#1313=ORIENTED_EDGE ( 'NONE', *, *, #6753, .F. ) ;
#1315=AXIS2_PLACEMENT_3D ( 'NONE', #7370, #11292, #6400 ) ;
#1316=CYLINDRICAL_SURFACE ( 'NONE', #4301, 7.400000000000010125 ) ;
#1324=EDGE_LOOP ( 'NONE', ( #1443, #12016, #2086, #5636 ) ) ;
#1326=AXIS2_PLACEMENT_3D ( 'NONE', #3544, #11648, #9502 ) ;
#1327=VERTEX_POINT ( 'NONE', #2151 ) ;
#1328=ORIENTED_EDGE ( 'NONE', *, *, #2045, .T. ) ;
#1330=CARTESIAN_POINT ( 'NONE',  ( -10.00000000000000178, 0.000000000000000000, 0.000000000000000000 ) ) ;
#1332=EDGE_LOOP ( 'NONE', ( #921, #250, #4664, #1712 ) ) ;
#1335=AXIS2_PLACEMENT_3D ( 'NONE', #7600, #3928, #1865 ) ;
#1337=FACE_OUTER_BOUND ( 'NONE', #10473, .T. ) ;
#1341=DIRECTION ( 'NONE',  ( -1.000000000000000000, 1.010728034814421376E-30, 1.090846720500930387E-30 ) ) ;
#1344=VECTOR ( 'NONE', #7617, 1000.000000000000000 ) ;
#1345=CARTESIAN_POINT ( 'NONE',  ( 9.999999999999998224, 5.025702764809090617, 5.431603052487417038 ) ) ;
#1347=CARTESIAN_POINT ( 'NONE',  ( 19.99999999999997868, -2.099089055167727480, -6.233932467347804263 ) ) ;
#1349=EDGE_CURVE ( 'NONE', #3794, #7169, #6770, .T. ) ;
#1350=AXIS2_PLACEMENT_3D ( 'NONE', #10220, #2335, #1415 ) ;
#1352=CARTESIAN_POINT ( 'NONE',  ( 19.99999999999997868, 4.177097350749889415, -6.108343287861160320 ) ) ;
#1359=AXIS2_PLACEMENT_3D ( 'NONE', #6417, #10457, #8529 ) ;
#1360=AXIS2_PLACEMENT_3D ( 'NONE', #1573, #12281, #5629 ) ;
#1363=DIRECTION ( 'NONE',  ( -1.000000000000000000, 1.010728034814421376E-30, 1.090846720500930387E-30 ) ) ;
#1364=DIRECTION ( 'NONE',  ( -1.000000000000000000, 1.010728034814421376E-30, 1.090846720500930387E-30 ) ) ;
#1365=CARTESIAN_POINT ( 'NONE',  ( 0.000000000000000000, 3.681899619563855808, -5.450844343808915582 ) ) ;
#1366=CARTESIAN_POINT ( 'NONE',  ( 19.99999999999999645, -6.453973581750233279, -0.7636923504069568214 ) ) ;
#1367=CIRCLE ( 'NONE', #11874, 2.800000000000003819 ) ;
#1369=AXIS2_PLACEMENT_3D ( 'NONE', #11425, #2605, #7863 ) ;
#1371=FILL_AREA_STYLE ('',( #11235 ) ) ;
#1374=VERTEX_POINT ( 'NONE', #627 ) ;
#1375=ORIENTED_EDGE ( 'NONE', *, *, #3001, .T. ) ;
#1378=EDGE_LOOP ( 'NONE', ( #7121, #8465, #1600, #2100 ) ) ;
#1379=ORIENTED_EDGE ( 'NONE', *, *, #1046, .F. ) ;
#1382=CARTESIAN_POINT ( 'NONE',  ( 19.99999999999997868, 3.908107171477257058, -5.192658214849914522 ) ) ;
#1386=ORIENTED_EDGE ( 'NONE', *, *, #3946, .F. ) ;
#1387=CARTESIAN_POINT ( 'NONE',  ( 19.99999999999999645, 0.000000000000000000, 0.000000000000000000 ) ) ;
#1389=CYLINDRICAL_SURFACE ( 'NONE', #10685, 2.800000000000003819 ) ;
#1390=ORIENTED_EDGE ( 'NONE', *, *, #11204, .T. ) ;
#1392=ORIENTED_EDGE ( 'NONE', *, *, #4468, .T. ) ;
#1397=VERTEX_POINT ( 'NONE', #3726 ) ;
#1399=DIRECTION ( 'NONE',  ( -1.000000000000000000, 1.010728034814421376E-30, 1.090846720500930387E-30 ) ) ;
#1400=VERTEX_POINT ( 'NONE', #11521 ) ;
#1401=DIRECTION ( 'NONE',  ( 1.000000000000000000, -1.010728034814421376E-30, -1.090846720500930387E-30 ) ) ;
#1405=LINE ( 'NONE', #6114, #6788 ) ;
#1408=CARTESIAN_POINT ( 'NONE',  ( 19.99999999999999645, -4.621065432155107011, 4.569765340993028779 ) ) ;
#1411=CARTESIAN_POINT ( 'NONE',  ( 0.000000000000000000, 1.052479792859144947, -6.413211932068313637 ) ) ;
#1415=DIRECTION ( 'NONE',  ( 0.000000000000000000, 0.4338837391175525693, 0.9009688679024219216 ) ) ;
#1420=CARTESIAN_POINT ( 'NONE',  ( 19.99999999999999645, -0.8135880386783197471, 6.527339685683405612 ) ) ;
#1422=EDGE_CURVE ( 'NONE', #3731, #12527, #3078, .T. ) ;
#1425=VECTOR ( 'NONE', #10437, 1000.000000000000000 ) ;
#1429=CARTESIAN_POINT ( 'NONE',  ( 19.99999999999999645, 0.2252065540229667429, 6.573992004634855668 ) ) ;
#1430=DIRECTION ( 'NONE',  ( 0.000000000000000000, 0.000000000000000000, 1.000000000000000000 ) ) ;
#1432=DIRECTION ( 'NONE',  ( -1.000000000000000000, 1.010728034814421376E-30, 1.090846720500930387E-30 ) ) ;
#1433=AXIS2_PLACEMENT_3D ( 'NONE', #8756, #64, #3989 ) ;
#1436=DIRECTION ( 'NONE',  ( -1.000000000000000000, 1.010728034814421376E-30, 1.090846720500930387E-30 ) ) ;
#1441=ORIENTED_EDGE ( 'NONE', *, *, #1913, .F. ) ;
#1443=ORIENTED_EDGE ( 'NONE', *, *, #8327, .F. ) ;
#1445=CARTESIAN_POINT ( 'NONE',  ( -10.00000000000000178, 0.000000000000000000, 0.000000000000000000 ) ) ;
#1446=EDGE_CURVE ( 'NONE', #2582, #9681, #4705, .T. ) ;
#1447=DIRECTION ( 'NONE',  ( -1.000000000000000000, 1.010728034814421376E-30, 1.090846720500930387E-30 ) ) ;
#1448=ADVANCED_FACE ( 'NONE', ( #566 ), #1782, .T. ) ;
#1451=EDGE_CURVE ( 'NONE', #6667, #11644, #7648, .T. ) ;
#1453=EDGE_LOOP ( 'NONE', ( #9220, #3978, #10581, #435 ) ) ;
#1454=CARTESIAN_POINT ( 'NONE',  ( 9.999999999999994671, -6.969736844459671232, -2.486517307195214244 ) ) ;
#1459=VERTEX_POINT ( 'NONE', #8418 ) ;
#1460=EDGE_LOOP ( 'NONE', ( #11682, #3932, #985, #10990 ) ) ;
#1461=LINE ( 'NONE', #10078, #6448 ) ;
#1465=AXIS2_PLACEMENT_3D ( 'NONE', #9991, #11040, #11890 ) ;
#1466=VERTEX_POINT ( 'NONE', #4497 ) ;
#1468=DIRECTION ( 'NONE',  ( 0.000000000000000000, 0.000000000000000000, 1.000000000000000000 ) ) ;
#1470=AXIS2_PLACEMENT_3D ( 'NONE', #2203, #6124, #10032 ) ;
#1473=ORIENTED_EDGE ( 'NONE', *, *, #1716, .F. ) ;
#1474=ORIENTED_EDGE ( 'NONE', *, *, #3146, .T. ) ;
#1478=CARTESIAN_POINT ( 'NONE',  ( 19.99999999999999645, 0.000000000000000000, 0.000000000000000000 ) ) ;
#1481=ORIENTED_EDGE ( 'NONE', *, *, #5409, .F. ) ;
#1483=CARTESIAN_POINT ( 'NONE',  ( 19.99999999999999645, 0.000000000000000000, 0.000000000000000000 ) ) ;
#1484=DIRECTION ( 'NONE',  ( -1.000000000000000000, 1.010728034814421376E-30, 1.090846720500930387E-30 ) ) ;
#1485=ORIENTED_EDGE ( 'NONE', *, *, #7308, .T. ) ;
#1488=DIRECTION ( 'NONE',  ( -1.000000000000000000, 1.010728034814421376E-30, 1.090846720500930387E-30 ) ) ;
#1489=CIRCLE ( 'NONE', #8063, 2.800000000000003375 ) ;
#1490=DIRECTION ( 'NONE',  ( 0.000000000000000000, 0.000000000000000000, 1.000000000000000000 ) ) ;
#1491=ORIENTED_EDGE ( 'NONE', *, *, #10519, .F. ) ;
#1492=DIRECTION ( 'NONE',  ( -1.000000000000000000, 1.010728034814421376E-30, 1.090846720500930387E-30 ) ) ;
#1493=LINE ( 'NONE', #3326, #11599 ) ;
#1494=AXIS2_PLACEMENT_3D ( 'NONE', #11116, #5067, #2302 ) ;
#1497=DIRECTION ( 'NONE',  ( 1.000000000000000000, -1.010728034814421376E-30, -1.090846720500930387E-30 ) ) ;
#1504=ORIENTED_EDGE ( 'NONE', *, *, #3812, .T. ) ;
#1507=ORIENTED_EDGE ( 'NONE', *, *, #12147, .T. ) ;
#1514=CYLINDRICAL_SURFACE ( 'NONE', #12658, 2.800000000000003819 ) ;
#1515=AXIS2_PLACEMENT_3D ( 'NONE', #11359, #2411, #589 ) ;
#1516=DIRECTION ( 'NONE',  ( -1.000000000000000000, 1.010728034814421376E-30, 1.090846720500930387E-30 ) ) ;
#1518=ORIENTED_EDGE ( 'NONE', *, *, #4952, .T. ) ;
#1519=ADVANCED_FACE ( 'NONE', ( #11896 ), #9936, .T. ) ;
#1521=ORIENTED_EDGE ( 'NONE', *, *, #1893, .T. ) ;
#1525=AXIS2_PLACEMENT_3D ( 'NONE', #1273, #3171, #1150 ) ;
#1526=VERTEX_POINT ( 'NONE', #10851 ) ;
#1528=DIRECTION ( 'NONE',  ( -1.000000000000000000, 1.010728034814421376E-30, 1.090846720500930387E-30 ) ) ;
#1530=LINE ( 'NONE', #6436, #9724 ) ;
#1534=CARTESIAN_POINT ( 'NONE',  ( 0.000000000000000000, 0.000000000000000000, 0.000000000000000000 ) ) ;
#1537=ORIENTED_EDGE ( 'NONE', *, *, #8644, .T. ) ;
#1545=CARTESIAN_POINT ( 'NONE',  ( 19.99999999999999645, -6.182645281642508372, 2.245659411033100294 ) ) ;
#1547=VECTOR ( 'NONE', #10508, 1000.000000000000000 ) ;
#1550=DIRECTION ( 'NONE',  ( -1.000000000000000000, 1.010728034814421376E-30, 1.090846720500930387E-30 ) ) ;
#1559=EDGE_CURVE ( 'NONE', #3892, #1466, #1622, .T. ) ;
#1565=( LENGTH_UNIT ( ) NAMED_UNIT ( * ) SI_UNIT ( .MILLI., .METRE. ) );
#1568=LINE ( 'NONE', #9162, #6405 ) ;
#1570=ORIENTED_EDGE ( 'NONE', *, *, #5694, .F. ) ;
#1572=CARTESIAN_POINT ( 'NONE',  ( 19.99999999999999645, 0.000000000000000000, 0.000000000000000000 ) ) ;
#1573=CARTESIAN_POINT ( 'NONE',  ( 0.000000000000000000, -3.055252325922224621, 5.825248672282130613 ) ) ;
#1578=VECTOR ( 'NONE', #6610, 1000.000000000000000 ) ;
#1579=CYLINDRICAL_SURFACE ( 'NONE', #6904, 6.499000000000010324 ) ;
#1591=DIRECTION ( 'NONE',  ( 0.000000000000000000, 0.1785568947986369281, -0.9839295885986296675 ) ) ;
#1592=FACE_OUTER_BOUND ( 'NONE', #11349, .T. ) ;
#1595=EDGE_CURVE ( 'NONE', #1400, #5017, #4510, .T. ) ;
#1596=DIRECTION ( 'NONE',  ( -1.257247067695985813E-30, 0.9749279121818227312, 0.2225209339563182509 ) ) ;
#1598=DIRECTION ( 'NONE',  ( -1.000000000000000000, 1.010728034814421376E-30, 1.090846720500930387E-30 ) ) ;
#1600=ORIENTED_EDGE ( 'NONE', *, *, #6359, .F. ) ;
#1601=ORIENTED_EDGE ( 'NONE', *, *, #5372, .T. ) ;
#1602=DIRECTION ( 'NONE',  ( 0.000000000000000000, 0.000000000000000000, 1.000000000000000000 ) ) ;
#1605=DIRECTION ( 'NONE',  ( -1.000000000000000000, 1.010728034814421376E-30, 1.090846720500930387E-30 ) ) ;
#1608=EDGE_CURVE ( 'NONE', #4761, #363, #2464, .T. ) ;
#1609=CARTESIAN_POINT ( 'NONE',  ( -2.727116801252319662E-30, 5.510332127717284397E-15, -2.499999999999999556 ) ) ;
#1613=DIRECTION ( 'NONE',  ( 0.000000000000000000, 0.000000000000000000, 1.000000000000000000 ) ) ;
#1619=CARTESIAN_POINT ( 'NONE',  ( 0.000000000000000000, 5.895746314278409450, 2.916892913127012488 ) ) ;
#1620=FACE_OUTER_BOUND ( 'NONE', #6017, .T. ) ;
#1622=CIRCLE ( 'NONE', #5741, 7.400000000000009237 ) ;
#1623=CARTESIAN_POINT ( 'NONE',  ( 0.000000000000000000, 0.000000000000000000, 0.000000000000000000 ) ) ;
#1627=CARTESIAN_POINT ( 'NONE',  ( 19.99999999999999645, -5.774092856145738750, 2.982759240804856660 ) ) ;
#1628=AXIS2_PLACEMENT_3D ( 'NONE', #7984, #7866, #2997 ) ;
#1629=AXIS2_PLACEMENT_3D ( 'NONE', #12368, #1722, #8543 ) ;
#1631=DIRECTION ( 'NONE',  ( -1.000000000000000000, 1.010728034814421376E-30, 1.090846720500930387E-30 ) ) ;
#1633=ORIENTED_EDGE ( 'NONE', *, *, #12507, .T. ) ;
#1635=CYLINDRICAL_SURFACE ( 'NONE', #2337, 7.400000000000010125 ) ;
#1638=DIRECTION ( 'NONE',  ( 1.140150527077241873E-30, 0.000000000000000000, -1.000000000000000000 ) ) ;
#1640=CIRCLE ( 'NONE', #11928, 2.800000000000004263 ) ;
#1642=CARTESIAN_POINT ( 'NONE',  ( 19.99999999999999645, 2.918117354836642363, 5.807029542149858337 ) ) ;
#1643=ORIENTED_EDGE ( 'NONE', *, *, #454, .F. ) ;
#1646=CYLINDRICAL_SURFACE ( 'NONE', #11537, 7.400000000000010125 ) ;
#1648=EDGE_LOOP ( 'NONE', ( #4098, #11451, #3860, #9831 ) ) ;
#1649=CARTESIAN_POINT ( 'NONE',  ( 9.999999999999998224, 0.2110513566294528187, -7.396989747516558467 ) ) ;
#1650=EDGE_LOOP ( 'NONE', ( #4150, #4153, #284, #4995 ) ) ;
#1654=CIRCLE ( 'NONE', #4737, 2.800000000000003819 ) ;
#1657=ORIENTED_EDGE ( 'NONE', *, *, #6911, .F. ) ;
#1658=CARTESIAN_POINT ( 'NONE',  ( 19.99999999999997868, 3.238809497145301197, -5.634457741540144227 ) ) ;
#1659=LINE ( 'NONE', #5460, #10280 ) ;
#1660=EDGE_CURVE ( 'NONE', #9362, #4951, #10461, .T. ) ;
#1665=EDGE_CURVE ( 'NONE', #8569, #4277, #1189, .T. ) ;
#1666=FACE_OUTER_BOUND ( 'NONE', #11127, .T. ) ;
#1669=ORIENTED_EDGE ( 'NONE', *, *, #11869, .F. ) ;
#1674=DIRECTION ( 'NONE',  ( -1.000000000000000000, 1.010728034814421376E-30, 1.090846720500930387E-30 ) ) ;
#1678=AXIS2_PLACEMENT_3D ( 'NONE', #7119, #2227, #221 ) ;
#1681=CARTESIAN_POINT ( 'NONE',  ( 19.99999999999999645, 0.000000000000000000, 0.000000000000000000 ) ) ;
#1682=LINE ( 'NONE', #4589, #9483 ) ;
#1684=ADVANCED_FACE ( 'NONE', ( #3216 ), #1316, .T. ) ;
#1685=CYLINDRICAL_SURFACE ( 'NONE', #3911, 2.800000000000003819 ) ;
#1689=FACE_OUTER_BOUND ( 'NONE', #9355, .T. ) ;
#1690=DIRECTION ( 'NONE',  ( -1.000000000000000000, 1.010728034814421376E-30, 1.090846720500930387E-30 ) ) ;
#1692=DIRECTION ( 'NONE',  ( 1.000000000000000000, -1.010728034814421376E-30, -1.090846720500930387E-30 ) ) ;
#1694=ORIENTED_EDGE ( 'NONE', *, *, #2030, .F. ) ;
#1695=EDGE_CURVE ( 'NONE', #6900, #3787, #2674, .T. ) ;
#1697=ORIENTED_EDGE ( 'NONE', *, *, #1717, .F. ) ;
#1699=AXIS2_PLACEMENT_3D ( 'NONE', #2942, #5880, #4917 ) ;
#1703=FACE_OUTER_BOUND ( 'NONE', #1332, .T. ) ;
#1709=CARTESIAN_POINT ( 'NONE',  ( 0.000000000000000000, 0.000000000000000000, 0.000000000000000000 ) ) ;
#1711=VECTOR ( 'NONE', #12408, 1000.000000000000000 ) ;
#1712=ORIENTED_EDGE ( 'NONE', *, *, #2405, .T. ) ;
#1713=CARTESIAN_POINT ( 'NONE',  ( 0.000000000000000000, -5.362766118793872216, 3.671204237728608266 ) ) ;
#1716=EDGE_CURVE ( 'NONE', #5117, #1836, #10245, .T. ) ;
#1717=EDGE_CURVE ( 'NONE', #9801, #3793, #601, .T. ) ;
#1718=CYLINDRICAL_SURFACE ( 'NONE', #6790, 2.800000000000003819 ) ;
#1722=DIRECTION ( 'NONE',  ( -1.000000000000000000, 1.010728034814421376E-30, 1.090846720500930387E-30 ) ) ;
#1725=CARTESIAN_POINT ( 'NONE',  ( 0.000000000000000000, 6.613766744932247477, 3.319350756342029474 ) ) ;
#1726=ADVANCED_FACE ( 'NONE', ( #8797 ), #12739, .T. ) ;
#1729=ORIENTED_EDGE ( 'NONE', *, *, #8152, .T. ) ;
#1730=AXIS2_PLACEMENT_3D ( 'NONE', #8509, #7743, #1080 ) ;
#1733=CYLINDRICAL_SURFACE ( 'NONE', #7269, 7.400000000000010125 ) ;
#1736=CIRCLE ( 'NONE', #9323, 2.800000000000002931 ) ;
#1740=DIRECTION ( 'NONE',  ( 0.000000000000000000, 0.000000000000000000, 1.000000000000000000 ) ) ;
#1744=ORIENTED_EDGE ( 'NONE', *, *, #3604, .T. ) ;
#1745=AXIS2_PLACEMENT_3D ( 'NONE', #6437, #3358, #1468 ) ;
#1747=LINE ( 'NONE', #5613, #2900 ) ;
#1748=CARTESIAN_POINT ( 'NONE',  ( -10.00000000000000178, 0.000000000000000000, 0.000000000000000000 ) ) ;
#1749=EDGE_CURVE ( 'NONE', #3985, #10901, #874, .T. ) ;
#1750=LINE ( 'NONE', #844, #10761 ) ;
#1751=AXIS2_PLACEMENT_3D ( 'NONE', #634, #5467, #4438 ) ;
#1752=CARTESIAN_POINT ( 'NONE',  ( 19.99999999999999645, 0.000000000000000000, 0.000000000000000000 ) ) ;
#1756=DIRECTION ( 'NONE',  ( 6.902532920683843663E-31, -0.9749279121818259508, 0.2225209339563040956 ) ) ;
#1757=EDGE_CURVE ( 'NONE', #9234, #4686, #5709, .T. ) ;
#1758=LINE ( 'NONE', #3575, #2566 ) ;
#1761=ORIENTED_EDGE ( 'NONE', *, *, #646, .F. ) ;
#1762=CIRCLE ( 'NONE', #117, 7.400000000000009237 ) ;
#1765=DIRECTION ( 'NONE',  ( -2.280301054154484185E-31, -0.5877852522924801315, 0.8090169943749423442 ) ) ;
#1767=CARTESIAN_POINT ( 'NONE',  ( 19.99999999999999645, 0.4528593230174772222, 7.386130139224198921 ) ) ;
#1768=CARTESIAN_POINT ( 'NONE',  ( 0.000000000000000000, 6.146182963951696721, -2.112211157443803611 ) ) ;
#1769=ORIENTED_EDGE ( 'NONE', *, *, #9334, .F. ) ;
#1771=ADVANCED_FACE ( 'NONE', ( #809 ), #1905, .T. ) ;
#1773=CYLINDRICAL_SURFACE ( 'NONE', #8442, 7.400000000000010125 ) ;
#1774=ORIENTED_EDGE ( 'NONE', *, *, #6435, .F. ) ;
#1777=ORIENTED_EDGE ( 'NONE', *, *, #10672, .F. ) ;
#1778=VERTEX_POINT ( 'NONE', #6875 ) ;
#1780=CARTESIAN_POINT ( 'NONE',  ( -10.00000000000000178, 0.000000000000000000, 0.000000000000000000 ) ) ;
#1781=ORIENTED_EDGE ( 'NONE', *, *, #2838, .T. ) ;
#1782=CYLINDRICAL_SURFACE ( 'NONE', #3494, 2.800000000000003819 ) ;
#1785=CARTESIAN_POINT ( 'NONE',  ( 9.999999999999998224, 6.613766744932301656, -3.319350756341945985 ) ) ;
#1786=CYLINDRICAL_SURFACE ( 'NONE', #8936, 2.800000000000003819 ) ;
#1788=DIRECTION ( 'NONE',  ( 0.000000000000000000, 0.000000000000000000, 1.000000000000000000 ) ) ;
#1789=EDGE_CURVE ( 'NONE', #5127, #3630, #7770, .T. ) ;
#1791=AXIS2_PLACEMENT_3D ( 'NONE', #10565, #10692, #4781 ) ;
#1800=AXIS2_PLACEMENT_3D ( 'NONE', #5396, #4500, #5649 ) ;
#1801=EDGE_CURVE ( 'NONE', #4676, #3717, #5748, .T. ) ;
#1802=ADVANCED_FACE ( 'NONE', ( #747 ), #7645, .T. ) ;
#1803=CARTESIAN_POINT ( 'NONE',  ( 0.000000000000000000, 0.000000000000000000, 0.000000000000000000 ) ) ;
#1804=LINE ( 'NONE', #5917, #5550 ) ;
#1806=CARTESIAN_POINT ( 'NONE',  ( 0.000000000000000000, 6.018220532833807646, -2.453165835849195453 ) ) ;
#1809=DIRECTION ( 'NONE',  ( -1.000000000000000000, 1.010728034814421376E-30, 1.090846720500930387E-30 ) ) ;
#1810=CARTESIAN_POINT ( 'NONE',  ( 0.000000000000000000, -4.155687294075626426, 5.098857909653524700 ) ) ;
#1811=DIRECTION ( 'NONE',  ( 0.000000000000000000, 0.000000000000000000, 1.000000000000000000 ) ) ;
#1812=DIRECTION ( 'NONE',  ( 0.000000000000000000, 0.000000000000000000, 1.000000000000000000 ) ) ;
#1813=DIRECTION ( 'NONE',  ( -1.000000000000000000, 1.010728034814421376E-30, 1.090846720500930387E-30 ) ) ;
#1815=DIRECTION ( 'NONE',  ( -1.000000000000000000, 1.010728034814421376E-30, 1.090846720500930387E-30 ) ) ;
#1816=ADVANCED_FACE ( 'NONE', ( #3783 ), #1718, .T. ) ;
#1830=AXIS2_PLACEMENT_3D ( 'NONE', #4258, #12127, #4322 ) ;
#1833=ORIENTED_EDGE ( 'NONE', *, *, #9129, .F. ) ;
#1835=FACE_OUTER_BOUND ( 'NONE', #7253, .T. ) ;
#1836=VERTEX_POINT ( 'NONE', #4809 ) ;
#1838=EDGE_CURVE ( 'NONE', #4793, #2771, #197, .T. ) ;
#1841=CARTESIAN_POINT ( 'NONE',  ( 19.99999999999999645, -6.459281472512932609, -1.243290685169442966 ) ) ;
#1845=CIRCLE ( 'NONE', #9850, 6.499000000000008548 ) ;
#1847=EDGE_CURVE ( 'NONE', #7505, #11033, #6165, .T. ) ;
#1848=LINE ( 'NONE', #10657, #1912 ) ;
#1849=VERTEX_POINT ( 'NONE', #4219 ) ;
#1851=LINE ( 'NONE', #1785, #10008 ) ;
#1853=VECTOR ( 'NONE', #6550, 1000.000000000000000 ) ;
#1857=ORIENTED_EDGE ( 'NONE', *, *, #3811, .F. ) ;
#1858=CARTESIAN_POINT ( 'NONE',  ( 0.000000000000000000, 2.520781513113740324, -6.075668640744172677 ) ) ;
#1860=EDGE_LOOP ( 'NONE', ( #689, #1241, #5697, #1744 ) ) ;
#1863=DIRECTION ( 'NONE',  ( 0.000000000000000000, 0.5128992774059070170, -0.8584487936018656562 ) ) ;
#1865=DIRECTION ( 'NONE',  ( -1.140150527077241873E-30, 0.000000000000000000, 1.000000000000000000 ) ) ;
#1876=DIRECTION ( 'NONE',  ( 0.000000000000000000, 0.000000000000000000, 1.000000000000000000 ) ) ;
#1878=FACE_OUTER_BOUND ( 'NONE', #1378, .T. ) ;
#1879=CARTESIAN_POINT ( 'NONE',  ( 0.000000000000000000, -3.399584271718375739, 6.572885726945587592 ) ) ;
#1881=CARTESIAN_POINT ( 'NONE',  ( 19.99999999999997868, 6.321830586517952710, -1.817291089601262621 ) ) ;
#1883=CIRCLE ( 'NONE', #6833, 6.499000000000008548 ) ;
#1884=LINE ( 'NONE', #9470, #12385 ) ;
#1888=CARTESIAN_POINT ( 'NONE',  ( 19.99999999999997868, 2.649444137877677186, -6.020675595748665287 ) ) ;
#1892=ORIENTED_EDGE ( 'NONE', *, *, #4957, .T. ) ;
#1893=EDGE_CURVE ( 'NONE', #5416, #41, #1845, .T. ) ;
#1897=DIRECTION ( 'NONE',  ( -1.000000000000000000, 1.010728034814421376E-30, 1.090846720500930387E-30 ) ) ;
#1900=DIRECTION ( 'NONE',  ( -1.000000000000000000, 1.010728034814421376E-30, 1.090846720500930387E-30 ) ) ;
#1901=VERTEX_POINT ( 'NONE', #9996 ) ;
#1902=ORIENTED_EDGE ( 'NONE', *, *, #1349, .T. ) ;
#1903=CIRCLE ( 'NONE', #669, 2.800000000000003819 ) ;
#1904=AXIS2_PLACEMENT_3D ( 'NONE', #1014, #3921, #11906 ) ;
#1905=CYLINDRICAL_SURFACE ( 'NONE', #11093, 2.800000000000003819 ) ;
#1909=ORIENTED_EDGE ( 'NONE', *, *, #10219, .F. ) ;
#1912=VECTOR ( 'NONE', #6942, 1000.000000000000000 ) ;
#1913=EDGE_CURVE ( 'NONE', #3292, #11603, #1187, .T. ) ;
#1914=EDGE_CURVE ( 'NONE', #10811, #9165, #1640, .T. ) ;
#1920=ORIENTED_EDGE ( 'NONE', *, *, #3854, .F. ) ;
#1925=AXIS2_PLACEMENT_3D ( 'NONE', #3817, #1401, #11266 ) ;
#1928=CYLINDRICAL_SURFACE ( 'NONE', #6172, 7.400000000000010125 ) ;
#1929=ORIENTED_EDGE ( 'NONE', *, *, #5468, .F. ) ;
#1930=CARTESIAN_POINT ( 'NONE',  ( 19.99999999999997868, 0.6915992404090851586, -6.462096524400249287 ) ) ;
#1931=SURFACE_SIDE_STYLE ('',( #11015 ) ) ;
#1935=DIRECTION ( 'NONE',  ( 0.000000000000000000, 0.000000000000000000, 1.000000000000000000 ) ) ;
#1939=ADVANCED_FACE ( 'NONE', ( #6937 ), #4999, .T. ) ;
#1946=AXIS2_PLACEMENT_3D ( 'NONE', #3484, #11269, #5334 ) ;
#1948=VECTOR ( 'NONE', #2107, 1000.000000000000000 ) ;
#1951=DIRECTION ( 'NONE',  ( -1.000000000000000000, 1.010728034814421376E-30, 1.090846720500930387E-30 ) ) ;
#1955=DIRECTION ( 'NONE',  ( 0.000000000000000000, 0.000000000000000000, 1.000000000000000000 ) ) ;
#1956=AXIS2_PLACEMENT_3D ( 'NONE', #704, #10495, #12187 ) ;
#1963=ORIENTED_EDGE ( 'NONE', *, *, #11213, .F. ) ;
#1965=ORIENTED_EDGE ( 'NONE', *, *, #7963, .F. ) ;
#1968=ORIENTED_EDGE ( 'NONE', *, *, #6206, .F. ) ;
#1969=DIRECTION ( 'NONE',  ( -1.000000000000000000, 1.010728034814421376E-30, 1.090846720500930387E-30 ) ) ;
#1970=CARTESIAN_POINT ( 'NONE',  ( 0.000000000000000000, 3.908107171477253505, -5.192658214849918075 ) ) ;
#1975=ORIENTED_EDGE ( 'NONE', *, *, #12321, .T. ) ;
#1982=DIRECTION ( 'NONE',  ( 0.000000000000000000, 0.000000000000000000, 1.000000000000000000 ) ) ;
#1983=EDGE_LOOP ( 'NONE', ( #1087, #486, #3233, #4564 ) ) ;
#1985=CIRCLE ( 'NONE', #1169, 7.400000000000011902 ) ;
#1987=CARTESIAN_POINT ( 'NONE',  ( 0.000000000000000000, 0.000000000000000000, 0.000000000000000000 ) ) ;
#1988=ORIENTED_EDGE ( 'NONE', *, *, #3075, .T. ) ;
#1992=DIRECTION ( 'NONE',  ( 0.000000000000000000, 0.000000000000000000, 1.000000000000000000 ) ) ;
#1995=VECTOR ( 'NONE', #5411, 1000.000000000000000 ) ;
#1996=CIRCLE ( 'NONE', #9193, 7.400000000000009237 ) ;
#1997=ADVANCED_FACE ( 'NONE', ( #6997 ), #2099, .T. ) ;
#1998=CARTESIAN_POINT ( 'NONE',  ( 19.99999999999999645, 5.956456411769392112, 2.790827096699012522 ) ) ;
#2000=EDGE_CURVE ( 'NONE', #5523, #6000, #3096, .T. ) ;
#2001=DIRECTION ( 'NONE',  ( 1.000000000000000000, -1.010728034814421376E-30, -1.090846720500930387E-30 ) ) ;
#2005=EDGE_CURVE ( 'NONE', #3964, #1526, #10483, .T. ) ;
#2006=DIRECTION ( 'NONE',  ( -1.000000000000000000, 1.010728034814421376E-30, 1.090846720500930387E-30 ) ) ;
#2008=DIRECTION ( 'NONE',  ( 1.000000000000000000, -1.010728034814421376E-30, -1.090846720500930387E-30 ) ) ;
#2009=EDGE_LOOP ( 'NONE', ( #11304, #3949, #12355, #174 ) ) ;
#2010=CARTESIAN_POINT ( 'NONE',  ( 19.99999999999999645, -3.055252325922228174, 5.825248672282130613 ) ) ;
#2013=CARTESIAN_POINT ( 'NONE',  ( 9.999999999999998224, 3.975087478966649712, 6.241688836730239665 ) ) ;
#2014=CARTESIAN_POINT ( 'NONE',  ( 0.000000000000000000, 0.000000000000000000, 0.000000000000000000 ) ) ;
#2020=VERTEX_POINT ( 'NONE', #10849 ) ;
#2022=DIRECTION ( 'NONE',  ( 0.000000000000000000, 0.000000000000000000, 1.000000000000000000 ) ) ;
#2024=ORIENTED_EDGE ( 'NONE', *, *, #4685, .T. ) ;
#2028=EDGE_CURVE ( 'NONE', #2020, #2096, #6368, .T. ) ;
#2030=EDGE_CURVE ( 'NONE', #3319, #2041, #1747, .T. ) ;
#2031=DIRECTION ( 'NONE',  ( -1.000000000000000000, 1.010728034814421376E-30, 1.090846720500930387E-30 ) ) ;
#2032=EDGE_LOOP ( 'NONE', ( #3642, #6100, #12638, #3784 ) ) ;
#2034=CIRCLE ( 'NONE', #1213, 6.499000000000009436 ) ;
#2035=CYLINDRICAL_SURFACE ( 'NONE', #7555, 2.800000000000003819 ) ;
#2036=DIRECTION ( 'NONE',  ( 0.000000000000000000, 0.000000000000000000, 1.000000000000000000 ) ) ;
#2039=ORIENTED_EDGE ( 'NONE', *, *, #6604, .T. ) ;
#2040=AXIS2_PLACEMENT_3D ( 'NONE', #645, #10362, #1740 ) ;
#2041=VERTEX_POINT ( 'NONE', #5673 ) ;
#2043=AXIS2_PLACEMENT_3D ( 'NONE', #8736, #12677, #11697 ) ;
#2045=EDGE_CURVE ( 'NONE', #6829, #742, #10054, .T. ) ;
#2048=ORIENTED_EDGE ( 'NONE', *, *, #9917, .F. ) ;
#2051=EDGE_CURVE ( 'NONE', #7451, #12421, #7675, .T. ) ;
#2053=AXIS2_PLACEMENT_3D ( 'NONE', #5932, #5874, #18 ) ;
#2054=VECTOR ( 'NONE', #969, 1000.000000000000000 ) ;
#2055=EDGE_CURVE ( 'NONE', #7946, #5257, #4725, .T. ) ;
#2060=EDGE_LOOP ( 'NONE', ( #7767, #6994, #3073, #6097 ) ) ;
#2061=DIRECTION ( 'NONE',  ( 1.140150527077241873E-30, 0.000000000000000000, -1.000000000000000000 ) ) ;
#2063=VECTOR ( 'NONE', #7763, 1000.000000000000000 ) ;
#2067=EDGE_CURVE ( 'NONE', #11719, #825, #10881, .T. ) ;
#2068=FACE_OUTER_BOUND ( 'NONE', #2362, .T. ) ;
#2069=CARTESIAN_POINT ( 'NONE',  ( 9.999999999999994671, -6.413745496774073906, -3.691052519622338490 ) ) ;
#2070=CARTESIAN_POINT ( 'NONE',  ( 19.99999999999999645, -3.426907987218856810, 5.522074125465504579 ) ) ;
#2074=EDGE_CURVE ( 'NONE', #11856, #4356, #7599, .T. ) ;
#2076=EDGE_CURVE ( 'NONE', #8334, #4606, #9637, .T. ) ;
#2078=DIRECTION ( 'NONE',  ( -1.000000000000000000, 1.010728034814421376E-30, 1.090846720500930387E-30 ) ) ;
#2080=ORIENTED_EDGE ( 'NONE', *, *, #9076, .F. ) ;
#2081=ORIENTED_EDGE ( 'NONE', *, *, #10640, .T. ) ;
#2082=CARTESIAN_POINT ( 'NONE',  ( 0.000000000000000000, 4.177097350749890303, -6.108343287861167425 ) ) ;
#2083=DIRECTION ( 'NONE',  ( -1.000000000000000000, 1.010728034814421376E-30, 1.090846720500930387E-30 ) ) ;
#2085=DIRECTION ( 'NONE',  ( -1.000000000000000000, 1.010728034814421376E-30, 1.090846720500930387E-30 ) ) ;
#2086=ORIENTED_EDGE ( 'NONE', *, *, #10039, .T. ) ;
#2090=CIRCLE ( 'NONE', #5171, 6.499000000000009436 ) ;
#2091=CARTESIAN_POINT ( 'NONE',  ( -10.00000000000000178, 0.000000000000000000, 0.000000000000000000 ) ) ;
#2094=ORIENTED_EDGE ( 'NONE', *, *, #368, .F. ) ;
#2095=DIRECTION ( 'NONE',  ( -1.000000000000000000, 1.010728034814421376E-30, 1.090846720500930387E-30 ) ) ;
#2096=VERTEX_POINT ( 'NONE', #12516 ) ;
#2097=ORIENTED_EDGE ( 'NONE', *, *, #5025, .T. ) ;
#2099=CYLINDRICAL_SURFACE ( 'NONE', #4316, 7.400000000000010125 ) ;
#2100=ORIENTED_EDGE ( 'NONE', *, *, #8298, .F. ) ;
#2102=ADVANCED_FACE ( 'NONE', ( #7546 ), #1685, .T. ) ;
#2105=VERTEX_POINT ( 'NONE', #716 ) ;
#2107=DIRECTION ( 'NONE',  ( -1.000000000000000000, 1.010728034814421376E-30, 1.090846720500930387E-30 ) ) ;
#2108=ORIENTED_EDGE ( 'NONE', *, *, #12483, .T. ) ;
#2110=EDGE_CURVE ( 'NONE', #229, #3731, #11310, .T. ) ;
#2113=CIRCLE ( 'NONE', #52, 2.800000000000003819 ) ;
#2114=ADVANCED_FACE ( 'NONE', ( #11552 ), #3566, .T. ) ;
#2115=ORIENTED_EDGE ( 'NONE', *, *, #3812, .F. ) ;
#2116=ADVANCED_FACE ( 'NONE', ( #9461 ), #3629, .T. ) ;
#2119=VERTEX_POINT ( 'NONE', #8576 ) ;
#2120=EDGE_CURVE ( 'NONE', #3178, #1849, #7206, .T. ) ;
#2123=DIRECTION ( 'NONE',  ( -1.000000000000000000, 1.010728034814421376E-30, 1.090846720500930387E-30 ) ) ;
#2125=CARTESIAN_POINT ( 'NONE',  ( 19.99999999999999645, -4.518585619147844845, -5.860237538055132589 ) ) ;
#2126=CARTESIAN_POINT ( 'NONE',  ( 19.99999999999999645, 0.000000000000000000, 0.000000000000000000 ) ) ;
#2132=( LENGTH_UNIT ( ) NAMED_UNIT ( * ) SI_UNIT ( .MILLI., .METRE. ) );
#2135=CIRCLE ( 'NONE', #9516, 2.800000000000002931 ) ;
#2136=FACE_OUTER_BOUND ( 'NONE', #5986, .T. ) ;
#2139=LINE ( 'NONE', #3943, #3312 ) ;
#2141=CARTESIAN_POINT ( 'NONE',  ( 0.000000000000000000, 2.796709610837340598, 6.851161606081848987 ) ) ;
#2142=CIRCLE ( 'NONE', #10562, 7.400000000000009237 ) ;
#2144=APPLICATION_CONTEXT ( 'automotive_design' ) ;
#2146=FACE_OUTER_BOUND ( 'NONE', #7765, .T. ) ;
#2149=AXIS2_PLACEMENT_3D ( 'NONE', #5413, #5544, #12384 ) ;
#2151=CARTESIAN_POINT ( 'NONE',  ( 0.000000000000000000, -1.268072931708545736, 6.374087545670214183 ) ) ;
#2154=CIRCLE ( 'NONE', #8323, 2.800000000000003819 ) ;
#2159=DIRECTION ( 'NONE',  ( -1.000000000000000000, 1.010728034814421376E-30, 1.090846720500930387E-30 ) ) ;
#2162=VERTEX_POINT ( 'NONE', #12325 ) ;
#2164=AXIS2_PLACEMENT_3D ( 'NONE', #10726, #8862, #5970 ) ;
#2168=CARTESIAN_POINT ( 'NONE',  ( 19.99999999999997868, 0.2252065540230664964, -6.573992004634869879 ) ) ;
#2169=EDGE_CURVE ( 'NONE', #2162, #10498, #1654, .T. ) ;
#2173=CARTESIAN_POINT ( 'NONE',  ( 9.999999999999994671, -1.113123845672416401, 7.315801754025030412 ) ) ;
#2175=CARTESIAN_POINT ( 'NONE',  ( 19.99999999999999645, -6.486618105788070743, -0.4009819817180210189 ) ) ;
#2176=CIRCLE ( 'NONE', #4432, 6.499000000000008548 ) ;
#2178=ORIENTED_EDGE ( 'NONE', *, *, #5293, .T. ) ;
#2179=ORIENTED_EDGE ( 'NONE', *, *, #10492, .F. ) ;
#2187=EDGE_CURVE ( 'NONE', #3764, #6793, #6906, .T. ) ;
#2188=FACE_OUTER_BOUND ( 'NONE', #12740, .T. ) ;
#2191=VECTOR ( 'NONE', #2556, 1000.000000000000000 ) ;
#2192=DIRECTION ( 'NONE',  ( -1.000000000000000000, 1.010728034814421376E-30, 1.090846720500930387E-30 ) ) ;
#2197=ORIENTED_EDGE ( 'NONE', *, *, #414, .F. ) ;
#2199=( NAMED_UNIT ( * ) SI_UNIT ( $, .STERADIAN. ) SOLID_ANGLE_UNIT ( ) );
#2201=AXIS2_PLACEMENT_3D ( 'NONE', #7197, #11119, #2305 ) ;
#2202=EDGE_CURVE ( 'NONE', #2374, #7064, #6800, .T. ) ;
#2203=CARTESIAN_POINT ( 'NONE',  ( 19.99999999999999645, 0.000000000000000000, 0.000000000000000000 ) ) ;
#2208=CARTESIAN_POINT ( 'NONE',  ( 0.000000000000000000, 2.796709610837448068, -6.851161606081825006 ) ) ;
#2215=DIRECTION ( 'NONE',  ( -1.000000000000000000, 1.010728034814421376E-30, 1.090846720500930387E-30 ) ) ;
#2216=DIRECTION ( 'NONE',  ( -8.073498326871283938E-31, -0.2660368455666825005, 0.9639628606958513535 ) ) ;
#2217=DIRECTION ( 'NONE',  ( -1.000000000000000000, 1.010728034814421376E-30, 1.090846720500930387E-30 ) ) ;
#2218=DIRECTION ( 'NONE',  ( 0.000000000000000000, 0.9989930665413144784, 0.04486483035051876817 ) ) ;
#2221=ADVANCED_FACE ( 'NONE', ( #8948 ), #10813, .T. ) ;
#2224=EDGE_CURVE ( 'NONE', #6542, #8459, #3712, .T. ) ;
#2227=DIRECTION ( 'NONE',  ( -1.000000000000000000, 1.010728034814421376E-30, 1.090846720500930387E-30 ) ) ;
#2228=VERTEX_POINT ( 'NONE', #8764 ) ;
#2229=ORIENTED_EDGE ( 'NONE', *, *, #4099, .F. ) ;
#2234=ORIENTED_EDGE ( 'NONE', *, *, #7074, .F. ) ;
#2235=CARTESIAN_POINT ( 'NONE',  ( 19.99999999999997868, -3.178467454237100309, -5.758943784352606343 ) ) ;
#2237=CARTESIAN_POINT ( 'NONE',  ( 0.000000000000000000, 6.424561140605085541, 0.9808237102696959475 ) ) ;
#2239=ORIENTED_EDGE ( 'NONE', *, *, #11747, .F. ) ;
#2242=VERTEX_POINT ( 'NONE', #11801 ) ;
#2243=ADVANCED_FACE ( 'NONE', ( #7029 ), #5797, .T. ) ;
#2245=VERTEX_POINT ( 'NONE', #4902 ) ;
#2248=VECTOR ( 'NONE', #1900, 1000.000000000000000 ) ;
#2251=DIRECTION ( 'NONE',  ( 0.000000000000000000, 0.000000000000000000, 1.000000000000000000 ) ) ;
#2259=EDGE_LOOP ( 'NONE', ( #7198, #5294, #108, #7736 ) ) ;
#2260=CARTESIAN_POINT ( 'NONE',  ( 3.054370817402599269E-30, -6.577476285968334224, 2.730038749994992742 ) ) ;
#2261=EDGE_CURVE ( 'NONE', #11340, #4626, #5032, .T. ) ;
#2263=DIRECTION ( 'NONE',  ( -1.000000000000000000, 1.010728034814421376E-30, 1.090846720500930387E-30 ) ) ;
#2266=AXIS2_PLACEMENT_3D ( 'NONE', #2126, #6048, #9959 ) ;
#2267=CIRCLE ( 'NONE', #2053, 2.800000000000003819 ) ;
#2268=AXIS2_PLACEMENT_3D ( 'NONE', #2737, #9587, #2538 ) ;
#2274=DIRECTION ( 'NONE',  ( -1.000000000000000000, 1.010728034814421376E-30, 1.090846720500930387E-30 ) ) ;
#2276=AXIS2_PLACEMENT_3D ( 'NONE', #5092, #4833, #11795 ) ;
#2278=EDGE_CURVE ( 'NONE', #6542, #6552, #7978, .T. ) ;
#2280=EDGE_CURVE ( 'NONE', #11065, #6291, #12156, .T. ) ;
#2281=ORIENTED_EDGE ( 'NONE', *, *, #2261, .T. ) ;
#2288=ORIENTED_EDGE ( 'NONE', *, *, #11408, .F. ) ;
#2290=FACE_OUTER_BOUND ( 'NONE', #9866, .T. ) ;
#2293=DIRECTION ( 'NONE',  ( -1.000000000000000000, 1.010728034814421376E-30, 1.090846720500930387E-30 ) ) ;
#2294=ORIENTED_EDGE ( 'NONE', *, *, #6065, .F. ) ;
#2298=DIRECTION ( 'NONE',  ( -1.000000000000000000, 1.010728034814421376E-30, 1.090846720500930387E-30 ) ) ;
#2302=DIRECTION ( 'NONE',  ( 0.000000000000000000, 0.000000000000000000, 1.000000000000000000 ) ) ;
#2305=DIRECTION ( 'NONE',  ( 0.000000000000000000, 0.000000000000000000, 1.000000000000000000 ) ) ;
#2309=EDGE_LOOP ( 'NONE', ( #1929, #8849, #11954, #2723 ) ) ;
#2311=ORIENTED_EDGE ( 'NONE', *, *, #8517, .F. ) ;
#2314=CIRCLE ( 'NONE', #11775, 2.800000000000002931 ) ;
#2317=CYLINDRICAL_SURFACE ( 'NONE', #6387, 7.400000000000010125 ) ;
#2318=ORIENTED_EDGE ( 'NONE', *, *, #4711, .T. ) ;
#2320=ADVANCED_FACE ( 'NONE', ( #7797 ), #9776, .T. ) ;
#2325=DIRECTION ( 'NONE',  ( -1.000000000000000000, 1.010728034814421376E-30, 1.090846720500930387E-30 ) ) ;
#2327=CARTESIAN_POINT ( 'NONE',  ( 19.99999999999999645, 1.052479792859053020, 6.413211932068313637 ) ) ;
#2328=VERTEX_POINT ( 'NONE', #11991 ) ;
#2331=DIRECTION ( 'NONE',  ( -1.000000000000000000, 1.010728034814421376E-30, 1.090846720500930387E-30 ) ) ;
#2335=DIRECTION ( 'NONE',  ( -1.000000000000000000, 1.010728034814421376E-30, 1.090846720500930387E-30 ) ) ;
#2337=AXIS2_PLACEMENT_3D ( 'NONE', #8338, #6411, #8274 ) ;
#2340=DIRECTION ( 'NONE',  ( 0.000000000000000000, 0.000000000000000000, 1.000000000000000000 ) ) ;
#2347=CYLINDRICAL_SURFACE ( 'NONE', #11394, 2.800000000000003819 ) ;
#2348=DIRECTION ( 'NONE',  ( 0.000000000000000000, -0.9749279121818260618, 0.2225209339563040956 ) ) ;
#2350=LINE ( 'NONE', #592, #5900 ) ;
#2351=DIRECTION ( 'NONE',  ( 0.000000000000000000, 0.000000000000000000, 1.000000000000000000 ) ) ;
#2356=CIRCLE ( 'NONE', #12436, 2.800000000000002931 ) ;
#2362=EDGE_LOOP ( 'NONE', ( #3841, #7184, #3552, #6393 ) ) ;
#2364=EDGE_LOOP ( 'NONE', ( #7780, #6932, #6499, #12596, #9572, #5402, #6108, #11207, #11988, #1264, #5955, #8102, #319, #12564, #7240, #3207, #9224, #3930, #7017, #10431, #51, #9507, #6444, #9945, #4832, #3721, #11830, #4410, #11404, #351, #5306, #4986, #7843, #2435, #7250, #1920, #5689, #2968, #5450, #5849, #2424, #1963, #12260, #4749, #9685, #8609, #9549, #6926, #5783, #683, #10681, #11238, #10058, #5820, #4546, #5242, #2443, #5579, #1379, #5590, #8026, #9021, #8697, #8412, #10539, #11469, #7440, #6180, #2294, #1909, #1009, #12531, #2823, #6226, #651, #10123, #6033, #9088, #1481, #12405, #12579, #9124, #7324, #9177, #6150, #6744, #236, #9299, #1491, #11263, #7519, #11520, #9952, #285, #2115, #7654, #3486, #1833, #1697, #869, #3457, #10205, #10332, #429, #5669, #3475, #5921, #9854, #11787, #5984, #2685, #9446, #6712, #8983, #1774, #6178, #10264, #7690, #5385, #2229, #6540, #10859, #7890, #8521, #6042, #10939, #6334, #4943, #6868, #6806, #1311, #11511, #4037, #5608, #5178, #9474, #5386, #1857, #3581, #857, #5915, #9947, #11140, #5287 ) ) ;
#2367=LINE ( 'NONE', #4480, #10342 ) ;
#2368=FACE_OUTER_BOUND ( 'NONE', #10655, .T. ) ;
#2371=VERTEX_POINT ( 'NONE', #11078 ) ;
#2374=VERTEX_POINT ( 'NONE', #257 ) ;
#2376=AXIS2_PLACEMENT_3D ( 'NONE', #7461, #10409, #1596 ) ;
#2377=ORIENTED_EDGE ( 'NONE', *, *, #687, .T. ) ;
#2378=VERTEX_POINT ( 'NONE', #4125 ) ;
#2379=ORIENTED_EDGE ( 'NONE', *, *, #6174, .T. ) ;
#2384=AXIS2_PLACEMENT_3D ( 'NONE', #12179, #9066, #11136 ) ;
#2388=CARTESIAN_POINT ( 'NONE',  ( 0.000000000000000000, 4.192831774279053292, -4.965597920955355349 ) ) ;
#2394=DIRECTION ( 'NONE',  ( 0.000000000000000000, -0.1785568947986228838, -0.9839295885986322210 ) ) ;
#2396=CARTESIAN_POINT ( 'NONE',  ( 19.99999999999999645, -3.612733913993637636, 6.458185013351672055 ) ) ;
#2398=DIRECTION ( 'NONE',  ( -1.000000000000000000, 1.010728034814421376E-30, 1.090846720500930387E-30 ) ) ;
#2400=ORIENTED_EDGE ( 'NONE', *, *, #8367, .F. ) ;
#2402=DIRECTION ( 'NONE',  ( -1.000000000000000000, 1.010728034814421376E-30, 1.090846720500930387E-30 ) ) ;
#2404=EDGE_CURVE ( 'NONE', #9218, #291, #6309, .T. ) ;
#2405=EDGE_CURVE ( 'NONE', #7451, #125, #4326, .T. ) ;
#2407=AXIS2_PLACEMENT_3D ( 'NONE', #28, #11817, #3009 ) ;
#2409=ORIENTED_EDGE ( 'NONE', *, *, #843, .F. ) ;
#2411=DIRECTION ( 'NONE',  ( -1.000000000000000000, 1.010728034814421376E-30, 1.090846720500930387E-30 ) ) ;
#2422=ORIENTED_EDGE ( 'NONE', *, *, #1157, .T. ) ;
#2423=EDGE_LOOP ( 'NONE', ( #10077, #4368, #11891, #11402 ) ) ;
#2424=ORIENTED_EDGE ( 'NONE', *, *, #6816, .F. ) ;
#2435=ORIENTED_EDGE ( 'NONE', *, *, #5855, .F. ) ;
#2436=ORIENTED_EDGE ( 'NONE', *, *, #7161, .F. ) ;
#2440=CYLINDRICAL_SURFACE ( 'NONE', #3172, 2.800000000000003819 ) ;
#2441=EDGE_CURVE ( 'NONE', #4499, #3985, #418, .T. ) ;
#2443=ORIENTED_EDGE ( 'NONE', *, *, #6814, .F. ) ;
#2449=CARTESIAN_POINT ( 'NONE',  ( 19.99999999999999645, 5.025702764809077294, 5.431603052487407268 ) ) ;
#2450=CARTESIAN_POINT ( 'NONE',  ( 0.000000000000000000, -4.518585619147925669, 5.860237538055052653 ) ) ;
#2452=ADVANCED_FACE ( 'NONE', ( #7596 ), #6376, .T. ) ;
#2455=AXIS2_PLACEMENT_3D ( 'NONE', #12471, #3586, #7503 ) ;
#2459=ADVANCED_FACE ( 'NONE', ( #8368 ), #5602, .T. ) ;
#2460=AXIS2_PLACEMENT_3D ( 'NONE', #1881, #8829, #8955 ) ;
#2462=CYLINDRICAL_SURFACE ( 'NONE', #6919, 2.800000000000003819 ) ;
#2463=DIRECTION ( 'NONE',  ( 0.000000000000000000, 0.000000000000000000, 1.000000000000000000 ) ) ;
#2464=CIRCLE ( 'NONE', #11085, 2.800000000000003819 ) ;
#2470=AXIS2_PLACEMENT_3D ( 'NONE', #3502, #528, #6590 ) ;
#2471=CIRCLE ( 'NONE', #9640, 6.499000000000007660 ) ;
#2472=VERTEX_POINT ( 'NONE', #2527 ) ;
#2473=DIRECTION ( 'NONE',  ( -1.121661599611125110E-30, 0.9989930665413145894, 0.04486483035051865020 ) ) ;
#2474=DIRECTION ( 'NONE',  ( -1.000000000000000000, 1.010728034814421376E-30, 1.090846720500930387E-30 ) ) ;
#2478=CARTESIAN_POINT ( 'NONE',  ( 19.99999999999997868, 5.914787828628611521, -4.446941076999673115 ) ) ;
#2479=AXIS2_PLACEMENT_3D ( 'NONE', #7343, #3426, #3548 ) ;
#2481=AXIS2_PLACEMENT_3D ( 'NONE', #7985, #6129, #6063 ) ;
#2486=ORIENTED_EDGE ( 'NONE', *, *, #8133, .T. ) ;
#2488=VERTEX_POINT ( 'NONE', #4511 ) ;
#2490=AXIS2_PLACEMENT_3D ( 'NONE', #11316, #1516, #5449 ) ;
#2491=VERTEX_POINT ( 'NONE', #11473 ) ;
#2496=DIRECTION ( 'NONE',  ( 0.000000000000000000, 0.000000000000000000, 1.000000000000000000 ) ) ;
#2501=ORIENTED_EDGE ( 'NONE', *, *, #10414, .T. ) ;
#2502=ORIENTED_EDGE ( 'NONE', *, *, #1717, .T. ) ;
#2503=ORIENTED_EDGE ( 'NONE', *, *, #6126, .T. ) ;
#2515=DIRECTION ( 'NONE',  ( -1.000000000000000000, 1.010728034814421376E-30, 1.090846720500930387E-30 ) ) ;
#2519=DIRECTION ( 'NONE',  ( -1.140150527077241873E-30, 0.000000000000000000, 1.000000000000000000 ) ) ;
#2525=ADVANCED_FACE ( 'NONE', ( #515 ), #7474, .T. ) ;
#2527=CARTESIAN_POINT ( 'NONE',  ( 0.000000000000000000, 6.146182963951664746, 2.112211157443887100 ) ) ;
#2528=DIRECTION ( 'NONE',  ( -6.532754371361492628E-31, 0.9510565162951544194, -0.3090169943749445092 ) ) ;
#2530=CARTESIAN_POINT ( 'NONE',  ( 19.99999999999999645, 7.380072687735807158, -0.5427035320837090282 ) ) ;
#2531=CARTESIAN_POINT ( 'NONE',  ( 19.99999999999997868, 1.528443194675511707, -7.240432404259457222 ) ) ;
#2536=DIRECTION ( 'NONE',  ( 1.000000000000000000, -1.010728034814421376E-30, -1.090846720500930387E-30 ) ) ;
#2538=DIRECTION ( 'NONE',  ( 1.140150527077241873E-30, 0.000000000000000000, -1.000000000000000000 ) ) ;
#2541=CYLINDRICAL_SURFACE ( 'NONE', #5422, 7.400000000000010125 ) ;
#2542=AXIS2_PLACEMENT_3D ( 'NONE', #11966, #102, #1063 ) ;
#2544=DIRECTION ( 'NONE',  ( 1.140150527077241873E-30, 0.000000000000000000, -1.000000000000000000 ) ) ;
#2545=AXIS2_PLACEMENT_3D ( 'NONE', #1347, #9202, #386 ) ;
#2546=CYLINDRICAL_SURFACE ( 'NONE', #3826, 7.400000000000010125 ) ;
#2547=LINE ( 'NONE', #6468, #2790 ) ;
#2552=ORIENTED_EDGE ( 'NONE', *, *, #6765, .T. ) ;
#2553=DIRECTION ( 'NONE',  ( -1.140150527077241873E-30, 0.000000000000000000, 1.000000000000000000 ) ) ;
#2556=DIRECTION ( 'NONE',  ( -1.000000000000000000, 1.010728034814421376E-30, 1.090846720500930387E-30 ) ) ;
#2557=ORIENTED_EDGE ( 'NONE', *, *, #3685, .F. ) ;
#2559=VECTOR ( 'NONE', #6363, 1000.000000000000000 ) ;
#2560=CARTESIAN_POINT ( 'NONE',  ( -10.00000000000000178, 0.000000000000000000, 0.000000000000000000 ) ) ;
#2561=ORIENTED_EDGE ( 'NONE', *, *, #1243, .T. ) ;
#2563=DIRECTION ( 'NONE',  ( -1.000000000000000000, 1.010728034814421376E-30, 1.090846720500930387E-30 ) ) ;
#2566=VECTOR ( 'NONE', #3759, 1000.000000000000000 ) ;
#2568=EDGE_CURVE ( 'NONE', #9520, #3892, #5407, .T. ) ;
#2569=EDGE_CURVE ( 'NONE', #10994, #11920, #11947, .T. ) ;
#2575=VERTEX_POINT ( 'NONE', #2725 ) ;
#2576=CARTESIAN_POINT ( 'NONE',  ( 0.000000000000000000, 0.000000000000000000, 0.000000000000000000 ) ) ;
#2577=FACE_OUTER_BOUND ( 'NONE', #1203, .T. ) ;
#2578=VECTOR ( 'NONE', #2994, 1000.000000000000000 ) ;
#2580=FACE_OUTER_BOUND ( 'NONE', #8850, .T. ) ;
#2582=VERTEX_POINT ( 'NONE', #4698 ) ;
#2584=CIRCLE ( 'NONE', #9953, 7.400000000000009237 ) ;
#2589=ADVANCED_FACE ( 'NONE', ( #9322 ), #8933, .T. ) ;
#2593=ORIENTED_EDGE ( 'NONE', *, *, #4633, .T. ) ;
#2594=DIRECTION ( 'NONE',  ( -1.000000000000000000, 1.010728034814421376E-30, 1.090846720500930387E-30 ) ) ;
#2599=DIRECTION ( 'NONE',  ( 0.000000000000000000, 0.000000000000000000, 1.000000000000000000 ) ) ;
#2601=VECTOR ( 'NONE', #9717, 1000.000000000000000 ) ;
#2605=DIRECTION ( 'NONE',  ( 1.000000000000000000, -1.010728034814421376E-30, -1.090846720500930387E-30 ) ) ;
#2607=DIRECTION ( 'NONE',  ( -1.000000000000000000, 1.010728034814421376E-30, 1.090846720500930387E-30 ) ) ;
#2608=DIRECTION ( 'NONE',  ( -1.000000000000000000, 1.010728034814421376E-30, 1.090846720500930387E-30 ) ) ;
#2612=DIRECTION ( 'NONE',  ( -1.454462294001238940E-30, 0.7227948638273878901, 0.6910626489868685329 ) ) ;
#2613=ORIENTED_EDGE ( 'NONE', *, *, #9129, .T. ) ;
#2619=CARTESIAN_POINT ( 'NONE',  ( 0.000000000000000000, 3.565124043461679992, 5.527927226701645935 ) ) ;
#2620=AXIS2_PLACEMENT_3D ( 'NONE', #9982, #7935, #1177 ) ;
#2622=EDGE_LOOP ( 'NONE', ( #8603, #1892, #8493, #4956 ) ) ;
#2625=DIRECTION ( 'NONE',  ( -1.000000000000000000, 1.010728034814421376E-30, 1.090846720500930387E-30 ) ) ;
#2626=DIRECTION ( 'NONE',  ( -9.737501798821852212E-31, 0.9909497617679352555, -0.1342332658176522697 ) ) ;
#2627=ORIENTED_EDGE ( 'NONE', *, *, #5232, .T. ) ;
#2631=AXIS2_PLACEMENT_3D ( 'NONE', #12157, #7255, #11177 ) ;
#2632=ORIENTED_EDGE ( 'NONE', *, *, #5652, .F. ) ;
#2633=AXIS2_PLACEMENT_3D ( 'NONE', #7982, #6909, #12060 ) ;
#2634=CIRCLE ( 'NONE', #3256, 7.400000000000011902 ) ;
#2638=DIRECTION ( 'NONE',  ( -1.000000000000000000, 1.010728034814421376E-30, 1.090846720500930387E-30 ) ) ;
#2639=DIRECTION ( 'NONE',  ( -1.000000000000000000, 1.010728034814421376E-30, 1.090846720500930387E-30 ) ) ;
#2642=DIRECTION ( 'NONE',  ( 0.000000000000000000, 0.000000000000000000, 1.000000000000000000 ) ) ;
#2645=CARTESIAN_POINT ( 'NONE',  ( 19.99999999999999645, 5.362412286431453623, 3.809543717993933765 ) ) ;
#2646=UNCERTAINTY_MEASURE_WITH_UNIT (LENGTH_MEASURE( 1.000000000000000082E-05 ), #12452, 'distance_accuracy_value', 'NONE');
#2647=EDGE_CURVE ( 'NONE', #87, #2374, #2034, .T. ) ;
#2649=ADVANCED_FACE ( 'NONE', ( #8810 ), #3864, .T. ) ;
#2651=ORIENTED_EDGE ( 'NONE', *, *, #448, .F. ) ;
#2653=DIRECTION ( 'NONE',  ( -1.000000000000000000, 1.010728034814421376E-30, 1.090846720500930387E-30 ) ) ;
#2658=DIRECTION ( 'NONE',  ( 0.000000000000000000, 0.7227948638273878901, 0.6910626489868685329 ) ) ;
#2660=DIRECTION ( 'NONE',  ( -1.000000000000000000, 1.010728034814421376E-30, 1.090846720500930387E-30 ) ) ;
#2666=EDGE_CURVE ( 'NONE', #4686, #11547, #11090, .T. ) ;
#2674=CIRCLE ( 'NONE', #11508, 6.499000000000007660 ) ;
#2675=CARTESIAN_POINT ( 'NONE',  ( 19.99999999999999645, -6.453973581750233279, -0.7636923504069568214 ) ) ;
#2677=CARTESIAN_POINT ( 'NONE',  ( 0.000000000000000000, -6.310777386698704028, -1.552768423021405608 ) ) ;
#2679=FACE_OUTER_BOUND ( 'NONE', #5687, .T. ) ;
#2684=DIRECTION ( 'NONE',  ( 7.272311470006191196E-31, 0.3513748240813435175, -0.9362348706397368714 ) ) ;
#2685=ORIENTED_EDGE ( 'NONE', *, *, #9015, .F. ) ;
#2687=EDGE_CURVE ( 'NONE', #363, #6740, #11718, .T. ) ;
#2691=VECTOR ( 'NONE', #5090, 1000.000000000000000 ) ;
#2692=DIRECTION ( 'NONE',  ( -1.140150527077241873E-30, 0.000000000000000000, 1.000000000000000000 ) ) ;
#2696=CYLINDRICAL_SURFACE ( 'NONE', #1359, 2.800000000000003819 ) ;
#2699=DIRECTION ( 'NONE',  ( -1.140150527077241873E-30, 0.000000000000000000, 1.000000000000000000 ) ) ;
#2701=ORIENTED_EDGE ( 'NONE', *, *, #8073, .F. ) ;
#2702=CARTESIAN_POINT ( 'NONE',  ( 19.99999999999999645, -1.268072931708538853, 6.374087545670210631 ) ) ;
#2708=ADVANCED_FACE ( 'NONE', ( #7848 ), #2977, .T. ) ;
#2713=PLANE ( 'NONE',  #12131 ) ;
#2714=ORIENTED_EDGE ( 'NONE', *, *, #1305, .F. ) ;
#2718=CARTESIAN_POINT ( 'NONE',  ( 19.99999999999999645, 0.000000000000000000, 0.000000000000000000 ) ) ;
#2723=ORIENTED_EDGE ( 'NONE', *, *, #3237, .T. ) ;
#2724=EDGE_CURVE ( 'NONE', #4395, #4686, #10241, .T. ) ;
#2725=CARTESIAN_POINT ( 'NONE',  ( 0.000000000000000000, 1.834336845376802971, -6.234758161925229913 ) ) ;
#2729=FACE_OUTER_BOUND ( 'NONE', #11531, .T. ) ;
#2730=AXIS2_PLACEMENT_3D ( 'NONE', #6143, #5187, #2022 ) ;
#2733=CARTESIAN_POINT ( 'NONE',  ( 19.99999999999999645, -6.289597356626462243, -3.898841506334609797 ) ) ;
#2737=CARTESIAN_POINT ( 'NONE',  ( 0.000000000000000000, 5.956456411769424975, -2.790827096698929477 ) ) ;
#2739=EDGE_CURVE ( 'NONE', #11576, #7570, #12107, .T. ) ;
#2741=DIRECTION ( 'NONE',  ( 1.140150527077241873E-30, 0.000000000000000000, -1.000000000000000000 ) ) ;
#2742=CARTESIAN_POINT ( 'NONE',  ( 0.000000000000000000, 0.000000000000000000, 0.000000000000000000 ) ) ;
#2744=DIRECTION ( 'NONE',  ( -1.000000000000000000, 1.010728034814421376E-30, 1.090846720500930387E-30 ) ) ;
#2748=AXIS2_PLACEMENT_3D ( 'NONE', #9007, #4121, #4055 ) ;
#2749=DIRECTION ( 'NONE',  ( -1.000000000000000000, 1.010728034814421376E-30, 1.090846720500930387E-30 ) ) ;
#2752=ORIENTED_EDGE ( 'NONE', *, *, #7074, .T. ) ;
#2753=ADVANCED_FACE ( 'NONE', ( #9951 ), #2317, .T. ) ;
#2756=CARTESIAN_POINT ( 'NONE',  ( 0.000000000000000000, -6.484265599627161869, -1.105616797299001419 ) ) ;
#2760=DIRECTION ( 'NONE',  ( 1.000000000000000000, -1.010728034814421376E-30, -1.090846720500930387E-30 ) ) ;
#2762=VERTEX_POINT ( 'NONE', #6107 ) ;
#2763=LINE ( 'NONE', #6677, #9550 ) ;
#2764=ADVANCED_FACE ( 'NONE', ( #6233 ), #10017, .T. ) ;
#2765=CARTESIAN_POINT ( 'NONE',  ( 19.99999999999999645, -0.4733669331952357062, 6.481737787550290619 ) ) ;
#2766=ORIENTED_EDGE ( 'NONE', *, *, #12001, .T. ) ;
#2767=AXIS2_PLACEMENT_3D ( 'NONE', #3149, #290, #4222 ) ;
#2771=VERTEX_POINT ( 'NONE', #10143 ) ;
#2772=CARTESIAN_POINT ( 'NONE',  ( 0.000000000000000000, -4.357840574720623472, 4.821434073521961849 ) ) ;
#2773=DIRECTION ( 'NONE',  ( 0.000000000000000000, 0.000000000000000000, 1.000000000000000000 ) ) ;
#2775=DIRECTION ( 'NONE',  ( -1.000000000000000000, 1.010728034814421376E-30, 1.090846720500930387E-30 ) ) ;
#2778=ORIENTED_EDGE ( 'NONE', *, *, #8111, .F. ) ;
#2781=DIRECTION ( 'NONE',  ( -1.000000000000000000, 1.010728034814421376E-30, 1.090846720500930387E-30 ) ) ;
#2783=VERTEX_POINT ( 'NONE', #7967 ) ;
#2784=AXIS2_PLACEMENT_3D ( 'NONE', #9956, #8166, #7338 ) ;
#2786=DIRECTION ( 'NONE',  ( -1.000000000000000000, 1.010728034814421376E-30, 1.090846720500930387E-30 ) ) ;
#2790=VECTOR ( 'NONE', #12652, 1000.000000000000000 ) ;
#2793=CARTESIAN_POINT ( 'NONE',  ( 0.000000000000000000, 0.000000000000000000, 0.000000000000000000 ) ) ;
#2798=AXIS2_PLACEMENT_3D ( 'NONE', #1194, #11778, #6822 ) ;
#2799=LINE ( 'NONE', #8502, #12402 ) ;
#2802=DIRECTION ( 'NONE',  ( 0.000000000000000000, 0.000000000000000000, 1.000000000000000000 ) ) ;
#2803=DIRECTION ( 'NONE',  ( -1.000000000000000000, 1.010728034814421376E-30, 1.090846720500930387E-30 ) ) ;
#2812=CARTESIAN_POINT ( 'NONE',  ( -10.00000000000000178, 0.000000000000000000, 0.000000000000000000 ) ) ;
#2813=ADVANCED_FACE ( 'NONE', ( #179 ), #9062, .T. ) ;
#2814=EDGE_CURVE ( 'NONE', #6098, #3319, #6976, .T. ) ;
#2817=ORIENTED_EDGE ( 'NONE', *, *, #12561, .T. ) ;
#2822=DIRECTION ( 'NONE',  ( -1.000000000000000000, 1.010728034814421376E-30, 1.090846720500930387E-30 ) ) ;
#2823=ORIENTED_EDGE ( 'NONE', *, *, #11411, .F. ) ;
#2824=CARTESIAN_POINT ( 'NONE',  ( 0.000000000000000000, 7.358375340956995636, 0.7837807994561865055 ) ) ;
#2827=CARTESIAN_POINT ( 'NONE',  ( 9.999999999999994671, -6.969736844459704095, 2.486517307195113879 ) ) ;
#2828=VERTEX_POINT ( 'NONE', #3293 ) ;
#2830=FACE_OUTER_BOUND ( 'NONE', #11061, .T. ) ;
#2831=ORIENTED_EDGE ( 'NONE', *, *, #3749, .T. ) ;
#2834=DIRECTION ( 'NONE',  ( -1.000000000000000000, 1.010728034814421376E-30, 1.090846720500930387E-30 ) ) ;
#2836=AXIS2_PLACEMENT_3D ( 'NONE', #1110, #6982, #8059 ) ;
#2837=CARTESIAN_POINT ( 'NONE',  ( 0.000000000000000000, 0.000000000000000000, 0.000000000000000000 ) ) ;
#2838=EDGE_CURVE ( 'NONE', #3787, #35, #4750, .T. ) ;
#2840=CARTESIAN_POINT ( 'NONE',  ( 50.00005079999998969, 5.204170427930421283E-15, -6.938893903907228378E-15 ) ) ;
#2842=DIRECTION ( 'NONE',  ( -1.000000000000000000, 1.010728034814421376E-30, 1.090846720500930387E-30 ) ) ;
#2844=FACE_OUTER_BOUND ( 'NONE', #9377, .T. ) ;
#2851=ORIENTED_EDGE ( 'NONE', *, *, #8169, .T. ) ;
#2853=DIRECTION ( 'NONE',  ( -1.000000000000000000, 1.010728034814421376E-30, 1.090846720500930387E-30 ) ) ;
#2855=CARTESIAN_POINT ( 'NONE',  ( 0.000000000000000000, 0.000000000000000000, 0.000000000000000000 ) ) ;
#2857=CARTESIAN_POINT ( 'NONE',  ( 19.99999999999997868, 6.557268578288196537, 0.5199208220222073518 ) ) ;
#2860=ORIENTED_EDGE ( 'NONE', *, *, #9146, .F. ) ;
#2861=DIRECTION ( 'NONE',  ( -1.000000000000000000, 1.010728034814421376E-30, 1.090846720500930387E-30 ) ) ;
#2862=VERTEX_POINT ( 'NONE', #3540 ) ;
#2864=EDGE_CURVE ( 'NONE', #9871, #1836, #1659, .T. ) ;
#2865=CARTESIAN_POINT ( 'NONE',  ( 19.99999999999997868, 6.544726022087268724, -0.6592800351836389794 ) ) ;
#2869=DIRECTION ( 'NONE',  ( 0.000000000000000000, 0.000000000000000000, 1.000000000000000000 ) ) ;
#2870=CARTESIAN_POINT ( 'NONE',  ( 19.99999999999997868, 5.012092988314006625, -4.137139697483489087 ) ) ;
#2871=CIRCLE ( 'NONE', #2455, 2.800000000000004263 ) ;
#2879=CARTESIAN_POINT ( 'NONE',  ( 19.99999999999999645, -0.1095571986795048497, 6.498076501567022767 ) ) ;
#2880=CARTESIAN_POINT ( 'NONE',  ( 0.000000000000000000, 6.613766744932292774, -3.319350756341939324 ) ) ;
#2881=CARTESIAN_POINT ( 'NONE',  ( 10.00000000000000178, 5.914787828628545796, 4.446941076999770814 ) ) ;
#2884=VERTEX_POINT ( 'NONE', #6559 ) ;
#2885=CARTESIAN_POINT ( 'NONE',  ( 19.99999999999999645, -6.486618105788068966, 0.4009819817179238743 ) ) ;
#2886=CIRCLE ( 'NONE', #10042, 2.800000000000003819 ) ;
#2887=VECTOR ( 'NONE', #1674, 1000.000000000000000 ) ;
#2888=MECHANICAL_DESIGN_GEOMETRIC_PRESENTATION_REPRESENTATION('',(#4724),#9029);
#2891=ORIENTED_EDGE ( 'NONE', *, *, #323, .F. ) ;
#2892=ORIENTED_EDGE ( 'NONE', *, *, #10410, .T. ) ;
#2893=DIRECTION ( 'NONE',  ( 0.000000000000000000, 0.000000000000000000, 1.000000000000000000 ) ) ;
#2895=ORIENTED_EDGE ( 'NONE', *, *, #9762, .T. ) ;
#2900=VECTOR ( 'NONE', #4591, 1000.000000000000000 ) ;
#2903=ORIENTED_EDGE ( 'NONE', *, *, #4894, .T. ) ;
#2905=FACE_OUTER_BOUND ( 'NONE', #11001, .T. ) ;
#2907=FACE_OUTER_BOUND ( 'NONE', #11846, .T. ) ;
#2908=AXIS2_PLACEMENT_3D ( 'NONE', #635, #11400, #12375 ) ;
#2913=ORIENTED_EDGE ( 'NONE', *, *, #7561, .T. ) ;
#2916=DIRECTION ( 'NONE',  ( 0.000000000000000000, 0.000000000000000000, 1.000000000000000000 ) ) ;
#2922=ADVANCED_FACE ( 'NONE', ( #1592 ), #4625, .T. ) ;
#2923=CARTESIAN_POINT ( 'NONE',  ( 9.999999999999994671, -6.413745496774120092, 3.691052519622234129 ) ) ;
#2924=DIRECTION ( 'NONE',  ( -1.140150527077241873E-30, 0.000000000000000000, 1.000000000000000000 ) ) ;
#2925=EDGE_CURVE ( 'NONE', #6318, #156, #7193, .T. ) ;
#2931=LINE ( 'NONE', #10815, #5595 ) ;
#2933=LINE ( 'NONE', #12587, #12088 ) ;
#2940=AXIS2_PLACEMENT_3D ( 'NONE', #12319, #1488, #4519 ) ;
#2942=CARTESIAN_POINT ( 'NONE',  ( 19.99999999999997868, -0.9522442067290397549, -6.508557431545724192 ) ) ;
#2944=DIRECTION ( 'NONE',  ( 1.140150527077241873E-30, 0.000000000000000000, -1.000000000000000000 ) ) ;
#2945=DIRECTION ( 'NONE',  ( -1.000000000000000000, 1.010728034814421376E-30, 1.090846720500930387E-30 ) ) ;
#2946=DIRECTION ( 'NONE',  ( -1.000000000000000000, 1.010728034814421376E-30, 1.090846720500930387E-30 ) ) ;
#2947=ORIENTED_EDGE ( 'NONE', *, *, #3112, .F. ) ;
#2948=CARTESIAN_POINT ( 'NONE',  ( 19.99999999999997868, 6.557268578288196537, 3.319920822022211393 ) ) ;
#2952=ORIENTED_EDGE ( 'NONE', *, *, #3997, .T. ) ;
#2954=EDGE_CURVE ( 'NONE', #8658, #7451, #8167, .T. ) ;
#2955=CARTESIAN_POINT ( 'NONE',  ( 19.99999999999997868, 5.012092988314006625, -4.137139697483489087 ) ) ;
#2960=DIRECTION ( 'NONE',  ( -1.000000000000000000, 1.010728034814421376E-30, 1.090846720500930387E-30 ) ) ;
#2961=VERTEX_POINT ( 'NONE', #7336 ) ;
#2967=AXIS2_PLACEMENT_3D ( 'NONE', #6544, #10387, #8398 ) ;
#2968=ORIENTED_EDGE ( 'NONE', *, *, #9876, .F. ) ;
#2971=EDGE_CURVE ( 'NONE', #4951, #5144, #4925, .T. ) ;
#2972=ADVANCED_FACE ( 'NONE', ( #3602, #11458 ), #2713, .F. ) ;
#2973=EDGE_LOOP ( 'NONE', ( #8784, #5135, #4932, #2593 ) ) ;
#2975=AXIS2_PLACEMENT_3D ( 'NONE', #6858, #10765, #792 ) ;
#2977=CYLINDRICAL_SURFACE ( 'NONE', #7799, 6.499000000000010324 ) ;
#2978=ORIENTED_EDGE ( 'NONE', *, *, #2187, .T. ) ;
#2979=EDGE_CURVE ( 'NONE', #10149, #4676, #12299, .T. ) ;
#2983=ORIENTED_EDGE ( 'NONE', *, *, #4077, .T. ) ;
#2986=DIRECTION ( 'NONE',  ( 0.000000000000000000, 0.000000000000000000, 1.000000000000000000 ) ) ;
#2988=VECTOR ( 'NONE', #9468, 1000.000000000000000 ) ;
#2989=DIRECTION ( 'NONE',  ( -1.000000000000000000, 1.010728034814421376E-30, 1.090846720500930387E-30 ) ) ;
#2992=DIRECTION ( 'NONE',  ( -1.000000000000000000, 1.010728034814421376E-30, 1.090846720500930387E-30 ) ) ;
#2994=DIRECTION ( 'NONE',  ( -1.000000000000000000, 1.010728034814421376E-30, 1.090846720500930387E-30 ) ) ;
#2996=CIRCLE ( 'NONE', #4631, 2.800000000000003819 ) ;
#2997=DIRECTION ( 'NONE',  ( 1.140150527077241873E-30, 0.000000000000000000, -1.000000000000000000 ) ) ;
#2999=EDGE_CURVE ( 'NONE', #802, #10380, #8212, .T. ) ;
#3001=EDGE_CURVE ( 'NONE', #5017, #7234, #5712, .T. ) ;
#3003=ORIENTED_EDGE ( 'NONE', *, *, #4759, .F. ) ;
#3005=FACE_OUTER_BOUND ( 'NONE', #3654, .T. ) ;
#3006=DIRECTION ( 'NONE',  ( 0.000000000000000000, 0.000000000000000000, 1.000000000000000000 ) ) ;
#3009=DIRECTION ( 'NONE',  ( 0.000000000000000000, 0.000000000000000000, 1.000000000000000000 ) ) ;
#3010=VERTEX_POINT ( 'NONE', #3913 ) ;
#3017=CYLINDRICAL_SURFACE ( 'NONE', #4567, 6.499000000000010324 ) ;
#3019=VERTEX_POINT ( 'NONE', #1970 ) ;
#3021=ADVANCED_FACE ( 'NONE', ( #11584 ), #8739, .F. ) ;
#3029=AXIS2_PLACEMENT_3D ( 'NONE', #9184, #5082, #3166 ) ;
#3033=ORIENTED_EDGE ( 'NONE', *, *, #11401, .T. ) ;
#3034=ADVANCED_FACE ( 'NONE', ( #4755 ), #5902, .T. ) ;
#3036=CIRCLE ( 'NONE', #12077, 2.800000000000004263 ) ;
#3037=ORIENTED_EDGE ( 'NONE', *, *, #2647, .T. ) ;
#3039=EDGE_LOOP ( 'NONE', ( #6750, #11892, #8395, #9336 ) ) ;
#3043=EDGE_CURVE ( 'NONE', #3101, #7946, #1848, .T. ) ;
#3045=CYLINDRICAL_SURFACE ( 'NONE', #8943, 6.499000000000010324 ) ;
#3046=CARTESIAN_POINT ( 'NONE',  ( 0.000000000000000000, -4.518585619147845733, -5.860237538055125484 ) ) ;
#3047=VERTEX_POINT ( 'NONE', #7774 ) ;
#3049=ORIENTED_EDGE ( 'NONE', *, *, #10659, .T. ) ;
#3051=DIRECTION ( 'NONE',  ( 0.000000000000000000, 0.000000000000000000, 1.000000000000000000 ) ) ;
#3053=DIRECTION ( 'NONE',  ( 1.000000000000000000, -1.010728034814421376E-30, -1.090846720500930387E-30 ) ) ;
#3055=DIRECTION ( 'NONE',  ( -1.000000000000000000, 1.010728034814421376E-30, 1.090846720500930387E-30 ) ) ;
#3056=DIRECTION ( 'NONE',  ( -1.000000000000000000, 1.010728034814421376E-30, 1.090846720500930387E-30 ) ) ;
#3060=CARTESIAN_POINT ( 'NONE',  ( 0.000000000000000000, -4.357840574720561300, -4.821434073522038233 ) ) ;
#3062=ORIENTED_EDGE ( 'NONE', *, *, #6963, .T. ) ;
#3064=LINE ( 'NONE', #10110, #3788 ) ;
#3067=CARTESIAN_POINT ( 'NONE',  ( 0.000000000000000000, -0.9522442067290397549, -6.508557431545724192 ) ) ;
#3073=ORIENTED_EDGE ( 'NONE', *, *, #1665, .F. ) ;
#3075=EDGE_CURVE ( 'NONE', #3964, #2374, #942, .T. ) ;
#3077=ORIENTED_EDGE ( 'NONE', *, *, #10381, .F. ) ;
#3078=CIRCLE ( 'NONE', #10230, 2.800000000000002931 ) ;
#3086=CIRCLE ( 'NONE', #5562, 7.400000000000011902 ) ;
#3089=LINE ( 'NONE', #6029, #6704 ) ;
#3093=CIRCLE ( 'NONE', #3700, 2.800000000000003819 ) ;
#3094=ORIENTED_EDGE ( 'NONE', *, *, #3425, .T. ) ;
#3095=AXIS2_PLACEMENT_3D ( 'NONE', #12653, #9721, #11431 ) ;
#3096=CIRCLE ( 'NONE', #812, 7.400000000000011902 ) ;
#3097=CARTESIAN_POINT ( 'NONE',  ( 9.999999999999994671, -7.258495115966583811, 1.440225208600806717 ) ) ;
#3098=CARTESIAN_POINT ( 'NONE',  ( 19.99999999999997868, -3.399584271718297579, -6.572885726945642659 ) ) ;
#3101=VERTEX_POINT ( 'NONE', #752 ) ;
#3102=DIRECTION ( 'NONE',  ( -1.000000000000000000, 1.010728034814421376E-30, 1.090846720500930387E-30 ) ) ;
#3104=AXIS2_PLACEMENT_3D ( 'NONE', #5289, #11155, #11282 ) ;
#3110=EDGE_LOOP ( 'NONE', ( #11693, #9803, #12735, #1781 ) ) ;
#3111=FACE_OUTER_BOUND ( 'NONE', #10549, .T. ) ;
#3112=EDGE_CURVE ( 'NONE', #3412, #8231, #3727, .T. ) ;
#3114=CIRCLE ( 'NONE', #11322, 6.499000000000008548 ) ;
#3116=DIRECTION ( 'NONE',  ( 0.000000000000000000, 0.000000000000000000, 1.000000000000000000 ) ) ;
#3117=DIRECTION ( 'NONE',  ( -1.000000000000000000, 1.010728034814421376E-30, 1.090846720500930387E-30 ) ) ;
#3122=CARTESIAN_POINT ( 'NONE',  ( 19.99999999999999645, -5.148708580507647348, -3.965829163366334953 ) ) ;
#3126=ORIENTED_EDGE ( 'NONE', *, *, #2724, .T. ) ;
#3130=CARTESIAN_POINT ( 'NONE',  ( 19.99999999999997868, 6.557268578288196537, 0.5199208220222073518 ) ) ;
#3132=EDGE_CURVE ( 'NONE', #10380, #8069, #5210, .T. ) ;
#3133=CARTESIAN_POINT ( 'NONE',  ( 9.999999999999998224, 5.200656487704272912, 5.264330166022994639 ) ) ;
#3137=DIRECTION ( 'NONE',  ( 0.000000000000000000, -0.9749279121818259508, 0.2225209339563041233 ) ) ;
#3141=ORIENTED_EDGE ( 'NONE', *, *, #7277, .T. ) ;
#3146=EDGE_CURVE ( 'NONE', #6793, #5973, #10124, .T. ) ;
#3147=CARTESIAN_POINT ( 'NONE',  ( 19.99999999999997868, 6.359055127044406674, -1.682410996215896848 ) ) ;
#3149=CARTESIAN_POINT ( 'NONE',  ( 0.000000000000000000, 6.557268578288212524, -0.5199208220221240850 ) ) ;
#3152=DIRECTION ( 'NONE',  ( 0.000000000000000000, 0.000000000000000000, 1.000000000000000000 ) ) ;
#3155=EDGE_CURVE ( 'NONE', #7064, #12067, #7680, .T. ) ;
#3159=VECTOR ( 'NONE', #10958, 1000.000000000000000 ) ;
#3160=VERTEX_POINT ( 'NONE', #228 ) ;
#3163=EDGE_CURVE ( 'NONE', #4169, #3964, #68, .T. ) ;
#3164=DIRECTION ( 'NONE',  ( 0.000000000000000000, 0.5128992774059070170, -0.8584487936018656562 ) ) ;
#3165=ADVANCED_FACE ( 'NONE', ( #7955 ), #7004, .T. ) ;
#3166=DIRECTION ( 'NONE',  ( 8.135128085091671982E-31, 0.1785568947986369281, -0.9839295885986296675 ) ) ;
#3170=AXIS2_PLACEMENT_3D ( 'NONE', #605, #11373, #2553 ) ;
#3171=DIRECTION ( 'NONE',  ( -1.000000000000000000, 1.010728034814421376E-30, 1.090846720500930387E-30 ) ) ;
#3172=AXIS2_PLACEMENT_3D ( 'NONE', #9058, #4362, #6166 ) ;
#3173=DIRECTION ( 'NONE',  ( -1.000000000000000000, 1.010728034814421376E-30, 1.090846720500930387E-30 ) ) ;
#3178=VERTEX_POINT ( 'NONE', #9110 ) ;
#3179=CARTESIAN_POINT ( 'NONE',  ( 0.000000000000000000, -1.113123845672308709, -7.315801754025043735 ) ) ;
#3180=EDGE_CURVE ( 'NONE', #12656, #4412, #8699, .T. ) ;
#3184=AXIS2_PLACEMENT_3D ( 'NONE', #246, #8035, #11068 ) ;
#3191=VECTOR ( 'NONE', #4303, 1000.000000000000000 ) ;
#3194=CARTESIAN_POINT ( 'NONE',  ( 19.99999999999999645, -3.055252325922228174, 5.825248672282130613 ) ) ;
#3202=CARTESIAN_POINT ( 'NONE',  ( 0.000000000000000000, -6.884685972239644514, -2.713134545806132003 ) ) ;
#3204=ADVANCED_FACE ( 'NONE', ( #12025 ), #8080, .T. ) ;
#3207=ORIENTED_EDGE ( 'NONE', *, *, #4633, .F. ) ;
#3208=DIRECTION ( 'NONE',  ( 0.000000000000000000, 0.000000000000000000, 1.000000000000000000 ) ) ;
#3210=CIRCLE ( 'NONE', #10372, 6.499000000000009436 ) ;
#3213=VECTOR ( 'NONE', #9924, 1000.000000000000000 ) ;
#3215=ORIENTED_EDGE ( 'NONE', *, *, #7466, .F. ) ;
#3216=FACE_OUTER_BOUND ( 'NONE', #11053, .T. ) ;
#3217=DIRECTION ( 'NONE',  ( 0.000000000000000000, 0.000000000000000000, 1.000000000000000000 ) ) ;
#3218=ORIENTED_EDGE ( 'NONE', *, *, #3359, .T. ) ;
#3219=DIRECTION ( 'NONE',  ( 1.000000000000000000, -1.010728034814421376E-30, -1.090846720500930387E-30 ) ) ;
#3224=ADVANCED_FACE ( 'NONE', ( #8145 ), #6149, .T. ) ;
#3229=ORIENTED_EDGE ( 'NONE', *, *, #7750, .F. ) ;
#3230=DIRECTION ( 'NONE',  ( -1.257247067695985463E-30, 0.9749279121818227312, 0.2225209339563182231 ) ) ;
#3231=ADVANCED_FACE ( 'NONE', ( #7127 ), #8982, .T. ) ;
#3233=ORIENTED_EDGE ( 'NONE', *, *, #12147, .F. ) ;
#3234=CARTESIAN_POINT ( 'NONE',  ( 19.99999999999999645, 5.895746314278407674, 2.916892913127008935 ) ) ;
#3235=ORIENTED_EDGE ( 'NONE', *, *, #5502, .F. ) ;
#3236=DIRECTION ( 'NONE',  ( -1.000000000000000000, 1.010728034814421376E-30, 1.090846720500930387E-30 ) ) ;
#3237=EDGE_CURVE ( 'NONE', #4592, #7505, #7057, .T. ) ;
#3238=CARTESIAN_POINT ( 'NONE',  ( 19.99999999999999645, 0.000000000000000000, 0.000000000000000000 ) ) ;
#3249=CIRCLE ( 'NONE', #8970, 2.800000000000003819 ) ;
#3254=CARTESIAN_POINT ( 'NONE',  ( 19.99999999999999645, -6.484265599627176968, 1.105616797298907716 ) ) ;
#3256=AXIS2_PLACEMENT_3D ( 'NONE', #1752, #780, #1812 ) ;
#3257=CARTESIAN_POINT ( 'NONE',  ( 19.99999999999999645, -5.492355906873422455, 4.959236492871922586 ) ) ;
#3259=EDGE_LOOP ( 'NONE', ( #8750, #11099, #1003, #6879 ) ) ;
#3260=CARTESIAN_POINT ( 'NONE',  ( 0.000000000000000000, -0.1095571986794155184, -6.498076501567039642 ) ) ;
#3261=DIRECTION ( 'NONE',  ( 1.000000000000000000, -1.010728034814421376E-30, -1.090846720500930387E-30 ) ) ;
#3264=ORIENTED_EDGE ( 'NONE', *, *, #6280, .T. ) ;
#3266=CYLINDRICAL_SURFACE ( 'NONE', #7326, 6.499000000000010324 ) ;
#3271=EDGE_LOOP ( 'NONE', ( #4453, #8960, #6681, #10701 ) ) ;
#3273=EDGE_CURVE ( 'NONE', #8777, #9626, #1290, .T. ) ;
#3274=DIRECTION ( 'NONE',  ( -1.000000000000000000, 1.010728034814421376E-30, 1.090846720500930387E-30 ) ) ;
#3275=EDGE_CURVE ( 'NONE', #4118, #7374, #262, .T. ) ;
#3280=CARTESIAN_POINT ( 'NONE',  ( 19.99999999999999645, -2.385831757338583881, 6.045230171438861433 ) ) ;
#3281=CYLINDRICAL_SURFACE ( 'NONE', #2201, 7.400000000000010125 ) ;
#3285=ORIENTED_EDGE ( 'NONE', *, *, #11315, .F. ) ;
#3287=ORIENTED_EDGE ( 'NONE', *, *, #5466, .T. ) ;
#3292=VERTEX_POINT ( 'NONE', #4608 ) ;
#3293=CARTESIAN_POINT ( 'NONE',  ( 0.000000000000000000, -6.213893036447800888, -1.903820982021603436 ) ) ;
#3295=ORIENTED_EDGE ( 'NONE', *, *, #2076, .T. ) ;
#3299=AXIS2_PLACEMENT_3D ( 'NONE', #6383, #1484, #6454 ) ;
#3301=AXIS2_PLACEMENT_3D ( 'NONE', #12148, #8197, #7180 ) ;
#3303=ORIENTED_EDGE ( 'NONE', *, *, #3425, .F. ) ;
#3305=VERTEX_POINT ( 'NONE', #482 ) ;
#3306=LINE ( 'NONE', #5218, #10534 ) ;
#3308=ADVANCED_FACE ( 'NONE', ( #420 ), #4413, .T. ) ;
#3309=DIRECTION ( 'NONE',  ( -1.000000000000000000, 1.010728034814421376E-30, 1.090846720500930387E-30 ) ) ;
#3310=EDGE_CURVE ( 'NONE', #8569, #1400, #4791, .T. ) ;
#3312=VECTOR ( 'NONE', #9016, 1000.000000000000000 ) ;
#3313=CARTESIAN_POINT ( 'NONE',  ( 19.99999999999999645, 1.531833341630123302, 6.396997380212702922 ) ) ;
#3314=ADVANCED_FACE ( 'NONE', ( #7501 ), #1635, .T. ) ;
#3315=DIRECTION ( 'NONE',  ( -1.000000000000000000, 1.010728034814421376E-30, 1.090846720500930387E-30 ) ) ;
#3316=EDGE_CURVE ( 'NONE', #8854, #5073, #4595, .T. ) ;
#3317=CARTESIAN_POINT ( 'NONE',  ( 19.99999999999997868, 5.362412286431509578, -3.809543717993867595 ) ) ;
#3319=VERTEX_POINT ( 'NONE', #8525 ) ;
#3322=AXIS2_PLACEMENT_3D ( 'NONE', #4459, #3688, #12583 ) ;
#3323=DIRECTION ( 'NONE',  ( -1.000000000000000000, 1.010728034814421376E-30, 1.090846720500930387E-30 ) ) ;
#3325=CYLINDRICAL_SURFACE ( 'NONE', #9503, 6.499000000000010324 ) ;
#3326=CARTESIAN_POINT ( 'NONE',  ( 9.999999999999998224, 4.177097350749799709, 6.108343287861219828 ) ) ;
#3330=( NAMED_UNIT ( * ) SI_UNIT ( $, .STERADIAN. ) SOLID_ANGLE_UNIT ( ) );
#3331=ORIENTED_EDGE ( 'NONE', *, *, #4464, .T. ) ;
#3335=ORIENTED_EDGE ( 'NONE', *, *, #8891, .T. ) ;
#3343=CIRCLE ( 'NONE', #8039, 2.800000000000003819 ) ;
#3346=ORIENTED_EDGE ( 'NONE', *, *, #3043, .T. ) ;
#3347=ORIENTED_EDGE ( 'NONE', *, *, #4136, .T. ) ;
#3349=CIRCLE ( 'NONE', #4145, 7.400000000000009237 ) ;
#3350=DIRECTION ( 'NONE',  ( 1.000000000000000000, -1.010728034814421376E-30, -1.090846720500930387E-30 ) ) ;
#3351=CIRCLE ( 'NONE', #1064, 2.800000000000004263 ) ;
#3358=DIRECTION ( 'NONE',  ( -1.000000000000000000, 1.010728034814421376E-30, 1.090846720500930387E-30 ) ) ;
#3359=EDGE_CURVE ( 'NONE', #1141, #12437, #7069, .T. ) ;
#3360=DIRECTION ( 'NONE',  ( -1.140150527077241873E-30, 0.000000000000000000, 1.000000000000000000 ) ) ;
#3361=AXIS2_PLACEMENT_3D ( 'NONE', #9072, #12244, #4251 ) ;
#3364=EDGE_CURVE ( 'NONE', #2371, #3019, #11178, .T. ) ;
#3365=DIRECTION ( 'NONE',  ( 1.158639454543359513E-30, -0.1785568947986228838, -0.9839295885986322210 ) ) ;
#3367=ORIENTED_EDGE ( 'NONE', *, *, #3878, .T. ) ;
#3368=CARTESIAN_POINT ( 'NONE',  ( 19.99999999999999645, -6.484265599627167198, -1.105616797299011855 ) ) ;
#3370=AXIS2_PLACEMENT_3D ( 'NONE', #12394, #7486, #2473 ) ;
#3372=AXIS2_PLACEMENT_3D ( 'NONE', #5912, #4046, #5975 ) ;
#3374=CARTESIAN_POINT ( 'NONE',  ( 19.99999999999999645, -5.682309657208357123, 3.313524683561968942 ) ) ;
#3378=DIRECTION ( 'NONE',  ( -1.000000000000000000, 1.010728034814421376E-30, 1.090846720500930387E-30 ) ) ;
#3379=CARTESIAN_POINT ( 'NONE',  ( 10.00000000000000178, 6.057062246029517816, 4.251117141143491374 ) ) ;
#3382=AXIS2_PLACEMENT_3D ( 'NONE', #533, #4267, #7301 ) ;
#3383=ORIENTED_EDGE ( 'NONE', *, *, #1559, .T. ) ;
#3384=CARTESIAN_POINT ( 'NONE',  ( 19.99999999999999645, 0.000000000000000000, 0.000000000000000000 ) ) ;
#3385=CARTESIAN_POINT ( 'NONE',  ( 19.99999999999997868, 3.565124043461763037, -5.527927226701607744 ) ) ;
#3386=FACE_OUTER_BOUND ( 'NONE', #9740, .T. ) ;
#3388=DIRECTION ( 'NONE',  ( 1.140150527077241873E-30, 0.000000000000000000, -1.000000000000000000 ) ) ;
#3390=CARTESIAN_POINT ( 'NONE',  ( 19.99999999999997868, 6.424561140605097087, -0.9808237102696195642 ) ) ;
#3391=EDGE_CURVE ( 'NONE', #4606, #8354, #2367, .T. ) ;
#3392=AXIS2_PLACEMENT_3D ( 'NONE', #9589, #6780, #6593 ) ;
#3393=EDGE_LOOP ( 'NONE', ( #7871, #9625, #11895, #4353 ) ) ;
#3394=DIRECTION ( 'NONE',  ( -1.000000000000000000, 1.010728034814421376E-30, 1.090846720500930387E-30 ) ) ;
#3395=ORIENTED_EDGE ( 'NONE', *, *, #7749, .T. ) ;
#3399=CIRCLE ( 'NONE', #10568, 2.800000000000004263 ) ;
#3409=EDGE_LOOP ( 'NONE', ( #11844, #1968, #3778, #10857 ) ) ;
#3410=AXIS2_PLACEMENT_3D ( 'NONE', #122, #4048, #6175 ) ;
#3411=CIRCLE ( 'NONE', #7719, 2.800000000000002487 ) ;
#3412=VERTEX_POINT ( 'NONE', #12533 ) ;
#3414=VERTEX_POINT ( 'NONE', #3767 ) ;
#3416=ADVANCED_FACE ( 'NONE', ( #981 ), #11500, .T. ) ;
#3418=ORIENTED_EDGE ( 'NONE', *, *, #11715, .T. ) ;
#3422=CARTESIAN_POINT ( 'NONE',  ( 9.999999999999998224, 7.164568425986781897, -1.851744925564387856 ) ) ;
#3423=DIRECTION ( 'NONE',  ( 1.140150527077241873E-30, 0.000000000000000000, -1.000000000000000000 ) ) ;
#3424=DIRECTION ( 'NONE',  ( 1.503766100577551302E-30, -0.7818314824680222541, -0.6234898018587429203 ) ) ;
#3425=EDGE_CURVE ( 'NONE', #8686, #1459, #9714, .T. ) ;
#3426=DIRECTION ( 'NONE',  ( -1.000000000000000000, 1.010728034814421376E-30, 1.090846720500930387E-30 ) ) ;
#3427=ORIENTED_EDGE ( 'NONE', *, *, #6040, .T. ) ;
#3429=CIRCLE ( 'NONE', #11849, 2.800000000000003819 ) ;
#3430=DIRECTION ( 'NONE',  ( 0.000000000000000000, 0.000000000000000000, 1.000000000000000000 ) ) ;
#3432=DIRECTION ( 'NONE',  ( -1.000000000000000000, 1.010728034814421376E-30, 1.090846720500930387E-30 ) ) ;
#3437=CYLINDRICAL_SURFACE ( 'NONE', #7093, 2.800000000000003819 ) ;
#3438=LINE ( 'NONE', #6253, #3491 ) ;
#3447=CARTESIAN_POINT ( 'NONE',  ( 9.999999999999980460, -3.612733913993635859, 6.458185013351679160 ) ) ;
#3448=LINE ( 'NONE', #6661, #11465 ) ;
#3453=CIRCLE ( 'NONE', #5088, 2.800000000000004263 ) ;
#3457=ORIENTED_EDGE ( 'NONE', *, *, #5003, .F. ) ;
#3458=ORIENTED_EDGE ( 'NONE', *, *, #10519, .T. ) ;
#3459=ORIENTED_EDGE ( 'NONE', *, *, #3316, .T. ) ;
#3461=ORIENTED_EDGE ( 'NONE', *, *, #10011, .F. ) ;
#3463=CARTESIAN_POINT ( 'NONE',  ( 19.99999999999999645, -2.099089055167807860, 6.233932467347772288 ) ) ;
#3467=CARTESIAN_POINT ( 'NONE',  ( 9.999999999999998224, -4.518585619147841292, -5.860237538055118378 ) ) ;
#3469=LINE ( 'NONE', #1454, #11633 ) ;
#3470=EDGE_CURVE ( 'NONE', #11154, #8658, #8498, .T. ) ;
#3472=CARTESIAN_POINT ( 'NONE',  ( 19.99999999999999645, 0.2110513566293444054, 7.396989747516548697 ) ) ;
#3474=EDGE_LOOP ( 'NONE', ( #4408, #11578, #2239, #5120 ) ) ;
#3475=ORIENTED_EDGE ( 'NONE', *, *, #6690, .F. ) ;
#3476=ORIENTED_EDGE ( 'NONE', *, *, #375, .T. ) ;
#3477=VERTEX_POINT ( 'NONE', #11624 ) ;
#3484=CARTESIAN_POINT ( 'NONE',  ( 0.000000000000000000, 0.000000000000000000, 0.000000000000000000 ) ) ;
#3486=ORIENTED_EDGE ( 'NONE', *, *, #10436, .F. ) ;
#3491=VECTOR ( 'NONE', #10160, 1000.000000000000000 ) ;
#3492=LINE ( 'NONE', #11217, #1995 ) ;
#3494=AXIS2_PLACEMENT_3D ( 'NONE', #6432, #2638, #10474 ) ;
#3497=EDGE_LOOP ( 'NONE', ( #5062, #11549, #7558, #113 ) ) ;
#3499=CARTESIAN_POINT ( 'NONE',  ( 9.999999999999998224, 2.796709610837451621, -6.851161606081828559 ) ) ;
#3502=CARTESIAN_POINT ( 'NONE',  ( 0.000000000000000000, 3.681899619563770543, 5.450844343808953774 ) ) ;
#3503=AXIS2_PLACEMENT_3D ( 'NONE', #3802, #9697, #11659 ) ;
#3505=CARTESIAN_POINT ( 'NONE',  ( 19.99999999999997868, 3.565124043461763037, -5.527927226701607744 ) ) ;
#3511=AXIS2_PLACEMENT_3D ( 'NONE', #4587, #5733, #3627 ) ;
#3513=DIRECTION ( 'NONE',  ( -1.000000000000000000, 1.010728034814421376E-30, 1.090846720500930387E-30 ) ) ;
#3518=ORIENTED_EDGE ( 'NONE', *, *, #5800, .F. ) ;
#3520=AXIS2_PLACEMENT_3D ( 'NONE', #11691, #3901, #2699 ) ;
#3522=ORIENTED_EDGE ( 'NONE', *, *, #10099, .T. ) ;
#3524=DIRECTION ( 'NONE',  ( -1.000000000000000000, 1.010728034814421376E-30, 1.090846720500930387E-30 ) ) ;
#3525=CARTESIAN_POINT ( 'NONE',  ( 19.99999999999997868, 5.280167904461786854, -3.922743398397314341 ) ) ;
#3528=CYLINDRICAL_SURFACE ( 'NONE', #12460, 6.499000000000010324 ) ;
#3529=FACE_OUTER_BOUND ( 'NONE', #6424, .T. ) ;
#3531=EDGE_CURVE ( 'NONE', #8231, #3178, #3580, .T. ) ;
#3536=EDGE_LOOP ( 'NONE', ( #6168, #3218, #12152, #743 ) ) ;
#3540=CARTESIAN_POINT ( 'NONE',  ( 0.000000000000000000, 3.975087478966635945, 6.241688836730221901 ) ) ;
#3543=DIRECTION ( 'NONE',  ( -1.000000000000000000, 1.010728034814421376E-30, 1.090846720500930387E-30 ) ) ;
#3544=CARTESIAN_POINT ( 'NONE',  ( 19.99999999999999645, 0.000000000000000000, 0.000000000000000000 ) ) ;
#3545=CARTESIAN_POINT ( 'NONE',  ( 19.99999999999999645, 0.000000000000000000, 0.000000000000000000 ) ) ;
#3547=EDGE_CURVE ( 'NONE', #9929, #3010, #9600, .T. ) ;
#3548=DIRECTION ( 'NONE',  ( 0.000000000000000000, 0.000000000000000000, 1.000000000000000000 ) ) ;
#3549=EDGE_CURVE ( 'NONE', #5919, #5117, #11684, .T. ) ;
#3550=EDGE_LOOP ( 'NONE', ( #4460, #8266, #3264, #11637 ) ) ;
#3552=ORIENTED_EDGE ( 'NONE', *, *, #7749, .F. ) ;
#3556=CARTESIAN_POINT ( 'NONE',  ( 0.000000000000000000, 0.000000000000000000, 0.000000000000000000 ) ) ;
#3560=LINE ( 'NONE', #7480, #6164 ) ;
#3561=CIRCLE ( 'NONE', #3370, 6.499000000000005883 ) ;
#3565=EDGE_CURVE ( 'NONE', #5894, #6626, #12006, .T. ) ;
#3566=CYLINDRICAL_SURFACE ( 'NONE', #5552, 2.800000000000003819 ) ;
#3569=CARTESIAN_POINT ( 'NONE',  ( 0.000000000000000000, -5.932103089875909951, -2.654647609586779922 ) ) ;
#3570=VECTOR ( 'NONE', #4878, 1000.000000000000000 ) ;
#3572=CARTESIAN_POINT ( 'NONE',  ( 0.000000000000000000, 0.000000000000000000, 0.000000000000000000 ) ) ;
#3573=CARTESIAN_POINT ( 'NONE',  ( 19.99999999999997868, 1.052479792859146723, -6.413211932068299426 ) ) ;
#3575=CARTESIAN_POINT ( 'NONE',  ( 9.999999999999998224, 7.380072687735808934, -0.5427035320837159116 ) ) ;
#3579=ORIENTED_EDGE ( 'NONE', *, *, #6176, .F. ) ;
#3580=CIRCLE ( 'NONE', #10133, 2.800000000000003375 ) ;
#3581=ORIENTED_EDGE ( 'NONE', *, *, #3997, .F. ) ;
#3586=DIRECTION ( 'NONE',  ( -1.000000000000000000, 1.010728034814421376E-30, 1.090846720500930387E-30 ) ) ;
#3587=EDGE_CURVE ( 'NONE', #7514, #11636, #2135, .T. ) ;
#3588=LINE ( 'NONE', #3467, #12690 ) ;
#3589=VERTEX_POINT ( 'NONE', #146 ) ;
#3591=AXIS2_PLACEMENT_3D ( 'NONE', #9894, #4780, #6718 ) ;
#3592=DIRECTION ( 'NONE',  ( 0.000000000000000000, 0.000000000000000000, 1.000000000000000000 ) ) ;
#3594=VERTEX_POINT ( 'NONE', #2082 ) ;
#3596=ORIENTED_EDGE ( 'NONE', *, *, #1243, .F. ) ;
#3602=FACE_BOUND ( 'NONE', #12467, .T. ) ;
#3603=ORIENTED_EDGE ( 'NONE', *, *, #4448, .T. ) ;
#3604=EDGE_CURVE ( 'NONE', #3737, #6636, #3064, .T. ) ;
#3605=DIRECTION ( 'NONE',  ( 0.000000000000000000, 0.000000000000000000, 1.000000000000000000 ) ) ;
#3608=VECTOR ( 'NONE', #8235, 1000.000000000000000 ) ;
#3612=ORIENTED_EDGE ( 'NONE', *, *, #2120, .F. ) ;
#3613=ORIENTED_EDGE ( 'NONE', *, *, #5847, .T. ) ;
#3615=AXIS2_PLACEMENT_3D ( 'NONE', #7023, #3173, #10934 ) ;
#3617=ORIENTED_EDGE ( 'NONE', *, *, #7517, .F. ) ;
#3618=VECTOR ( 'NONE', #7958, 1000.000000000000000 ) ;
#3619=DIRECTION ( 'NONE',  ( -1.000000000000000000, 1.010728034814421376E-30, 1.090846720500930387E-30 ) ) ;
#3621=DIRECTION ( 'NONE',  ( 0.000000000000000000, 0.5877852522924685852, 0.8090169943749506709 ) ) ;
#3625=CARTESIAN_POINT ( 'NONE',  ( 19.99999999999999645, -5.492355906873351401, -4.959236492872019397 ) ) ;
#3627=DIRECTION ( 'NONE',  ( 7.241496590895993670E-32, 0.6579387259397136978, -0.7530714660036098573 ) ) ;
#3629=CYLINDRICAL_SURFACE ( 'NONE', #9449, 2.800000000000003819 ) ;
#3630=VERTEX_POINT ( 'NONE', #7932 ) ;
#3632=DIRECTION ( 'NONE',  ( 0.000000000000000000, -0.9909497617679332571, -0.1342332658176667581 ) ) ;
#3633=DIRECTION ( 'NONE',  ( 0.000000000000000000, 0.000000000000000000, 1.000000000000000000 ) ) ;
#3642=ORIENTED_EDGE ( 'NONE', *, *, #11747, .T. ) ;
#3643=ORIENTED_EDGE ( 'NONE', *, *, #6490, .F. ) ;
#3648=CIRCLE ( 'NONE', #11049, 2.800000000000002487 ) ;
#3652=CARTESIAN_POINT ( 'NONE',  ( -10.00000000000000178, 0.000000000000000000, 0.000000000000000000 ) ) ;
#3654=EDGE_LOOP ( 'NONE', ( #5185, #7120, #215, #8534 ) ) ;
#3657=ORIENTED_EDGE ( 'NONE', *, *, #6412, .T. ) ;
#3660=VERTEX_POINT ( 'NONE', #9090 ) ;
#3661=DIRECTION ( 'NONE',  ( -1.000000000000000000, 1.010728034814421376E-30, 1.090846720500930387E-30 ) ) ;
#3663=EDGE_LOOP ( 'NONE', ( #8523, #2860, #12695, #6763 ) ) ;
#3666=ORIENTED_EDGE ( 'NONE', *, *, #59, .T. ) ;
#3674=FACE_OUTER_BOUND ( 'NONE', #2060, .T. ) ;
#3677=DIRECTION ( 'NONE',  ( -1.429810390713081971E-30, 0.5877852522924685852, 0.8090169943749506709 ) ) ;
#3679=CARTESIAN_POINT ( 'NONE',  ( 19.99999999999999645, 6.057062246029508046, 4.251117141143484268 ) ) ;
#3685=EDGE_CURVE ( 'NONE', #4011, #9943, #11096, .T. ) ;
#3687=ADVANCED_FACE ( 'NONE', ( #1299 ), #7873, .T. ) ;
#3688=DIRECTION ( 'NONE',  ( -1.000000000000000000, 1.010728034814421376E-30, 1.090846720500930387E-30 ) ) ;
#3690=AXIS2_PLACEMENT_3D ( 'NONE', #12175, #1148, #2251 ) ;
#3697=LINE ( 'NONE', #656, #1344 ) ;
#3700=AXIS2_PLACEMENT_3D ( 'NONE', #5101, #7166, #6128 ) ;
#3701=CIRCLE ( 'NONE', #7800, 7.400000000000011902 ) ;
#3705=ORIENTED_EDGE ( 'NONE', *, *, #12507, .F. ) ;
#3708=AXIS2_PLACEMENT_3D ( 'NONE', #5605, #6583, #10497 ) ;
#3710=FACE_OUTER_BOUND ( 'NONE', #10638, .T. ) ;
#3712=CIRCLE ( 'NONE', #10688, 2.800000000000002931 ) ;
#3713=DIRECTION ( 'NONE',  ( 1.000000000000000000, -1.010728034814421376E-30, -1.090846720500930387E-30 ) ) ;
#3714=ORIENTED_EDGE ( 'NONE', *, *, #7229, .T. ) ;
#3715=DIRECTION ( 'NONE',  ( -1.000000000000000000, 1.010728034814421376E-30, 1.090846720500930387E-30 ) ) ;
#3717=VERTEX_POINT ( 'NONE', #12263 ) ;
#3719=ORIENTED_EDGE ( 'NONE', *, *, #5293, .F. ) ;
#3720=AXIS2_PLACEMENT_3D ( 'NONE', #4573, #5401, #2519 ) ;
#3721=ORIENTED_EDGE ( 'NONE', *, *, #4787, .F. ) ;
#3723=ADVANCED_FACE ( 'NONE', ( #1620 ), #5360, .T. ) ;
#3724=CARTESIAN_POINT ( 'NONE',  ( 19.99999999999999645, 5.483475578891613189, 3.488337222187588793 ) ) ;
#3725=ORIENTED_EDGE ( 'NONE', *, *, #12034, .F. ) ;
#3726=CARTESIAN_POINT ( 'NONE',  ( 19.99999999999999645, 5.670261409740655623, 3.175710400084685858 ) ) ;
#3727=LINE ( 'NONE', #9812, #679 ) ;
#3730=DIRECTION ( 'NONE',  ( -1.000000000000000000, 1.010728034814421376E-30, 1.090846720500930387E-30 ) ) ;
#3731=VERTEX_POINT ( 'NONE', #9212 ) ;
#3732=ORIENTED_EDGE ( 'NONE', *, *, #12515, .F. ) ;
#3735=AXIS2_PLACEMENT_3D ( 'NONE', #6080, #8068, #11956 ) ;
#3737=VERTEX_POINT ( 'NONE', #12138 ) ;
#3740=EDGE_CURVE ( 'NONE', #5455, #11575, #8448, .T. ) ;
#3741=EDGE_CURVE ( 'NONE', #4036, #6829, #1493, .T. ) ;
#3742=EDGE_CURVE ( 'NONE', #5751, #4277, #6037, .T. ) ;
#3743=VECTOR ( 'NONE', #6907, 1000.000000000000000 ) ;
#3746=CARTESIAN_POINT ( 'NONE',  ( 19.99999999999997868, -2.401522331692818035, -6.999477872697425163 ) ) ;
#3747=ORIENTED_EDGE ( 'NONE', *, *, #7999, .T. ) ;
#3748=CARTESIAN_POINT ( 'NONE',  ( 0.000000000000000000, 0.000000000000000000, 0.000000000000000000 ) ) ;
#3749=EDGE_CURVE ( 'NONE', #10396, #7062, #9396, .T. ) ;
#3750=ORIENTED_EDGE ( 'NONE', *, *, #9055, .F. ) ;
#3752=DIRECTION ( 'NONE',  ( -1.000000000000000000, 1.010728034814421376E-30, 1.090846720500930387E-30 ) ) ;
#3755=CARTESIAN_POINT ( 'NONE',  ( 19.99999999999997868, 3.681899619563859360, -5.450844343808918246 ) ) ;
#3757=DIRECTION ( 'NONE',  ( -1.000000000000000000, 1.010728034814421376E-30, 1.090846720500930387E-30 ) ) ;
#3759=DIRECTION ( 'NONE',  ( -1.000000000000000000, 1.010728034814421376E-30, 1.090846720500930387E-30 ) ) ;
#3760=CIRCLE ( 'NONE', #4373, 6.499000000000008548 ) ;
#3761=ADVANCED_FACE ( 'NONE', ( #7366 ), #2347, .T. ) ;
#3764=VERTEX_POINT ( 'NONE', #5494 ) ;
#3766=VECTOR ( 'NONE', #8123, 1000.000000000000000 ) ;
#3767=CARTESIAN_POINT ( 'NONE',  ( 19.99999999999999645, 5.200656487704265807, 5.264330166022984869 ) ) ;
#3770=ADVANCED_FACE ( 'NONE', ( #10171 ), #2541, .T. ) ;
#3771=DIRECTION ( 'NONE',  ( 0.000000000000000000, -0.7227948638273979931, 0.6910626489868579858 ) ) ;
#3774=DIRECTION ( 'NONE',  ( -1.000000000000000000, 1.010728034814421376E-30, 1.090846720500930387E-30 ) ) ;
#3775=FACE_OUTER_BOUND ( 'NONE', #12610, .T. ) ;
#3778=ORIENTED_EDGE ( 'NONE', *, *, #8477, .T. ) ;
#3783=FACE_OUTER_BOUND ( 'NONE', #6903, .T. ) ;
#3784=ORIENTED_EDGE ( 'NONE', *, *, #10381, .T. ) ;
#3787=VERTEX_POINT ( 'NONE', #12204 ) ;
#3788=VECTOR ( 'NONE', #8899, 1000.000000000000000 ) ;
#3792=EDGE_CURVE ( 'NONE', #291, #2575, #9317, .T. ) ;
#3793=VERTEX_POINT ( 'NONE', #8386 ) ;
#3794=VERTEX_POINT ( 'NONE', #7243 ) ;
#3800=CIRCLE ( 'NONE', #10394, 2.800000000000002931 ) ;
#3802=CARTESIAN_POINT ( 'NONE',  ( -10.00000000000000178, 0.000000000000000000, 0.000000000000000000 ) ) ;
#3803=DIRECTION ( 'NONE',  ( -1.000000000000000000, 1.010728034814421376E-30, 1.090846720500930387E-30 ) ) ;
#3805=ORIENTED_EDGE ( 'NONE', *, *, #3316, .F. ) ;
#3807=CIRCLE ( 'NONE', #2384, 2.800000000000003375 ) ;
#3810=CARTESIAN_POINT ( 'NONE',  ( 0.000000000000000000, -4.621065432155110564, 4.569765340993028779 ) ) ;
#3811=EDGE_CURVE ( 'NONE', #12687, #8054, #7477, .T. ) ;
#3812=EDGE_CURVE ( 'NONE', #10396, #4592, #9523, .T. ) ;
#3814=CARTESIAN_POINT ( 'NONE',  ( 19.99999999999999645, 4.192831774278975132, 4.965597920955411304 ) ) ;
#3815=CIRCLE ( 'NONE', #1956, 6.499000000000006771 ) ;
#3817=CARTESIAN_POINT ( 'NONE',  ( 0.000000000000000000, 6.359055127044410227, -1.682410996215903731 ) ) ;
#3818=CARTESIAN_POINT ( 'NONE',  ( 19.99999999999999645, -3.730839900301562206, 5.321450426182494198 ) ) ;
#3826=AXIS2_PLACEMENT_3D ( 'NONE', #5560, #5679, #6596 ) ;
#3830=CYLINDRICAL_SURFACE ( 'NONE', #10864, 7.400000000000010125 ) ;
#3831=DIRECTION ( 'NONE',  ( -1.140150527077241873E-30, 0.000000000000000000, 1.000000000000000000 ) ) ;
#3832=VERTEX_POINT ( 'NONE', #5425 ) ;
#3835=VECTOR ( 'NONE', #3315, 1000.000000000000000 ) ;
#3837=VERTEX_POINT ( 'NONE', #3569 ) ;
#3838=DIRECTION ( 'NONE',  ( -1.000000000000000000, 1.010728034814421376E-30, 1.090846720500930387E-30 ) ) ;
#3841=ORIENTED_EDGE ( 'NONE', *, *, #894, .T. ) ;
#3845=DIRECTION ( 'NONE',  ( -1.000000000000000000, 1.010728034814421376E-30, 1.090846720500930387E-30 ) ) ;
#3847=CIRCLE ( 'NONE', #7951, 2.800000000000002931 ) ;
#3850=CIRCLE ( 'NONE', #6304, 6.499000000000008548 ) ;
#3853=CARTESIAN_POINT ( 'NONE',  ( 19.99999999999999645, 0.000000000000000000, 0.000000000000000000 ) ) ;
#3854=EDGE_CURVE ( 'NONE', #11879, #1901, #7891, .T. ) ;
#3855=DIRECTION ( 'NONE',  ( 0.000000000000000000, -0.7227948638273979931, 0.6910626489868579858 ) ) ;
#3857=CIRCLE ( 'NONE', #7350, 2.800000000000002487 ) ;
#3859=AXIS2_PLACEMENT_3D ( 'NONE', #1623, #7367, #466 ) ;
#3860=ORIENTED_EDGE ( 'NONE', *, *, #7163, .T. ) ;
#3862=DIRECTION ( 'NONE',  ( 1.503766100577551302E-30, -0.6579387259397027066, -0.7530714660036197383 ) ) ;
#3863=ORIENTED_EDGE ( 'NONE', *, *, #5075, .T. ) ;
#3864=CYLINDRICAL_SURFACE ( 'NONE', #5129, 2.800000000000003819 ) ;
#3865=ORIENTED_EDGE ( 'NONE', *, *, #8891, .F. ) ;
#3867=CIRCLE ( 'NONE', #4056, 6.499000000000010324 ) ;
#3870=ORIENTED_EDGE ( 'NONE', *, *, #5003, .T. ) ;
#3876=FACE_OUTER_BOUND ( 'NONE', #10135, .T. ) ;
#3877=CARTESIAN_POINT ( 'NONE',  ( 19.99999999999999645, 5.670261409740655623, 3.175710400084685858 ) ) ;
#3878=EDGE_CURVE ( 'NONE', #4885, #10785, #5223, .T. ) ;
#3888=DIRECTION ( 'NONE',  ( 0.000000000000000000, -0.1785568947986228838, -0.9839295885986322210 ) ) ;
#3890=DIRECTION ( 'NONE',  ( 0.000000000000000000, 0.000000000000000000, 1.000000000000000000 ) ) ;
#3891=CARTESIAN_POINT ( 'NONE',  ( 0.000000000000000000, 0.2252065540230630269, -6.573992004634855668 ) ) ;
#3892=VERTEX_POINT ( 'NONE', #5676 ) ;
#3893=EDGE_CURVE ( 'NONE', #9064, #8334, #1750, .T. ) ;
#3895=ADVANCED_FACE ( 'NONE', ( #4716 ), #7548, .T. ) ;
#3901=DIRECTION ( 'NONE',  ( -1.000000000000000000, 1.010728034814421376E-30, 1.090846720500930387E-30 ) ) ;
#3902=ORIENTED_EDGE ( 'NONE', *, *, #317, .F. ) ;
#3903=EDGE_LOOP ( 'NONE', ( #1570, #9581, #1270, #9893 ) ) ;
#3908=CARTESIAN_POINT ( 'NONE',  ( 19.99999999999999645, -6.577476285968334224, 2.730038749995000735 ) ) ;
#3911=AXIS2_PLACEMENT_3D ( 'NONE', #5491, #12453, #7612 ) ;
#3912=DIRECTION ( 'NONE',  ( -1.000000000000000000, 1.010728034814421376E-30, 1.090846720500930387E-30 ) ) ;
#3913=CARTESIAN_POINT ( 'NONE',  ( 0.000000000000000000, -0.4733669331952392034, 6.481737787550296837 ) ) ;
#3915=CARTESIAN_POINT ( 'NONE',  ( 19.99999999999997868, 3.019282868015183752, -6.756029230465944835 ) ) ;
#3916=CARTESIAN_POINT ( 'NONE',  ( 19.99999999999999645, 4.177097350749791715, 6.108343287861209170 ) ) ;
#3921=DIRECTION ( 'NONE',  ( -1.000000000000000000, 1.010728034814421376E-30, 1.090846720500930387E-30 ) ) ;
#3927=EDGE_CURVE ( 'NONE', #8041, #5416, #2356, .T. ) ;
#3928=DIRECTION ( 'NONE',  ( -1.000000000000000000, 1.010728034814421376E-30, 1.090846720500930387E-30 ) ) ;
#3930=ORIENTED_EDGE ( 'NONE', *, *, #10640, .F. ) ;
#3932=ORIENTED_EDGE ( 'NONE', *, *, #8076, .F. ) ;
#3933=DIRECTION ( 'NONE',  ( -1.000000000000000000, 1.010728034814421376E-30, 1.090846720500930387E-30 ) ) ;
#3937=VECTOR ( 'NONE', #4726, 1000.000000000000000 ) ;
#3938=DIRECTION ( 'NONE',  ( 0.000000000000000000, 0.5128992774059070170, -0.8584487936018656562 ) ) ;
#3942=EDGE_CURVE ( 'NONE', #8054, #3292, #11608, .T. ) ;
#3943=CARTESIAN_POINT ( 'NONE',  ( 9.999999999999980460, -4.518585619147922117, 5.860237538055066864 ) ) ;
#3946=EDGE_CURVE ( 'NONE', #2242, #2862, #7086, .T. ) ;
#3949=ORIENTED_EDGE ( 'NONE', *, *, #1801, .T. ) ;
#3951=CARTESIAN_POINT ( 'NONE',  ( 19.99999999999999645, -6.969736844459680114, -2.486517307195224902 ) ) ;
#3954=ORIENTED_EDGE ( 'NONE', *, *, #8130, .T. ) ;
#3955=CYLINDRICAL_SURFACE ( 'NONE', #5863, 2.800000000000003819 ) ;
#3961=ORIENTED_EDGE ( 'NONE', *, *, #4062, .T. ) ;
#3964=VERTEX_POINT ( 'NONE', #9525 ) ;
#3972=EDGE_CURVE ( 'NONE', #2328, #363, #2142, .T. ) ;
#3973=DIRECTION ( 'NONE',  ( -1.000000000000000000, 1.010728034814421376E-30, 1.090846720500930387E-30 ) ) ;
#3975=DIRECTION ( 'NONE',  ( 0.000000000000000000, 0.000000000000000000, 1.000000000000000000 ) ) ;
#3977=EDGE_LOOP ( 'NONE', ( #1247, #7856, #8384, #7936 ) ) ;
#3978=ORIENTED_EDGE ( 'NONE', *, *, #2280, .T. ) ;
#3982=ADVANCED_FACE ( 'NONE', ( #6659 ), #10564, .T. ) ;
#3983=ORIENTED_EDGE ( 'NONE', *, *, #1789, .T. ) ;
#3985=VERTEX_POINT ( 'NONE', #5740 ) ;
#3986=EDGE_CURVE ( 'NONE', #11644, #8701, #8506, .T. ) ;
#3988=AXIS2_PLACEMENT_3D ( 'NONE', #11488, #2123, #7021 ) ;
#3989=DIRECTION ( 'NONE',  ( 0.000000000000000000, 0.000000000000000000, 1.000000000000000000 ) ) ;
#3990=ORIENTED_EDGE ( 'NONE', *, *, #2055, .F. ) ;
#3993=DIRECTION ( 'NONE',  ( 0.000000000000000000, -0.9510565162951502005, -0.3090169943749582204 ) ) ;
#3994=EDGE_CURVE ( 'NONE', #11719, #11828, #10140, .T. ) ;
#3997=EDGE_CURVE ( 'NONE', #2783, #12687, #1306, .T. ) ;
#3998=FACE_OUTER_BOUND ( 'NONE', #3977, .T. ) ;
#4000=CARTESIAN_POINT ( 'NONE',  ( 19.99999999999999645, 0.000000000000000000, 0.000000000000000000 ) ) ;
#4002=EDGE_CURVE ( 'NONE', #477, #4490, #10020, .T. ) ;
#4006=CARTESIAN_POINT ( 'NONE',  ( 0.000000000000000000, 0.6915992404089872370, 6.462096524400245734 ) ) ;
#4011=VERTEX_POINT ( 'NONE', #7083 ) ;
#4015=DIRECTION ( 'NONE',  ( -1.140150527077241873E-30, 0.000000000000000000, 1.000000000000000000 ) ) ;
#4022=ORIENTED_EDGE ( 'NONE', *, *, #12303, .T. ) ;
#4025=EDGE_LOOP ( 'NONE', ( #12184, #1777, #12236, #2379 ) ) ;
#4028=DIRECTION ( 'NONE',  ( 1.140150527077241873E-30, 0.000000000000000000, -1.000000000000000000 ) ) ;
#4032=DIRECTION ( 'NONE',  ( -1.000000000000000000, 1.010728034814421376E-30, 1.090846720500930387E-30 ) ) ;
#4034=ADVANCED_FACE ( 'NONE', ( #2188 ), #7147, .T. ) ;
#4035=ORIENTED_EDGE ( 'NONE', *, *, #7970, .T. ) ;
#4036=VERTEX_POINT ( 'NONE', #9250 ) ;
#4037=ORIENTED_EDGE ( 'NONE', *, *, #8454, .F. ) ;
#4038=AXIS2_PLACEMENT_3D ( 'NONE', #11948, #2085, #10900 ) ;
#4039=LINE ( 'NONE', #3097, #12209 ) ;
#4040=CIRCLE ( 'NONE', #1360, 2.800000000000003819 ) ;
#4044=ORIENTED_EDGE ( 'NONE', *, *, #8938, .T. ) ;
#4046=DIRECTION ( 'NONE',  ( -1.000000000000000000, 1.010728034814421376E-30, 1.090846720500930387E-30 ) ) ;
#4048=DIRECTION ( 'NONE',  ( -1.000000000000000000, 1.010728034814421376E-30, 1.090846720500930387E-30 ) ) ;
#4051=CARTESIAN_POINT ( 'NONE',  ( 0.000000000000000000, 3.019282868015180643, -6.756029230465944835 ) ) ;
#4054=ORIENTED_EDGE ( 'NONE', *, *, #10514, .T. ) ;
#4055=DIRECTION ( 'NONE',  ( -1.140150527077241873E-30, 0.000000000000000000, 1.000000000000000000 ) ) ;
#4056=AXIS2_PLACEMENT_3D ( 'NONE', #5591, #3543, #4434 ) ;
#4060=DIRECTION ( 'NONE',  ( 0.000000000000000000, 0.000000000000000000, 1.000000000000000000 ) ) ;
#4062=EDGE_CURVE ( 'NONE', #11340, #3477, #9122, .T. ) ;
#4064=ADVANCED_FACE ( 'NONE', ( #8098 ), #1207, .T. ) ;
#4072=CARTESIAN_POINT ( 'NONE',  ( 0.000000000000000000, 6.057062246029573771, -4.251117141143404332 ) ) ;
#4073=CARTESIAN_POINT ( 'NONE',  ( 0.000000000000000000, -5.774092856145694341, -2.982759240804940148 ) ) ;
#4074=DIRECTION ( 'NONE',  ( 0.000000000000000000, 0.000000000000000000, 1.000000000000000000 ) ) ;
#4077=EDGE_CURVE ( 'NONE', #10909, #12630, #4192, .T. ) ;
#4078=DIRECTION ( 'NONE',  ( -1.000000000000000000, 1.010728034814421376E-30, 1.090846720500930387E-30 ) ) ;
#4079=EDGE_CURVE ( 'NONE', #125, #2328, #12237, .T. ) ;
#4083=ORIENTED_EDGE ( 'NONE', *, *, #4701, .T. ) ;
#4086=DIRECTION ( 'NONE',  ( 0.000000000000000000, 0.000000000000000000, 1.000000000000000000 ) ) ;
#4089=DIRECTION ( 'NONE',  ( 0.000000000000000000, 0.000000000000000000, 1.000000000000000000 ) ) ;
#4092=AXIS2_PLACEMENT_3D ( 'NONE', #3234, #7212, #6169 ) ;
#4098=ORIENTED_EDGE ( 'NONE', *, *, #8187, .F. ) ;
#4099=EDGE_CURVE ( 'NONE', #12171, #8569, #9940, .T. ) ;
#4101=AXIS2_PLACEMENT_3D ( 'NONE', #11916, #2192, #3365 ) ;
#4102=ORIENTED_EDGE ( 'NONE', *, *, #1446, .T. ) ;
#4105=CARTESIAN_POINT ( 'NONE',  ( 19.99999999999999645, 3.565124043461683101, 5.527927226701645935 ) ) ;
#4110=DIRECTION ( 'NONE',  ( 4.314083075427402290E-32, -0.7227948638273979931, 0.6910626489868579858 ) ) ;
#4111=EDGE_LOOP ( 'NONE', ( #4293, #3747, #12155, #545 ) ) ;
#4115=CARTESIAN_POINT ( 'NONE',  ( 19.99999999999999645, 1.531833341630123302, 6.396997380212702922 ) ) ;
#4116=CARTESIAN_POINT ( 'NONE',  ( 19.99999999999999645, 0.000000000000000000, 0.000000000000000000 ) ) ;
#4118=VERTEX_POINT ( 'NONE', #6171 ) ;
#4121=DIRECTION ( 'NONE',  ( -1.000000000000000000, 1.010728034814421376E-30, 1.090846720500930387E-30 ) ) ;
#4124=ADVANCED_FACE ( 'NONE', ( #1337 ), #5211, .T. ) ;
#4125=CARTESIAN_POINT ( 'NONE',  ( 19.99999999999999645, -1.113123845672405965, 7.315801754025019754 ) ) ;
#4128=FACE_OUTER_BOUND ( 'NONE', #11878, .T. ) ;
#4131=DIRECTION ( 'NONE',  ( -1.000000000000000000, 1.010728034814421376E-30, 1.090846720500930387E-30 ) ) ;
#4136=EDGE_CURVE ( 'NONE', #4592, #6148, #9562, .T. ) ;
#4137=ORIENTED_EDGE ( 'NONE', *, *, #1660, .T. ) ;
#4138=CARTESIAN_POINT ( 'NONE',  ( 19.99999999999999645, 0.000000000000000000, 0.000000000000000000 ) ) ;
#4140=DIRECTION ( 'NONE',  ( -1.000000000000000000, 1.010728034814421376E-30, 1.090846720500930387E-30 ) ) ;
#4142=CYLINDRICAL_SURFACE ( 'NONE', #4038, 6.499000000000010324 ) ;
#4144=DIRECTION ( 'NONE',  ( 0.000000000000000000, 0.000000000000000000, 1.000000000000000000 ) ) ;
#4145=AXIS2_PLACEMENT_3D ( 'NONE', #6967, #10882, #1161 ) ;
#4146=DIRECTION ( 'NONE',  ( -1.000000000000000000, 1.010728034814421376E-30, 1.090846720500930387E-30 ) ) ;
#4147=EDGE_CURVE ( 'NONE', #3717, #8468, #1530, .T. ) ;
#4149=DIRECTION ( 'NONE',  ( 0.000000000000000000, 0.000000000000000000, 1.000000000000000000 ) ) ;
#4150=ORIENTED_EDGE ( 'NONE', *, *, #12198, .T. ) ;
#4151=EDGE_CURVE ( 'NONE', #11776, #1400, #10277, .T. ) ;
#4153=ORIENTED_EDGE ( 'NONE', *, *, #11715, .F. ) ;
#4154=EDGE_LOOP ( 'NONE', ( #10074, #7337, #9554, #8349 ) ) ;
#4158=ADVANCED_FACE ( 'NONE', ( #5464 ), #9371, .T. ) ;
#4161=AXIS2_PLACEMENT_3D ( 'NONE', #8042, #5922, #11731 ) ;
#4162=VERTEX_POINT ( 'NONE', #12493 ) ;
#4165=DIRECTION ( 'NONE',  ( 0.000000000000000000, 0.000000000000000000, 1.000000000000000000 ) ) ;
#4166=EDGE_LOOP ( 'NONE', ( #7838, #12636, #10334, #6623 ) ) ;
#4169=VERTEX_POINT ( 'NONE', #9500 ) ;
#4171=ORIENTED_EDGE ( 'NONE', *, *, #3994, .T. ) ;
#4175=DIRECTION ( 'NONE',  ( -1.000000000000000000, 1.010728034814421376E-30, 1.090846720500930387E-30 ) ) ;
#4181=EDGE_CURVE ( 'NONE', #3319, #753, #3867, .T. ) ;
#4182=DIRECTION ( 'NONE',  ( -1.000000000000000000, 1.010728034814421376E-30, 1.090846720500930387E-30 ) ) ;
#4183=DIRECTION ( 'NONE',  ( 1.000000000000000000, -1.010728034814421376E-30, -1.090846720500930387E-30 ) ) ;
#4188=DIRECTION ( 'NONE',  ( -1.000000000000000000, 1.010728034814421376E-30, 1.090846720500930387E-30 ) ) ;
#4192=CIRCLE ( 'NONE', #12644, 2.800000000000003375 ) ;
#4195=FACE_OUTER_BOUND ( 'NONE', #9420, .T. ) ;
#4199=AXIS2_PLACEMENT_3D ( 'NONE', #5619, #2608, #9532 ) ;
#4202=ORIENTED_EDGE ( 'NONE', *, *, #8917, .T. ) ;
#4203=CARTESIAN_POINT ( 'NONE',  ( 19.99999999999997868, -7.258495115966569600, -1.440225208600917739 ) ) ;
#4206=CARTESIAN_POINT ( 'NONE',  ( 19.99999999999999645, 7.380072687735814263, 0.5427035320837090282 ) ) ;
#4207=CARTESIAN_POINT ( 'NONE',  ( 19.99999999999999645, -6.577476285968334224, -0.06996125000500313940 ) ) ;
#4211=DIRECTION ( 'NONE',  ( -1.000000000000000000, 1.010728034814421376E-30, 1.090846720500930387E-30 ) ) ;
#4217=ORIENTED_EDGE ( 'NONE', *, *, #4079, .F. ) ;
#4219=CARTESIAN_POINT ( 'NONE',  ( 0.000000000000000000, -6.413745496774080124, -3.691052519622338490 ) ) ;
#4221=DIRECTION ( 'NONE',  ( 0.000000000000000000, 0.000000000000000000, 1.000000000000000000 ) ) ;
#4222=DIRECTION ( 'NONE',  ( 1.140150527077241873E-30, 0.000000000000000000, -1.000000000000000000 ) ) ;
#4226=LINE ( 'NONE', #5314, #11246 ) ;
#4229=EDGE_LOOP ( 'NONE', ( #7376, #3461, #1024, #10894 ) ) ;
#4230=EDGE_CURVE ( 'NONE', #8468, #6636, #6948, .T. ) ;
#4233=ADVANCED_FACE ( 'NONE', ( #4569 ), #8480, .T. ) ;
#4241=CARTESIAN_POINT ( 'NONE',  ( 19.99999999999999645, -6.459281472512945932, 1.243290685169349485 ) ) ;
#4242=ORIENTED_EDGE ( 'NONE', *, *, #2568, .F. ) ;
#4243=DIRECTION ( 'NONE',  ( -1.000000000000000000, 1.010728034814421376E-30, 1.090846720500930387E-30 ) ) ;
#4244=CARTESIAN_POINT ( 'NONE',  ( 0.000000000000000000, 0.000000000000000000, 0.000000000000000000 ) ) ;
#4245=AXIS2_PLACEMENT_3D ( 'NONE', #7822, #2822, #984 ) ;
#4248=ORIENTED_EDGE ( 'NONE', *, *, #1608, .F. ) ;
#4251=DIRECTION ( 'NONE',  ( 0.000000000000000000, 0.000000000000000000, 1.000000000000000000 ) ) ;
#4253=AXIS2_PLACEMENT_3D ( 'NONE', #3067, #12008, #11032 ) ;
#4256=DIRECTION ( 'NONE',  ( -1.000000000000000000, 1.010728034814421376E-30, 1.090846720500930387E-30 ) ) ;
#4258=CARTESIAN_POINT ( 'NONE',  ( 19.99999999999999645, 0.000000000000000000, 0.000000000000000000 ) ) ;
#4264=ORIENTED_EDGE ( 'NONE', *, *, #8206, .T. ) ;
#4267=DIRECTION ( 'NONE',  ( -1.000000000000000000, 1.010728034814421376E-30, 1.090846720500930387E-30 ) ) ;
#4268=DIRECTION ( 'NONE',  ( -1.000000000000000000, 1.010728034814421376E-30, 1.090846720500930387E-30 ) ) ;
#4273=CARTESIAN_POINT ( 'NONE',  ( 19.99999999999999645, -6.213893036447818652, 1.903820982021499297 ) ) ;
#4274=ORIENTED_EDGE ( 'NONE', *, *, #9811, .F. ) ;
#4277=VERTEX_POINT ( 'NONE', #1725 ) ;
#4279=VERTEX_POINT ( 'NONE', #755 ) ;
#4280=DIRECTION ( 'NONE',  ( -1.000000000000000000, 1.010728034814421376E-30, 1.090846720500930387E-30 ) ) ;
#4284=DIRECTION ( 'NONE',  ( 1.000000000000000000, -1.010728034814421376E-30, -1.090846720500930387E-30 ) ) ;
#4285=LINE ( 'NONE', #1256, #4699 ) ;
#4287=CARTESIAN_POINT ( 'NONE',  ( 19.99999999999999645, -4.046291478462170410, -5.186098161460359179 ) ) ;
#4289=VECTOR ( 'NONE', #5943, 1000.000000000000000 ) ;
#4290=DIRECTION ( 'NONE',  ( -1.000000000000000000, 1.010728034814421376E-30, 1.090846720500930387E-30 ) ) ;
#4293=ORIENTED_EDGE ( 'NONE', *, *, #5727, .T. ) ;
#4294=ORIENTED_EDGE ( 'NONE', *, *, #9059, .F. ) ;
#4296=AXIS2_PLACEMENT_3D ( 'NONE', #10331, #2563, #7452 ) ;
#4301=AXIS2_PLACEMENT_3D ( 'NONE', #1445, #12087, #4221 ) ;
#4302=ORIENTED_EDGE ( 'NONE', *, *, #9334, .T. ) ;
#4303=DIRECTION ( 'NONE',  ( 1.000000000000000000, -1.010728034814421376E-30, -1.090846720500930387E-30 ) ) ;
#4305=CARTESIAN_POINT ( 'NONE',  ( 19.99999999999999645, -4.707829255731248885, 5.709320773864518195 ) ) ;
#4309=EDGE_LOOP ( 'NONE', ( #1441, #94, #1643, #437 ) ) ;
#4316=AXIS2_PLACEMENT_3D ( 'NONE', #1128, #2298, #8014 ) ;
#4322=DIRECTION ( 'NONE',  ( 0.000000000000000000, 0.000000000000000000, 1.000000000000000000 ) ) ;
#4323=EDGE_LOOP ( 'NONE', ( #760, #5899, #11045, #6572 ) ) ;
#4324=DIRECTION ( 'NONE',  ( 0.000000000000000000, 0.8345732537213000901, 0.5508969814521065267 ) ) ;
#4325=AXIS2_PLACEMENT_3D ( 'NONE', #4745, #5703, #2893 ) ;
#4326=CIRCLE ( 'NONE', #10890, 2.800000000000002931 ) ;
#4327=LINE ( 'NONE', #3379, #5184 ) ;
#4334=CYLINDRICAL_SURFACE ( 'NONE', #7543, 7.400000000000010125 ) ;
#4335=EDGE_CURVE ( 'NONE', #5973, #6015, #1851, .T. ) ;
#4336=DIRECTION ( 'NONE',  ( 1.000000000000000000, -1.010728034814421376E-30, -1.090846720500930387E-30 ) ) ;
#4337=DIRECTION ( 'NONE',  ( -1.000000000000000000, 1.010728034814421376E-30, 1.090846720500930387E-30 ) ) ;
#4342=CYLINDRICAL_SURFACE ( 'NONE', #10710, 7.400000000000010125 ) ;
#4345=ORIENTED_EDGE ( 'NONE', *, *, #9386, .T. ) ;
#4350=DIRECTION ( 'NONE',  ( -1.000000000000000000, 1.010728034814421376E-30, 1.090846720500930387E-30 ) ) ;
#4353=ORIENTED_EDGE ( 'NONE', *, *, #9491, .F. ) ;
#4356=VERTEX_POINT ( 'NONE', #12747 ) ;
#4358=EDGE_CURVE ( 'NONE', #9929, #5919, #9594, .T. ) ;
#4362=DIRECTION ( 'NONE',  ( -1.000000000000000000, 1.010728034814421376E-30, 1.090846720500930387E-30 ) ) ;
#4363=AXIS2_PLACEMENT_3D ( 'NONE', #5104, #2008, #977 ) ;
#4365=ORIENTED_EDGE ( 'NONE', *, *, #12034, .T. ) ;
#4367=DIRECTION ( 'NONE',  ( 0.000000000000000000, -0.9195277725514543476, 0.3930250316539146693 ) ) ;
#4368=ORIENTED_EDGE ( 'NONE', *, *, #3155, .F. ) ;
#4372=DIRECTION ( 'NONE',  ( -1.000000000000000000, 1.010728034814421376E-30, 1.090846720500930387E-30 ) ) ;
#4373=AXIS2_PLACEMENT_3D ( 'NONE', #253, #4188, #8178 ) ;
#4374=DIRECTION ( 'NONE',  ( 0.000000000000000000, 0.9749279121818227312, 0.2225209339563182787 ) ) ;
#4375=ORIENTED_EDGE ( 'NONE', *, *, #8905, .T. ) ;
#4382=DIRECTION ( 'NONE',  ( 0.000000000000000000, 0.000000000000000000, 1.000000000000000000 ) ) ;
#4386=AXIS2_PLACEMENT_3D ( 'NONE', #9937, #1132, #3217 ) ;
#4391=ADVANCED_FACE ( 'NONE', ( #10854 ), #2035, .T. ) ;
#4395=VERTEX_POINT ( 'NONE', #8861 ) ;
#4397=ADVANCED_FACE ( 'NONE', ( #2905 ), #8802, .T. ) ;
#4398=DIRECTION ( 'NONE',  ( 0.000000000000000000, 0.000000000000000000, 1.000000000000000000 ) ) ;
#4399=CARTESIAN_POINT ( 'NONE',  ( -10.00000000000000178, 0.000000000000000000, 0.000000000000000000 ) ) ;
#4402=DIRECTION ( 'NONE',  ( -1.000000000000000000, 1.010728034814421376E-30, 1.090846720500930387E-30 ) ) ;
#4407=ORIENTED_EDGE ( 'NONE', *, *, #4002, .T. ) ;
#4408=ORIENTED_EDGE ( 'NONE', *, *, #5789, .F. ) ;
#4410=ORIENTED_EDGE ( 'NONE', *, *, #2441, .F. ) ;
#4412=VERTEX_POINT ( 'NONE', #3915 ) ;
#4413=CYLINDRICAL_SURFACE ( 'NONE', #2967, 6.499000000000010324 ) ;
#4416=CARTESIAN_POINT ( 'NONE',  ( 0.000000000000000000, 7.100173756228419286, 2.085073771204575710 ) ) ;
#4422=AXIS2_PLACEMENT_3D ( 'NONE', #7008, #4032, #2036 ) ;
#4424=EDGE_LOOP ( 'NONE', ( #3750, #2234, #2503, #10653 ) ) ;
#4427=PRODUCT ( 'upper roller_ISO - Spur gear 0.4M 35T 20PA 20FW ---S35A75H50L5.0N', 'upper roller_ISO - Spur gear 0.4M 35T 20PA 20FW ---S35A75H50L5.0N', '', ( #1125 ) ) ;
#4430=DIRECTION ( 'NONE',  ( -1.140150527077241873E-30, 0.000000000000000000, 1.000000000000000000 ) ) ;
#4432=AXIS2_PLACEMENT_3D ( 'NONE', #3545, #6365, #7464 ) ;
#4434=DIRECTION ( 'NONE',  ( 0.000000000000000000, 0.000000000000000000, -1.000000000000000000 ) ) ;
#4437=DIRECTION ( 'NONE',  ( 0.000000000000000000, 0.000000000000000000, 1.000000000000000000 ) ) ;
#4438=DIRECTION ( 'NONE',  ( 1.140150527077241873E-30, 0.000000000000000000, -1.000000000000000000 ) ) ;
#4440=DIRECTION ( 'NONE',  ( -1.000000000000000000, 1.010728034814421376E-30, 1.090846720500930387E-30 ) ) ;
#4443=AXIS2_PLACEMENT_3D ( 'NONE', #6327, #1432, #5364 ) ;
#4448=EDGE_CURVE ( 'NONE', #12527, #955, #7960, .T. ) ;
#4450=AXIS2_PLACEMENT_3D ( 'NONE', #2235, #6152, #3152 ) ;
#4452=DIRECTION ( 'NONE',  ( 0.000000000000000000, -0.8805955318567322276, -0.4738686624730095165 ) ) ;
#4453=ORIENTED_EDGE ( 'NONE', *, *, #4002, .F. ) ;
#4456=CARTESIAN_POINT ( 'NONE',  ( 0.000000000000000000, 0.000000000000000000, 0.000000000000000000 ) ) ;
#4459=CARTESIAN_POINT ( 'NONE',  ( 0.000000000000000000, 0.000000000000000000, 0.000000000000000000 ) ) ;
#4460=ORIENTED_EDGE ( 'NONE', *, *, #1749, .F. ) ;
#4461=CARTESIAN_POINT ( 'NONE',  ( 19.99999999999997868, 6.544726022087268724, -0.6592800351836389794 ) ) ;
#4462=DIRECTION ( 'NONE',  ( 1.000000000000000000, -1.010728034814421376E-30, -1.090846720500930387E-30 ) ) ;
#4464=EDGE_CURVE ( 'NONE', #479, #5907, #151, .T. ) ;
#4468=EDGE_CURVE ( 'NONE', #8054, #11067, #8985, .T. ) ;
#4470=LINE ( 'NONE', #8390, #8315 ) ;
#4471=AXIS2_PLACEMENT_3D ( 'NONE', #1301, #2217, #9154 ) ;
#4479=VECTOR ( 'NONE', #8422, 1000.000000000000000 ) ;
#4480=CARTESIAN_POINT ( 'NONE',  ( 9.999999999999998224, 5.025702764809159895, -5.431603052487340655 ) ) ;
#4482=DIRECTION ( 'NONE',  ( 0.000000000000000000, 0.000000000000000000, 1.000000000000000000 ) ) ;
#4484=DIRECTION ( 'NONE',  ( -1.000000000000000000, 1.010728034814421376E-30, 1.090846720500930387E-30 ) ) ;
#4485=ORIENTED_EDGE ( 'NONE', *, *, #706, .T. ) ;
#4486=EDGE_CURVE ( 'NONE', #2488, #12421, #10210, .T. ) ;
#4487=CARTESIAN_POINT ( 'NONE',  ( 19.99999999999999645, 0.000000000000000000, 0.000000000000000000 ) ) ;
#4490=VERTEX_POINT ( 'NONE', #6283 ) ;
#4497=CARTESIAN_POINT ( 'NONE',  ( 0.000000000000000000, 1.528443194675508376, -7.240432404259457222 ) ) ;
#4498=DIRECTION ( 'NONE',  ( 0.000000000000000000, 0.000000000000000000, 1.000000000000000000 ) ) ;
#4499=VERTEX_POINT ( 'NONE', #10131 ) ;
#4500=DIRECTION ( 'NONE',  ( -1.000000000000000000, 1.010728034814421376E-30, 1.090846720500930387E-30 ) ) ;
#4501=DIRECTION ( 'NONE',  ( -1.000000000000000000, 1.010728034814421376E-30, 1.090846720500930387E-30 ) ) ;
#4503=EDGE_CURVE ( 'NONE', #4277, #11776, #1996, .T. ) ;
#4507=VERTEX_POINT ( 'NONE', #2237 ) ;
#4508=VERTEX_POINT ( 'NONE', #9170 ) ;
#4510=CIRCLE ( 'NONE', #10871, 2.800000000000004263 ) ;
#4511=CARTESIAN_POINT ( 'NONE',  ( 0.000000000000000000, 6.424561140605096199, -0.9808237102696265586 ) ) ;
#4516=CARTESIAN_POINT ( 'NONE',  ( 0.000000000000000000, -6.413745496774120092, 3.691052519622234129 ) ) ;
#4517=ORIENTED_EDGE ( 'NONE', *, *, #11869, .T. ) ;
#4518=DIRECTION ( 'NONE',  ( 0.000000000000000000, 0.7227948638273878901, 0.6910626489868685329 ) ) ;
#4519=DIRECTION ( 'NONE',  ( 8.135128085091670230E-31, 0.1785568947986370392, -0.9839295885986295565 ) ) ;
#4522=CIRCLE ( 'NONE', #6366, 7.400000000000009237 ) ;
#4524=AXIS2_PLACEMENT_3D ( 'NONE', #976, #5227, #8255 ) ;
#4525=AXIS2_PLACEMENT_3D ( 'NONE', #9335, #10561, #9522 ) ;
#4534=CIRCLE ( 'NONE', #2908, 7.400000000000009237 ) ;
#4537=DIRECTION ( 'NONE',  ( -1.000000000000000000, 1.010728034814421376E-30, 1.090846720500930387E-30 ) ) ;
#4539=FACE_OUTER_BOUND ( 'NONE', #7495, .T. ) ;
#4540=DIRECTION ( 'NONE',  ( 0.000000000000000000, 0.000000000000000000, 1.000000000000000000 ) ) ;
#4545=ORIENTED_EDGE ( 'NONE', *, *, #2074, .F. ) ;
#4546=ORIENTED_EDGE ( 'NONE', *, *, #4790, .F. ) ;
#4553=LINE ( 'NONE', #11380, #11841 ) ;
#4555=CARTESIAN_POINT ( 'NONE',  ( 0.000000000000000000, -1.113123845672418177, 7.315801754025009096 ) ) ;
#4559=EDGE_LOOP ( 'NONE', ( #1149, #10605, #6760, #9597 ) ) ;
#4561=EDGE_CURVE ( 'NONE', #7169, #4507, #4226, .T. ) ;
#4562=ADVANCED_FACE ( 'NONE', ( #10918 ), #3281, .T. ) ;
#4563=CARTESIAN_POINT ( 'NONE',  ( 19.99999999999997868, 2.796709610837448068, -6.851161606081828559 ) ) ;
#4564=ORIENTED_EDGE ( 'NONE', *, *, #5409, .T. ) ;
#4565=DIRECTION ( 'NONE',  ( -1.000000000000000000, 1.010728034814421376E-30, 1.090846720500930387E-30 ) ) ;
#4566=DIRECTION ( 'NONE',  ( -1.000000000000000000, 1.010728034814421376E-30, 1.090846720500930387E-30 ) ) ;
#4567=AXIS2_PLACEMENT_3D ( 'NONE', #5060, #11107, #6209 ) ;
#4569=FACE_OUTER_BOUND ( 'NONE', #11301, .T. ) ;
#4572=CIRCLE ( 'NONE', #247, 7.400000000000009237 ) ;
#4573=CARTESIAN_POINT ( 'NONE',  ( 0.000000000000000000, 0.000000000000000000, 0.000000000000000000 ) ) ;
#4575=AXIS2_PLACEMENT_3D ( 'NONE', #10891, #5997, #4977 ) ;
#4587=CARTESIAN_POINT ( 'NONE',  ( 0.000000000000000000, 6.359055127044389799, 1.682410996215986998 ) ) ;
#4589=CARTESIAN_POINT ( 'NONE',  ( 19.99999999999999645, 4.772487208025126826, 4.411390579991361527 ) ) ;
#4590=CIRCLE ( 'NONE', #10333, 2.800000000000004263 ) ;
#4591=DIRECTION ( 'NONE',  ( -1.000000000000000000, 1.010728034814421376E-30, 1.090846720500930387E-30 ) ) ;
#4592=VERTEX_POINT ( 'NONE', #11311 ) ;
#4595=CIRCLE ( 'NONE', #9509, 2.800000000000003819 ) ;
#4604=EDGE_LOOP ( 'NONE', ( #7254, #8728, #11317, #8154 ) ) ;
#4605=VECTOR ( 'NONE', #4795, 1000.000000000000000 ) ;
#4606=VERTEX_POINT ( 'NONE', #12285 ) ;
#4608=CARTESIAN_POINT ( 'NONE',  ( 19.99999999999999645, 2.796709610837343707, 6.851161606081852540 ) ) ;
#4609=CARTESIAN_POINT ( 'NONE',  ( 19.99999999999999645, -1.623118704078951202, 6.293050665016855838 ) ) ;
#4610=DIRECTION ( 'NONE',  ( 1.000000000000000000, -1.010728034814421376E-30, -1.090846720500930387E-30 ) ) ;
#4613=DIRECTION ( 'NONE',  ( -1.000000000000000000, 1.010728034814421376E-30, 1.090846720500930387E-30 ) ) ;
#4614=EDGE_CURVE ( 'NONE', #8175, #9475, #3588, .T. ) ;
#4615=DIRECTION ( 'NONE',  ( 0.000000000000000000, 0.9909497617679352555, -0.1342332658176522697 ) ) ;
#4620=ORIENTED_EDGE ( 'NONE', *, *, #5186, .T. ) ;
#4623=ORIENTED_EDGE ( 'NONE', *, *, #2051, .T. ) ;
#4625=CYLINDRICAL_SURFACE ( 'NONE', #5542, 2.800000000000003819 ) ;
#4626=VERTEX_POINT ( 'NONE', #4416 ) ;
#4628=DIRECTION ( 'NONE',  ( -1.000000000000000000, 1.010728034814421376E-30, 1.090846720500930387E-30 ) ) ;
#4631=AXIS2_PLACEMENT_3D ( 'NONE', #6502, #2781, #6632 ) ;
#4632=CARTESIAN_POINT ( 'NONE',  ( 19.99999999999999645, -4.907279493584762342, 4.380262188593320616 ) ) ;
#4633=EDGE_CURVE ( 'NONE', #8204, #11065, #11455, .T. ) ;
#4634=ORIENTED_EDGE ( 'NONE', *, *, #10414, .F. ) ;
#4635=ORIENTED_EDGE ( 'NONE', *, *, #11903, .T. ) ;
#4637=ADVANCED_FACE ( 'NONE', ( #6547 ), #2696, .T. ) ;
#4638=AXIS2_PLACEMENT_3D ( 'NONE', #7525, #440, #9314 ) ;
#4645=CARTESIAN_POINT ( 'NONE',  ( 0.000000000000000000, -2.720702104307052949, 5.902099716170440047 ) ) ;
#4649=FACE_OUTER_BOUND ( 'NONE', #1860, .T. ) ;
#4652=CARTESIAN_POINT ( 'NONE',  ( 19.99999999999997868, 6.359055127044406674, -1.682410996215896848 ) ) ;
#4654=CIRCLE ( 'NONE', #11027, 6.499000000000009436 ) ;
#4657=CARTESIAN_POINT ( 'NONE',  ( 0.000000000000000000, -2.099089055167725704, -6.233932467347810480 ) ) ;
#4658=CARTESIAN_POINT ( 'NONE',  ( 0.000000000000000000, -2.171317488608555557, 7.074275960383694439 ) ) ;
#4662=AXIS2_PLACEMENT_3D ( 'NONE', #10583, #3524, #11375 ) ;
#4664=ORIENTED_EDGE ( 'NONE', *, *, #2051, .F. ) ;
#4670=DIRECTION ( 'NONE',  ( 0.000000000000000000, 0.000000000000000000, 1.000000000000000000 ) ) ;
#4674=CARTESIAN_POINT ( 'NONE',  ( 19.99999999999999645, 0.000000000000000000, 0.000000000000000000 ) ) ;
#4676=VERTEX_POINT ( 'NONE', #8278 ) ;
#4678=ORIENTED_EDGE ( 'NONE', *, *, #3547, .F. ) ;
#4681=AXIS2_PLACEMENT_3D ( 'NONE', #3853, #2842, #9622 ) ;
#4683=EDGE_CURVE ( 'NONE', #5017, #9694, #8564, .T. ) ;
#4685=EDGE_CURVE ( 'NONE', #1261, #8686, #11378, .T. ) ;
#4686=VERTEX_POINT ( 'NONE', #6482 ) ;
#4695=FACE_OUTER_BOUND ( 'NONE', #7211, .T. ) ;
#4698=CARTESIAN_POINT ( 'NONE',  ( 0.000000000000000000, -4.707829255731254214, 5.709320773864518195 ) ) ;
#4699=VECTOR ( 'NONE', #10070, 1000.000000000000000 ) ;
#4701=EDGE_CURVE ( 'NONE', #5907, #1263, #674, .T. ) ;
#4703=CYLINDRICAL_SURFACE ( 'NONE', #3299, 2.800000000000003819 ) ;
#4704=ORIENTED_EDGE ( 'NONE', *, *, #5466, .F. ) ;
#4705=CIRCLE ( 'NONE', #11918, 7.400000000000009237 ) ;
#4711=EDGE_CURVE ( 'NONE', #3793, #7844, #5511, .T. ) ;
#4716=FACE_OUTER_BOUND ( 'NONE', #11379, .T. ) ;
#4717=AXIS2_PLACEMENT_3D ( 'NONE', #353, #8209, #9999 ) ;
#4718=DIRECTION ( 'NONE',  ( -1.000000000000000000, 1.010728034814421376E-30, 1.090846720500930387E-30 ) ) ;
#4719=CARTESIAN_POINT ( 'NONE',  ( 0.000000000000000000, -4.046291478462235247, 5.186098161460289901 ) ) ;
#4723=CIRCLE ( 'NONE', #9837, 2.800000000000002931 ) ;
#4724=STYLED_ITEM ( 'NONE', ( #7435 ), #10152 ) ;
#4725=CIRCLE ( 'NONE', #4525, 2.800000000000003819 ) ;
#4726=DIRECTION ( 'NONE',  ( -1.000000000000000000, 1.010728034814421376E-30, 1.090846720500930387E-30 ) ) ;
#4737=AXIS2_PLACEMENT_3D ( 'NONE', #7425, #11355, #9902 ) ;
#4738=DIRECTION ( 'NONE',  ( 1.140150527077241873E-30, 0.000000000000000000, -1.000000000000000000 ) ) ;
#4739=EDGE_LOOP ( 'NONE', ( #4953, #2895, #8457, #5258 ) ) ;
#4742=DIRECTION ( 'NONE',  ( -1.000000000000000000, 1.010728034814421376E-30, 1.090846720500930387E-30 ) ) ;
#4743=EDGE_LOOP ( 'NONE', ( #9923, #4756, #994, #2039 ) ) ;
#4744=ORIENTED_EDGE ( 'NONE', *, *, #375, .F. ) ;
#4745=CARTESIAN_POINT ( 'NONE',  ( -10.00000000000000178, 0.000000000000000000, 0.000000000000000000 ) ) ;
#4749=ORIENTED_EDGE ( 'NONE', *, *, #1695, .F. ) ;
#4750=CIRCLE ( 'NONE', #7988, 2.800000000000002931 ) ;
#4755=FACE_OUTER_BOUND ( 'NONE', #9257, .T. ) ;
#4756=ORIENTED_EDGE ( 'NONE', *, *, #6834, .T. ) ;
#4757=DIRECTION ( 'NONE',  ( -1.000000000000000000, 1.010728034814421376E-30, 1.090846720500930387E-30 ) ) ;
#4758=DIRECTION ( 'NONE',  ( 0.000000000000000000, 0.000000000000000000, 1.000000000000000000 ) ) ;
#4759=EDGE_CURVE ( 'NONE', #4162, #11649, #9779, .T. ) ;
#4761=VERTEX_POINT ( 'NONE', #1768 ) ;
#4763=ORIENTED_EDGE ( 'NONE', *, *, #10989, .F. ) ;
#4764=DIRECTION ( 'NONE',  ( -1.000000000000000000, 1.010728034814421376E-30, 1.090846720500930387E-30 ) ) ;
#4768=LINE ( 'NONE', #2173, #9612 ) ;
#4769=LINE ( 'NONE', #11852, #12245 ) ;
#4771=EDGE_CURVE ( 'NONE', #9801, #10601, #10835, .T. ) ;
#4780=DIRECTION ( 'NONE',  ( -1.000000000000000000, 1.010728034814421376E-30, 1.090846720500930387E-30 ) ) ;
#4781=DIRECTION ( 'NONE',  ( 4.314083075427402837E-32, -0.7227948638273978821, 0.6910626489868579858 ) ) ;
#4785=DIRECTION ( 'NONE',  ( -1.000000000000000000, 1.010728034814421376E-30, 1.090846720500930387E-30 ) ) ;
#4787=EDGE_CURVE ( 'NONE', #11478, #10207, #12488, .T. ) ;
#4789=DIRECTION ( 'NONE',  ( 0.000000000000000000, -0.9989930665413151445, 0.04486483035050449486 ) ) ;
#4790=EDGE_CURVE ( 'NONE', #11957, #9234, #12065, .T. ) ;
#4791=CIRCLE ( 'NONE', #12622, 7.400000000000011902 ) ;
#4793=VERTEX_POINT ( 'NONE', #11686 ) ;
#4795=DIRECTION ( 'NONE',  ( -1.000000000000000000, 1.010728034814421376E-30, 1.090846720500930387E-30 ) ) ;
#4797=CARTESIAN_POINT ( 'NONE',  ( 19.99999999999999645, 0.000000000000000000, 0.000000000000000000 ) ) ;
#4799=DIRECTION ( 'NONE',  ( -1.000000000000000000, 1.010728034814421376E-30, 1.090846720500930387E-30 ) ) ;
#4800=ORIENTED_EDGE ( 'NONE', *, *, #11315, .T. ) ;
#4802=CYLINDRICAL_SURFACE ( 'NONE', #5355, 2.800000000000003819 ) ;
#4805=ORIENTED_EDGE ( 'NONE', *, *, #5727, .F. ) ;
#4809=CARTESIAN_POINT ( 'NONE',  ( 0.000000000000000000, 0.2110513566293374665, 7.396989747516548697 ) ) ;
#4811=DIRECTION ( 'NONE',  ( 0.000000000000000000, 0.000000000000000000, 1.000000000000000000 ) ) ;
#4812=DIRECTION ( 'NONE',  ( -1.000000000000000000, 1.010728034814421376E-30, 1.090846720500930387E-30 ) ) ;
#4816=CARTESIAN_POINT ( 'NONE',  ( 19.99999999999999645, 3.565124043461683101, 5.527927226701645935 ) ) ;
#4817=AXIS2_PLACEMENT_3D ( 'NONE', #6600, #1692, #11363 ) ;
#4818=ORIENTED_EDGE ( 'NONE', *, *, #11619, .F. ) ;
#4819=ORIENTED_EDGE ( 'NONE', *, *, #9496, .T. ) ;
#4823=ORIENTED_EDGE ( 'NONE', *, *, #1451, .T. ) ;
#4826=ORIENTED_EDGE ( 'NONE', *, *, #6419, .T. ) ;
#4827=VECTOR ( 'NONE', #5285, 1000.000000000000000 ) ;
#4829=CARTESIAN_POINT ( 'NONE',  ( 19.99999999999997868, -2.385831757338501724, -6.045230171438906730 ) ) ;
#4830=LINE ( 'NONE', #2923, #11424 ) ;
#4831=DIRECTION ( 'NONE',  ( 1.000000000000000000, -1.010728034814421376E-30, -1.090846720500930387E-30 ) ) ;
#4832=ORIENTED_EDGE ( 'NONE', *, *, #5499, .F. ) ;
#4833=DIRECTION ( 'NONE',  ( -1.000000000000000000, 1.010728034814421376E-30, 1.090846720500930387E-30 ) ) ;
#4840=EDGE_CURVE ( 'NONE', #8271, #3837, #6862, .T. ) ;
#4842=CARTESIAN_POINT ( 'NONE',  ( 19.99999999999997868, 6.544726022087268724, -0.6592800351836389794 ) ) ;
#4845=CARTESIAN_POINT ( 'NONE',  ( 0.000000000000000000, 1.531833341630221224, -6.396997380212695816 ) ) ;
#4846=DIRECTION ( 'NONE',  ( -1.000000000000000000, 1.010728034814421376E-30, 1.090846720500930387E-30 ) ) ;
#4861=EDGE_CURVE ( 'NONE', #9789, #477, #11862, .T. ) ;
#4864=EDGE_LOOP ( 'NONE', ( #620, #12229, #7498, #4623 ) ) ;
#4866=ORIENTED_EDGE ( 'NONE', *, *, #3972, .F. ) ;
#4867=CARTESIAN_POINT ( 'NONE',  ( 19.99999999999999645, 0.000000000000000000, 0.000000000000000000 ) ) ;
#4868=ORIENTED_EDGE ( 'NONE', *, *, #1847, .T. ) ;
#4869=ORIENTED_EDGE ( 'NONE', *, *, #6913, .T. ) ;
#4875=CARTESIAN_POINT ( 'NONE',  ( 19.99999999999997868, 0.3649881613860929686, -6.567714405409704526 ) ) ;
#4878=DIRECTION ( 'NONE',  ( -1.000000000000000000, 1.010728034814421376E-30, 1.090846720500930387E-30 ) ) ;
#4881=PRODUCT_DEFINITION_CONTEXT ( 'detailed design', #826, 'design' ) ;
#4885=VERTEX_POINT ( 'NONE', #8841 ) ;
#4886=VECTOR ( 'NONE', #9091, 1000.000000000000000 ) ;
#4888=VERTEX_POINT ( 'NONE', #5819 ) ;
#4893=VECTOR ( 'NONE', #168, 1000.000000000000000 ) ;
#4894=EDGE_CURVE ( 'NONE', #8701, #9489, #5683, .T. ) ;
#4895=EDGE_CURVE ( 'NONE', #9520, #8041, #5479, .T. ) ;
#4896=DIRECTION ( 'NONE',  ( -1.000000000000000000, 1.010728034814421376E-30, 1.090846720500930387E-30 ) ) ;
#4902=CARTESIAN_POINT ( 'NONE',  ( 19.99999999999997868, 1.834336845376804748, -6.234758161925229913 ) ) ;
#4905=CARTESIAN_POINT ( 'NONE',  ( 0.000000000000000000, -2.385831757338585657, 6.045230171438855216 ) ) ;
#4906=CYLINDRICAL_SURFACE ( 'NONE', #5488, 2.800000000000003819 ) ;
#4909=DIRECTION ( 'NONE',  ( -1.000000000000000000, 1.010728034814421376E-30, 1.090846720500930387E-30 ) ) ;
#4910=EDGE_CURVE ( 'NONE', #6552, #4118, #9575, .T. ) ;
#4912=CARTESIAN_POINT ( 'NONE',  ( 19.99999999999999645, 5.914787828628542243, 4.446941076999763709 ) ) ;
#4913=ADVANCED_FACE ( 'NONE', ( #7112 ), #4142, .T. ) ;
#4914=EDGE_CURVE ( 'NONE', #9071, #9362, #130, .T. ) ;
#4916=EDGE_LOOP ( 'NONE', ( #9056, #4274, #12454, #8127 ) ) ;
#4917=DIRECTION ( 'NONE',  ( 0.000000000000000000, 0.000000000000000000, 1.000000000000000000 ) ) ;
#4919=CARTESIAN_POINT ( 'NONE',  ( 19.99999999999997868, 0.2110513566294510979, -7.396989747516558467 ) ) ;
#4923=DIRECTION ( 'NONE',  ( -1.000000000000000000, 1.010728034814421376E-30, 1.090846720500930387E-30 ) ) ;
#4925=CIRCLE ( 'NONE', #10471, 6.499000000000008548 ) ;
#4930=ORIENTED_EDGE ( 'NONE', *, *, #8076, .T. ) ;
#4932=ORIENTED_EDGE ( 'NONE', *, *, #5025, .F. ) ;
#4940=EDGE_CURVE ( 'NONE', #3717, #3737, #7132, .T. ) ;
#4942=EDGE_CURVE ( 'NONE', #7374, #3414, #86, .T. ) ;
#4943=ORIENTED_EDGE ( 'NONE', *, *, #4957, .F. ) ;
#4945=CYLINDRICAL_SURFACE ( 'NONE', #2798, 7.400000000000010125 ) ;
#4946=AXIS2_PLACEMENT_3D ( 'NONE', #10284, #8486, #4374 ) ;
#4951=VERTEX_POINT ( 'NONE', #1302 ) ;
#4952=EDGE_CURVE ( 'NONE', #6148, #11828, #6101, .T. ) ;
#4953=ORIENTED_EDGE ( 'NONE', *, *, #10787, .T. ) ;
#4954=EDGE_CURVE ( 'NONE', #2575, #3892, #1168, .T. ) ;
#4956=ORIENTED_EDGE ( 'NONE', *, *, #3275, .F. ) ;
#4957=EDGE_CURVE ( 'NONE', #8459, #3414, #8980, .T. ) ;
#4966=ORIENTED_EDGE ( 'NONE', *, *, #1451, .F. ) ;
#4967=CARTESIAN_POINT ( 'NONE',  ( 19.99999999999999645, 0.000000000000000000, 0.000000000000000000 ) ) ;
#4968=( NAMED_UNIT ( * ) PLANE_ANGLE_UNIT ( ) SI_UNIT ( $, .RADIAN. ) );
#4969=EDGE_CURVE ( 'NONE', #5919, #9871, #3857, .T. ) ;
#4970=DIRECTION ( 'NONE',  ( 9.367723249499501176E-31, -0.9989930665413151445, 0.04486483035050449486 ) ) ;
#4972=LINE ( 'NONE', #12647, #6537 ) ;
#4976=CARTESIAN_POINT ( 'NONE',  ( 19.99999999999997868, 5.483475578891663815, -3.488337222187519515 ) ) ;
#4977=DIRECTION ( 'NONE',  ( 0.000000000000000000, 0.000000000000000000, 1.000000000000000000 ) ) ;
#4979=ORIENTED_EDGE ( 'NONE', *, *, #11606, .F. ) ;
#4982=CYLINDRICAL_SURFACE ( 'NONE', #9376, 6.499000000000010324 ) ;
#4983=LINE ( 'NONE', #2881, #9822 ) ;
#4986=ORIENTED_EDGE ( 'NONE', *, *, #1422, .F. ) ;
#4988=AXIS2_PLACEMENT_3D ( 'NONE', #10624, #11666, #776 ) ;
#4993=FACE_OUTER_BOUND ( 'NONE', #11562, .T. ) ;
#4995=ORIENTED_EDGE ( 'NONE', *, *, #9015, .T. ) ;
#4997=CLOSED_SHELL ( 'NONE', ( #3021, #11005, #6157, #1816, #9265, #2972, #6415, #909, #11158, #6269, #10783, #9884, #12340, #4397, #1234, #432, #6352, #5176, #8655, #9938, #3314, #1997, #1802, #2764, #9967, #2813, #6792, #3895, #2753, #11336, #3770, #10025, #12592, #7516, #10204, #1684, #11047, #4562, #6249, #11998, #8504, #2525, #9148, #2452, #12069, #9451, #9227, #6813, #5730, #3416, #9301, #7304, #2102, #12383, #11, #1448, #3165, #11590, #7777, #1519, #1211, #504, #6389, #6442, #3982, #6493, #184, #7238, #7080, #3231, #4158, #1059, #3224, #2114, #7929, #4637, #4233, #9529, #12273, #8843, #3308, #12121, #11769, #11044, #9950, #6230, #2708, #3723, #4391, #10606, #9725, #7995, #6010, #11211, #4124, #2459, #4034, #462, #7146, #513, #5253, #11744, #3034, #1084, #2589, #2649, #10804, #5390, #9798, #5482, #3687, #2116, #5015, #8091, #27, #10489, #4913, #8487, #10796, #3204, #8207, #12681, #11167, #10283, #7015, #8043, #1771, #732, #7149, #6695, #6676, #2243, #2221, #2922, #7393, #1939, #3761, #109, #10911, #6120, #8485, #10826, #4064, #12113, #1726, #2320, #7126, #9564 ) ) ;
#4998=VECTOR ( 'NONE', #114, 1000.000000000000000 ) ;
#4999=CYLINDRICAL_SURFACE ( 'NONE', #9030, 2.800000000000003819 ) ;
#5002=CARTESIAN_POINT ( 'NONE',  ( 19.99999999999999645, 0.000000000000000000, 0.000000000000000000 ) ) ;
#5003=EDGE_CURVE ( 'NONE', #6740, #3160, #12295, .T. ) ;
#5004=ORIENTED_EDGE ( 'NONE', *, *, #2224, .T. ) ;
#5006=LINE ( 'NONE', #105, #3618 ) ;
#5009=EDGE_LOOP ( 'NONE', ( #5851, #9289, #10683, #2178 ) ) ;
#5010=ORIENTED_EDGE ( 'NONE', *, *, #9031, .F. ) ;
#5012=VECTOR ( 'NONE', #9339, 1000.000000000000000 ) ;
#5015=ADVANCED_FACE ( 'NONE', ( #11098 ), #275, .T. ) ;
#5017=VERTEX_POINT ( 'NONE', #339 ) ;
#5022=AXIS2_PLACEMENT_3D ( 'NONE', #11610, #2803, #1811 ) ;
#5023=FACE_OUTER_BOUND ( 'NONE', #1650, .T. ) ;
#5025=EDGE_CURVE ( 'NONE', #8204, #2582, #2350, .T. ) ;
#5030=PRESENTATION_STYLE_ASSIGNMENT (( #10030 ) ) ;
#5032=LINE ( 'NONE', #129, #2054 ) ;
#5038=AXIS2_PLACEMENT_3D ( 'NONE', #8171, #1151, #9958 ) ;
#5042=CARTESIAN_POINT ( 'NONE',  ( 0.000000000000000000, -5.651611091574772594, -4.776954267060654402 ) ) ;
#5045=ORIENTED_EDGE ( 'NONE', *, *, #3391, .F. ) ;
#5054=LINE ( 'NONE', #2885, #920 ) ;
#5060=CARTESIAN_POINT ( 'NONE',  ( 19.99999999999999645, 0.000000000000000000, 0.000000000000000000 ) ) ;
#5062=ORIENTED_EDGE ( 'NONE', *, *, #1913, .T. ) ;
#5065=ORIENTED_EDGE ( 'NONE', *, *, #5148, .F. ) ;
#5067=DIRECTION ( 'NONE',  ( -1.000000000000000000, 1.010728034814421376E-30, 1.090846720500930387E-30 ) ) ;
#5070=CARTESIAN_POINT ( 'NONE',  ( 0.000000000000000000, 0.000000000000000000, 0.000000000000000000 ) ) ;
#5073=VERTEX_POINT ( 'NONE', #5559 ) ;
#5075=EDGE_CURVE ( 'NONE', #2162, #4279, #343, .T. ) ;
#5076=ORIENTED_EDGE ( 'NONE', *, *, #4942, .T. ) ;
#5080=AXIS2_PLACEMENT_3D ( 'NONE', #2014, #12664, #3831 ) ;
#5081=DIRECTION ( 'NONE',  ( 1.000000000000000000, -1.010728034814421376E-30, -1.090846720500930387E-30 ) ) ;
#5082=DIRECTION ( 'NONE',  ( -1.000000000000000000, 1.010728034814421376E-30, 1.090846720500930387E-30 ) ) ;
#5086=CARTESIAN_POINT ( 'NONE',  ( 19.99999999999999645, 3.681899619563770543, 5.450844343808956438 ) ) ;
#5088=AXIS2_PLACEMENT_3D ( 'NONE', #4842, #8886, #8768 ) ;
#5089=DIRECTION ( 'NONE',  ( -1.140150527077241873E-30, 0.000000000000000000, 1.000000000000000000 ) ) ;
#5090=DIRECTION ( 'NONE',  ( 1.000000000000000000, -1.010728034814421376E-30, -1.090846720500930387E-30 ) ) ;
#5091=ORIENTED_EDGE ( 'NONE', *, *, #3112, .T. ) ;
#5092=CARTESIAN_POINT ( 'NONE',  ( 19.99999999999999645, -6.182645281642508372, 2.245659411033100294 ) ) ;
#5093=ORIENTED_EDGE ( 'NONE', *, *, #6520, .T. ) ;
#5094=FACE_OUTER_BOUND ( 'NONE', #5760, .T. ) ;
#5096=CARTESIAN_POINT ( 'NONE',  ( 19.99999999999999645, -3.178467454237171363, 5.758943784352557493 ) ) ;
#5101=CARTESIAN_POINT ( 'NONE',  ( 0.000000000000000000, -5.610543508060457540, 3.433640984893238102 ) ) ;
#5104=CARTESIAN_POINT ( 'NONE',  ( 0.000000000000000000, 5.280167904461722905, 3.922743398397384063 ) ) ;
#5107=DIRECTION ( 'NONE',  ( -1.000000000000000000, 1.010728034814421376E-30, 1.090846720500930387E-30 ) ) ;
#5110=DIRECTION ( 'NONE',  ( 0.000000000000000000, 0.000000000000000000, 1.000000000000000000 ) ) ;
#5112=CARTESIAN_POINT ( 'NONE',  ( 19.99999999999999645, 2.649444137877595473, 6.020675595748703479 ) ) ;
#5114=DIRECTION ( 'NONE',  ( -1.000000000000000000, 1.010728034814421376E-30, 1.090846720500930387E-30 ) ) ;
#5115=CARTESIAN_POINT ( 'NONE',  ( 0.000000000000000000, -5.492355906873426008, 4.959236492871922586 ) ) ;
#5117=VERTEX_POINT ( 'NONE', #12266 ) ;
#5120=ORIENTED_EDGE ( 'NONE', *, *, #12015, .F. ) ;
#5126=DIRECTION ( 'NONE',  ( -1.000000000000000000, 1.010728034814421376E-30, 1.090846720500930387E-30 ) ) ;
#5127=VERTEX_POINT ( 'NONE', #8388 ) ;
#5129=AXIS2_PLACEMENT_3D ( 'NONE', #7728, #11596, #1788 ) ;
#5135=ORIENTED_EDGE ( 'NONE', *, *, #1446, .F. ) ;
#5136=ORIENTED_EDGE ( 'NONE', *, *, #7236, .T. ) ;
#5137=ORIENTED_EDGE ( 'NONE', *, *, #9484, .T. ) ;
#5138=AXIS2_PLACEMENT_3D ( 'NONE', #4116, #1341, #10937 ) ;
#5140=VECTOR ( 'NONE', #1246, 1000.000000000000000 ) ;
#5143=CARTESIAN_POINT ( 'NONE',  ( 19.99999999999999645, 4.772487208025126826, 4.411390579991361527 ) ) ;
#5144=VERTEX_POINT ( 'NONE', #11231 ) ;
#5146=ORIENTED_EDGE ( 'NONE', *, *, #11395, .F. ) ;
#5147=CARTESIAN_POINT ( 'NONE',  ( 19.99999999999999645, 0.000000000000000000, 0.000000000000000000 ) ) ;
#5148=EDGE_CURVE ( 'NONE', #7570, #11547, #956, .T. ) ;
#5149=CIRCLE ( 'NONE', #2490, 7.400000000000011902 ) ;
#5150=EDGE_CURVE ( 'NONE', #701, #1466, #1367, .T. ) ;
#5151=AXIS2_PLACEMENT_3D ( 'NONE', #6456, #1550, #9580 ) ;
#5152=VECTOR ( 'NONE', #3309, 1000.000000000000000 ) ;
#5153=CARTESIAN_POINT ( 'NONE',  ( 0.000000000000000000, -5.932103089875957025, 2.654647609586676005 ) ) ;
#5161=( NAMED_UNIT ( * ) SI_UNIT ( $, .STERADIAN. ) SOLID_ANGLE_UNIT ( ) );
#5165=CARTESIAN_POINT ( 'NONE',  ( 0.000000000000000000, 6.359534927042314045, 1.339147681075194996 ) ) ;
#5171=AXIS2_PLACEMENT_3D ( 'NONE', #12464, #8585, #2684 ) ;
#5173=CARTESIAN_POINT ( 'NONE',  ( 0.000000000000000000, -2.401522331692917511, 6.999477872697379865 ) ) ;
#5175=LINE ( 'NONE', #12007, #4886 ) ;
#5176=ADVANCED_FACE ( 'NONE', ( #403 ), #4334, .T. ) ;
#5178=ORIENTED_EDGE ( 'NONE', *, *, #5856, .F. ) ;
#5181=CIRCLE ( 'NONE', #1470, 7.400000000000011902 ) ;
#5182=CARTESIAN_POINT ( 'NONE',  ( 19.99999999999999645, -4.999339924971525129, -4.274890546384038537 ) ) ;
#5184=VECTOR ( 'NONE', #5418, 1000.000000000000000 ) ;
#5185=ORIENTED_EDGE ( 'NONE', *, *, #11482, .T. ) ;
#5186=EDGE_CURVE ( 'NONE', #3305, #2119, #3648, .T. ) ;
#5187=DIRECTION ( 'NONE',  ( -1.000000000000000000, 1.010728034814421376E-30, 1.090846720500930387E-30 ) ) ;
#5190=DIRECTION ( 'NONE',  ( 1.000000000000000000, -1.010728034814421376E-30, -1.090846720500930387E-30 ) ) ;
#5191=ORIENTED_EDGE ( 'NONE', *, *, #1757, .T. ) ;
#5194=CIRCLE ( 'NONE', #3361, 7.400000000000011902 ) ;
#5197=DIRECTION ( 'NONE',  ( -1.000000000000000000, 1.010728034814421376E-30, 1.090846720500930387E-30 ) ) ;
#5198=CARTESIAN_POINT ( 'NONE',  ( 19.99999999999999645, 2.520781513113643513, 6.075668640744193105 ) ) ;
#5207=ORIENTED_EDGE ( 'NONE', *, *, #11737, .F. ) ;
#5210=CIRCLE ( 'NONE', #9102, 7.400000000000011902 ) ;
#5211=CYLINDRICAL_SURFACE ( 'NONE', #5433, 2.800000000000003819 ) ;
#5213=CARTESIAN_POINT ( 'NONE',  ( 0.000000000000000000, -5.362766118793832248, -3.671204237728701969 ) ) ;
#5216=CARTESIAN_POINT ( 'NONE',  ( 19.99999999999999645, -4.357840574720623472, 4.821434073521965402 ) ) ;
#5218=CARTESIAN_POINT ( 'NONE',  ( 19.99999999999997868, 1.834336845376804748, -6.234758161925229913 ) ) ;
#5219=EDGE_CURVE ( 'NONE', #1374, #9285, #3847, .T. ) ;
#5223=CIRCLE ( 'NONE', #3591, 7.400000000000011902 ) ;
#5226=LINE ( 'NONE', #5286, #8414 ) ;
#5227=DIRECTION ( 'NONE',  ( -1.000000000000000000, 1.010728034814421376E-30, 1.090846720500930387E-30 ) ) ;
#5228=CIRCLE ( 'NONE', #4199, 2.800000000000003819 ) ;
#5229=CARTESIAN_POINT ( 'NONE',  ( 19.99999999999999645, -5.362766118793865111, 3.671204237728611819 ) ) ;
#5232=EDGE_CURVE ( 'NONE', #11765, #6098, #9585, .T. ) ;
#5238=CIRCLE ( 'NONE', #1745, 7.400000000000011902 ) ;
#5239=CARTESIAN_POINT ( 'NONE',  ( 19.99999999999997868, -2.099089055167727480, -6.233932467347804263 ) ) ;
#5240=LINE ( 'NONE', #10238, #7707 ) ;
#5242=ORIENTED_EDGE ( 'NONE', *, *, #8637, .F. ) ;
#5245=CIRCLE ( 'NONE', #3615, 6.499000000000009436 ) ;
#5246=ORIENTED_EDGE ( 'NONE', *, *, #10436, .T. ) ;
#5248=ORIENTED_EDGE ( 'NONE', *, *, #2724, .F. ) ;
#5252=CARTESIAN_POINT ( 'NONE',  ( 0.000000000000000000, 0.000000000000000000, 0.000000000000000000 ) ) ;
#5253=ADVANCED_FACE ( 'NONE', ( #8647 ), #4906, .T. ) ;
#5257=VERTEX_POINT ( 'NONE', #1879 ) ;
#5258=ORIENTED_EDGE ( 'NONE', *, *, #368, .T. ) ;
#5259=ORIENTED_EDGE ( 'NONE', *, *, #9720, .F. ) ;
#5264=ORIENTED_EDGE ( 'NONE', *, *, #6419, .F. ) ;
#5268=ORIENTED_EDGE ( 'NONE', *, *, #2120, .T. ) ;
#5272=VECTOR ( 'NONE', #11503, 1000.000000000000000 ) ;
#5275=ORIENTED_EDGE ( 'NONE', *, *, #12168, .F. ) ;
#5280=VECTOR ( 'NONE', #7864, 1000.000000000000000 ) ;
#5282=CIRCLE ( 'NONE', #1369, 2.800000000000003819 ) ;
#5284=CARTESIAN_POINT ( 'NONE',  ( 0.000000000000000000, 3.975087478966741639, -6.241688836730176604 ) ) ;
#5285=DIRECTION ( 'NONE',  ( -1.000000000000000000, 1.010728034814421376E-30, 1.090846720500930387E-30 ) ) ;
#5286=CARTESIAN_POINT ( 'NONE',  ( 9.999999999999998224, 7.358375340957004518, -0.7837807994560894720 ) ) ;
#5287=ORIENTED_EDGE ( 'NONE', *, *, #603, .F. ) ;
#5289=CARTESIAN_POINT ( 'NONE',  ( 0.000000000000000000, 6.557268578288196537, 0.5199208220222142351 ) ) ;
#5290=AXIS2_PLACEMENT_3D ( 'NONE', #5928, #9970, #9141 ) ;
#5292=CARTESIAN_POINT ( 'NONE',  ( 0.000000000000000000, 6.718789039999951029, 3.101269713516811688 ) ) ;
#5293=EDGE_CURVE ( 'NONE', #1397, #8559, #12711, .T. ) ;
#5294=ORIENTED_EDGE ( 'NONE', *, *, #1838, .F. ) ;
#5295=CARTESIAN_POINT ( 'NONE',  ( 19.99999999999999645, -3.399584271718382844, 6.572885726945580487 ) ) ;
#5303=SURFACE_STYLE_FILL_AREA ( #1371 ) ;
#5306=ORIENTED_EDGE ( 'NONE', *, *, #4448, .F. ) ;
#5307=EDGE_LOOP ( 'NONE', ( #7877, #10476, #9366, #2913 ) ) ;
#5313=FACE_OUTER_BOUND ( 'NONE', #4323, .T. ) ;
#5314=CARTESIAN_POINT ( 'NONE',  ( 19.99999999999997868, 6.424561140605085541, 0.9808237102697028309 ) ) ;
#5315=ORIENTED_EDGE ( 'NONE', *, *, #8229, .T. ) ;
#5316=DIRECTION ( 'NONE',  ( -1.000000000000000000, 1.010728034814421376E-30, 1.090846720500930387E-30 ) ) ;
#5317=EDGE_CURVE ( 'NONE', #9583, #2582, #6733, .T. ) ;
#5330=ORIENTED_EDGE ( 'NONE', *, *, #2666, .F. ) ;
#5334=DIRECTION ( 'NONE',  ( 1.140150527077241698E-30, 0.000000000000000000, -1.000000000000000000 ) ) ;
#5336=AXIS2_PLACEMENT_3D ( 'NONE', #9785, #11934, #914 ) ;
#5341=CIRCLE ( 'NONE', #11314, 2.800000000000003375 ) ;
#5342=ORIENTED_EDGE ( 'NONE', *, *, #9702, .F. ) ;
#5345=DIRECTION ( 'NONE',  ( 0.000000000000000000, 0.000000000000000000, 1.000000000000000000 ) ) ;
#5347=CIRCLE ( 'NONE', #820, 6.499000000000006771 ) ;
#5349=LINE ( 'NONE', #5478, #3835 ) ;
#5351=DIRECTION ( 'NONE',  ( 0.000000000000000000, 0.000000000000000000, 1.000000000000000000 ) ) ;
#5355=AXIS2_PLACEMENT_3D ( 'NONE', #932, #4742, #12669 ) ;
#5360=CYLINDRICAL_SURFACE ( 'NONE', #3382, 2.800000000000003819 ) ;
#5364=DIRECTION ( 'NONE',  ( 0.000000000000000000, -0.7818314824680222541, -0.6234898018587429203 ) ) ;
#5369=VERTEX_POINT ( 'NONE', #5165 ) ;
#5371=ORIENTED_EDGE ( 'NONE', *, *, #4230, .T. ) ;
#5372=EDGE_CURVE ( 'NONE', #11663, #11879, #12086, .T. ) ;
#5373=ORIENTED_EDGE ( 'NONE', *, *, #4614, .T. ) ;
#5375=DIRECTION ( 'NONE',  ( -1.140150527077241873E-30, 0.000000000000000000, 1.000000000000000000 ) ) ;
#5378=AXIS2_PLACEMENT_3D ( 'NONE', #8707, #778, #2802 ) ;
#5380=ORIENTED_EDGE ( 'NONE', *, *, #1749, .T. ) ;
#5385=ORIENTED_EDGE ( 'NONE', *, *, #3310, .F. ) ;
#5386=ORIENTED_EDGE ( 'NONE', *, *, #3942, .F. ) ;
#5387=ORIENTED_EDGE ( 'NONE', *, *, #5468, .T. ) ;
#5388=FACE_OUTER_BOUND ( 'NONE', #6348, .T. ) ;
#5389=VECTOR ( 'NONE', #9457, 1000.000000000000000 ) ;
#5390=ADVANCED_FACE ( 'NONE', ( #2136 ), #327, .T. ) ;
#5396=CARTESIAN_POINT ( 'NONE',  ( 19.99999999999997868, 5.956456411769428527, -2.790827096698922372 ) ) ;
#5398=EDGE_CURVE ( 'NONE', #4508, #10621, #1098, .T. ) ;
#5400=AXIS2_PLACEMENT_3D ( 'NONE', #12566, #2853, #1602 ) ;
#5401=DIRECTION ( 'NONE',  ( -1.000000000000000000, 1.010728034814421376E-30, 1.090846720500930387E-30 ) ) ;
#5402=ORIENTED_EDGE ( 'NONE', *, *, #7036, .F. ) ;
#5407=LINE ( 'NONE', #9512, #2887 ) ;
#5408=AXIS2_PLACEMENT_3D ( 'NONE', #8288, #3350, #7332 ) ;
#5409=EDGE_CURVE ( 'NONE', #2245, #9520, #8168, .T. ) ;
#5410=DIRECTION ( 'NONE',  ( -1.000000000000000000, 1.010728034814421376E-30, 1.090846720500930387E-30 ) ) ;
#5411=DIRECTION ( 'NONE',  ( 1.000000000000000000, -1.010728034814421376E-30, -1.090846720500930387E-30 ) ) ;
#5413=CARTESIAN_POINT ( 'NONE',  ( 0.000000000000000000, 0.000000000000000000, 0.000000000000000000 ) ) ;
#5416=VERTEX_POINT ( 'NONE', #9906 ) ;
#5418=DIRECTION ( 'NONE',  ( 1.000000000000000000, -1.010728034814421376E-30, -1.090846720500930387E-30 ) ) ;
#5422=AXIS2_PLACEMENT_3D ( 'NONE', #6530, #401, #4398 ) ;
#5424=DIRECTION ( 'NONE',  ( -1.000000000000000000, 1.010728034814421376E-30, 1.090846720500930387E-30 ) ) ;
#5425=CARTESIAN_POINT ( 'NONE',  ( 19.99999999999999645, -5.148708580507705967, 3.965829163366258570 ) ) ;
#5426=FACE_OUTER_BOUND ( 'NONE', #10558, .T. ) ;
#5433=AXIS2_PLACEMENT_3D ( 'NONE', #12110, #9127, #9189 ) ;
#5448=CARTESIAN_POINT ( 'NONE',  ( 19.99999999999999645, 0.000000000000000000, 0.000000000000000000 ) ) ;
#5449=DIRECTION ( 'NONE',  ( 0.000000000000000000, 0.000000000000000000, 1.000000000000000000 ) ) ;
#5450=ORIENTED_EDGE ( 'NONE', *, *, #8947, .F. ) ;
#5453=ORIENTED_EDGE ( 'NONE', *, *, #11184, .T. ) ;
#5455=VERTEX_POINT ( 'NONE', #2396 ) ;
#5458=ORIENTED_EDGE ( 'NONE', *, *, #9702, .T. ) ;
#5460=CARTESIAN_POINT ( 'NONE',  ( 9.999999999999994671, 0.2110513566293444054, 7.396989747516548697 ) ) ;
#5461=ORIENTED_EDGE ( 'NONE', *, *, #7308, .F. ) ;
#5462=CIRCLE ( 'NONE', #12671, 6.499000000000008548 ) ;
#5463=AXIS2_PLACEMENT_3D ( 'NONE', #5239, #7114, #4144 ) ;
#5464=FACE_OUTER_BOUND ( 'NONE', #11198, .T. ) ;
#5465=CARTESIAN_POINT ( 'NONE',  ( 0.000000000000000000, 3.908107171477168684, 5.192658214849952714 ) ) ;
#5466=EDGE_CURVE ( 'NONE', #3837, #7377, #10833, .T. ) ;
#5467=DIRECTION ( 'NONE',  ( 1.000000000000000000, -1.010728034814421376E-30, -1.090846720500930387E-30 ) ) ;
#5468=EDGE_CURVE ( 'NONE', #11828, #7505, #3492, .T. ) ;
#5475=DIRECTION ( 'NONE',  ( -1.000000000000000000, 1.010728034814421376E-30, 1.090846720500930387E-30 ) ) ;
#5476=DIRECTION ( 'NONE',  ( 0.000000000000000000, 0.4338837391175525693, 0.9009688679024219216 ) ) ;
#5478=CARTESIAN_POINT ( 'NONE',  ( 50.00005079999998969, 5.204170427930421283E-15, 2.499999999999996447 ) ) ;
#5479=CIRCLE ( 'NONE', #2407, 7.400000000000011902 ) ;
#5481=DIRECTION ( 'NONE',  ( -1.000000000000000000, 1.010728034814421376E-30, 1.090846720500930387E-30 ) ) ;
#5482=ADVANCED_FACE ( 'NONE', ( #9326 ), #2462, .T. ) ;
#5486=LINE ( 'NONE', #5229, #10098 ) ;
#5488=AXIS2_PLACEMENT_3D ( 'NONE', #5870, #2744, #9591 ) ;
#5490=VECTOR ( 'NONE', #11117, 1000.000000000000000 ) ;
#5491=CARTESIAN_POINT ( 'NONE',  ( 19.99999999999997868, 3.681899619563859360, -5.450844343808918246 ) ) ;
#5492=VERTEX_POINT ( 'NONE', #2530 ) ;
#5494=CARTESIAN_POINT ( 'NONE',  ( 19.99999999999997868, 5.670261409740700920, -3.175710400084609475 ) ) ;
#5495=DIRECTION ( 'NONE',  ( 0.000000000000000000, -0.5877852522924802425, 0.8090169943749421222 ) ) ;
#5498=AXIS2_PLACEMENT_3D ( 'NONE', #11345, #9203, #12190 ) ;
#5499=EDGE_CURVE ( 'NONE', #10207, #11698, #542, .T. ) ;
#5502=EDGE_CURVE ( 'NONE', #2096, #7387, #5349, .T. ) ;
#5504=VERTEX_POINT ( 'NONE', #10292 ) ;
#5508=DIRECTION ( 'NONE',  ( 1.140150527077241873E-30, 0.000000000000000000, -1.000000000000000000 ) ) ;
#5511=LINE ( 'NONE', #612, #5272 ) ;
#5512=ORIENTED_EDGE ( 'NONE', *, *, #3146, .F. ) ;
#5515=VERTEX_POINT ( 'NONE', #5284 ) ;
#5516=EDGE_LOOP ( 'NONE', ( #4869, #8479, #5264, #1537 ) ) ;
#5523=VERTEX_POINT ( 'NONE', #8310 ) ;
#5527=DIRECTION ( 'NONE',  ( -1.000000000000000000, 1.010728034814421376E-30, 1.090846720500930387E-30 ) ) ;
#5529=AXIS2_PLACEMENT_3D ( 'NONE', #9981, #2775, #1591 ) ;
#5533=AXIS2_PLACEMENT_3D ( 'NONE', #4867, #3838, #936 ) ;
#5539=DIRECTION ( 'NONE',  ( -1.000000000000000000, 1.010728034814421376E-30, 1.090846720500930387E-30 ) ) ;
#5542=AXIS2_PLACEMENT_3D ( 'NONE', #10275, #9248, #4498 ) ;
#5544=DIRECTION ( 'NONE',  ( -1.000000000000000000, 1.010728034814421376E-30, 1.090846720500930387E-30 ) ) ;
#5545=VECTOR ( 'NONE', #11640, 1000.000000000000000 ) ;
#5548=DIRECTION ( 'NONE',  ( -1.140150527077241873E-30, 0.000000000000000000, 1.000000000000000000 ) ) ;
#5550=VECTOR ( 'NONE', #9896, 1000.000000000000000 ) ;
#5552=AXIS2_PLACEMENT_3D ( 'NONE', #4652, #11420, #2599 ) ;
#5553=CARTESIAN_POINT ( 'NONE',  ( 19.99999999999999645, 1.395418990828201533, 6.428133065596412621 ) ) ;
#5556=DIRECTION ( 'NONE',  ( -1.000000000000000000, 1.010728034814421376E-30, 1.090846720500930387E-30 ) ) ;
#5558=FACE_OUTER_BOUND ( 'NONE', #4309, .T. ) ;
#5559=CARTESIAN_POINT ( 'NONE',  ( 3.054370817402615033E-30, -6.459281472512932609, 1.556709314830545976 ) ) ;
#5560=CARTESIAN_POINT ( 'NONE',  ( -10.00000000000000178, 0.000000000000000000, 0.000000000000000000 ) ) ;
#5562=AXIS2_PLACEMENT_3D ( 'NONE', #5638, #8790, #12734 ) ;
#5563=AXIS2_PLACEMENT_3D ( 'NONE', #11536, #8560, #7411 ) ;
#5564=CARTESIAN_POINT ( 'NONE',  ( 0.000000000000000000, 0.000000000000000000, 0.000000000000000000 ) ) ;
#5570=ORIENTED_EDGE ( 'NONE', *, *, #564, .F. ) ;
#5575=DIRECTION ( 'NONE',  ( -1.000000000000000000, 1.010728034814421376E-30, 1.090846720500930387E-30 ) ) ;
#5576=ORIENTED_EDGE ( 'NONE', *, *, #12400, .T. ) ;
#5577=CARTESIAN_POINT ( 'NONE',  ( 19.99999999999999645, 0.000000000000000000, 0.000000000000000000 ) ) ;
#5579=ORIENTED_EDGE ( 'NONE', *, *, #11447, .F. ) ;
#5589=VECTOR ( 'NONE', #6727, 1000.000000000000000 ) ;
#5590=ORIENTED_EDGE ( 'NONE', *, *, #4940, .F. ) ;
#5591=CARTESIAN_POINT ( 'NONE',  ( 19.99999999999999645, 0.000000000000000000, 0.000000000000000000 ) ) ;
#5593=CYLINDRICAL_SURFACE ( 'NONE', #520, 2.800000000000003819 ) ;
#5594=UNCERTAINTY_MEASURE_WITH_UNIT (LENGTH_MEASURE( 1.000000000000000082E-05 ), #2132, 'distance_accuracy_value', 'NONE');
#5595=VECTOR ( 'NONE', #2001, 1000.000000000000000 ) ;
#5598=ORIENTED_EDGE ( 'NONE', *, *, #9179, .F. ) ;
#5599=DIRECTION ( 'NONE',  ( -1.158639454543359338E-30, 0.08963930890342672320, 0.9959742939952396235 ) ) ;
#5602=CYLINDRICAL_SURFACE ( 'NONE', #5563, 6.499000000000010324 ) ;
#5604=LINE ( 'NONE', #9267, #7302 ) ;
#5605=CARTESIAN_POINT ( 'NONE',  ( 0.000000000000000000, 5.362412286431502473, -3.809543717993857381 ) ) ;
#5608=ORIENTED_EDGE ( 'NONE', *, *, #714, .F. ) ;
#5611=VECTOR ( 'NONE', #5081, 1000.000000000000000 ) ;
#5613=CARTESIAN_POINT ( 'NONE',  ( 19.99999999999997868, 6.496448636052932990, 0.1820882179769736653 ) ) ;
#5614=CARTESIAN_POINT ( 'NONE',  ( 0.000000000000000000, 2.180689217871957908, -6.122221454264557217 ) ) ;
#5619=CARTESIAN_POINT ( 'NONE',  ( 19.99999999999999645, -5.610543508060446882, 3.433640984893234549 ) ) ;
#5621=EDGE_CURVE ( 'NONE', #5369, #4507, #6296, .T. ) ;
#5624=ORIENTED_EDGE ( 'NONE', *, *, #4503, .T. ) ;
#5626=ORIENTED_EDGE ( 'NONE', *, *, #11802, .T. ) ;
#5628=DIRECTION ( 'NONE',  ( -1.000000000000000000, 1.010728034814421376E-30, 1.090846720500930387E-30 ) ) ;
#5629=DIRECTION ( 'NONE',  ( -1.429810390713081445E-30, 0.5877852522924684742, 0.8090169943749507819 ) ) ;
#5635=DIRECTION ( 'NONE',  ( -1.000000000000000000, 1.010728034814421376E-30, 1.090846720500930387E-30 ) ) ;
#5636=ORIENTED_EDGE ( 'NONE', *, *, #5884, .T. ) ;
#5637=ORIENTED_EDGE ( 'NONE', *, *, #2687, .T. ) ;
#5638=CARTESIAN_POINT ( 'NONE',  ( 19.99999999999999645, 0.000000000000000000, 0.000000000000000000 ) ) ;
#5639=VERTEX_POINT ( 'NONE', #5143 ) ;
#5644=ORIENTED_EDGE ( 'NONE', *, *, #1006, .F. ) ;
#5649=DIRECTION ( 'NONE',  ( 0.000000000000000000, 0.000000000000000000, 1.000000000000000000 ) ) ;
#5651=VECTOR ( 'NONE', #11134, 1000.000000000000000 ) ;
#5652=EDGE_CURVE ( 'NONE', #6793, #7062, #4654, .T. ) ;
#5654=VERTEX_POINT ( 'NONE', #3098 ) ;
#5655=VERTEX_POINT ( 'NONE', #12173 ) ;
#5656=DIRECTION ( 'NONE',  ( 0.000000000000000000, 0.000000000000000000, 1.000000000000000000 ) ) ;
#5658=ORIENTED_EDGE ( 'NONE', *, *, #9957, .T. ) ;
#5668=CYLINDRICAL_SURFACE ( 'NONE', #12361, 6.499000000000010324 ) ;
#5669=ORIENTED_EDGE ( 'NONE', *, *, #3470, .F. ) ;
#5670=DIRECTION ( 'NONE',  ( -1.000000000000000000, 1.010728034814421376E-30, 1.090846720500930387E-30 ) ) ;
#5673=CARTESIAN_POINT ( 'NONE',  ( 0.000000000000000000, 6.496448636052942760, 0.1820882179769667264 ) ) ;
#5676=CARTESIAN_POINT ( 'NONE',  ( 0.000000000000000000, 1.764426149628233853, -7.186570834724189005 ) ) ;
#5679=DIRECTION ( 'NONE',  ( -1.000000000000000000, 1.010728034814421376E-30, 1.090846720500930387E-30 ) ) ;
#5683=CIRCLE ( 'NONE', #7938, 2.800000000000002487 ) ;
#5687=EDGE_LOOP ( 'NONE', ( #3062, #5576, #4930, #3427 ) ) ;
#5688=VERTEX_POINT ( 'NONE', #4563 ) ;
#5689=ORIENTED_EDGE ( 'NONE', *, *, #5372, .F. ) ;
#5694=EDGE_CURVE ( 'NONE', #2020, #7959, #9494, .T. ) ;
#5697=ORIENTED_EDGE ( 'NONE', *, *, #4940, .T. ) ;
#5700=CARTESIAN_POINT ( 'NONE',  ( -10.00000000000000178, 0.000000000000000000, 0.000000000000000000 ) ) ;
#5701=ORIENTED_EDGE ( 'NONE', *, *, #2000, .T. ) ;
#5703=DIRECTION ( 'NONE',  ( -1.000000000000000000, 1.010728034814421376E-30, 1.090846720500930387E-30 ) ) ;
#5704=ORIENTED_EDGE ( 'NONE', *, *, #9415, .F. ) ;
#5707=CARTESIAN_POINT ( 'NONE',  ( 0.000000000000000000, 0.000000000000000000, 0.000000000000000000 ) ) ;
#5708=AXIS2_PLACEMENT_3D ( 'NONE', #9814, #10725, #9751 ) ;
#5709=LINE ( 'NONE', #9616, #5545 ) ;
#5712=LINE ( 'NONE', #11643, #11412 ) ;
#5716=DIRECTION ( 'NONE',  ( -1.000000000000000000, 1.010728034814421376E-30, 1.090846720500930387E-30 ) ) ;
#5723=AXIS2_PLACEMENT_3D ( 'NONE', #9477, #12603, #4482 ) ;
#5727=EDGE_CURVE ( 'NONE', #8539, #11730, #10129, .T. ) ;
#5730=ADVANCED_FACE ( 'NONE', ( #2368 ), #7259, .T. ) ;
#5733=DIRECTION ( 'NONE',  ( -1.000000000000000000, 1.010728034814421376E-30, 1.090846720500930387E-30 ) ) ;
#5737=AXIS2_PLACEMENT_3D ( 'NONE', #10756, #9845, #8889 ) ;
#5739=DIRECTION ( 'NONE',  ( 1.000000000000000000, -1.010728034814421376E-30, -1.090846720500930387E-30 ) ) ;
#5740=CARTESIAN_POINT ( 'NONE',  ( 19.99999999999999645, -6.577476285968334224, 2.730038749994996294 ) ) ;
#5741=AXIS2_PLACEMENT_3D ( 'NONE', #2837, #1969, #8799 ) ;
#5742=FACE_OUTER_BOUND ( 'NONE', #933, .T. ) ;
#5744=DIRECTION ( 'NONE',  ( 1.140150527077241873E-30, 0.000000000000000000, -1.000000000000000000 ) ) ;
#5745=CARTESIAN_POINT ( 'NONE',  ( 19.99999999999999645, -6.289597356626510205, 3.898841506334512541 ) ) ;
#5748=CIRCLE ( 'NONE', #611, 2.800000000000002931 ) ;
#5751=VERTEX_POINT ( 'NONE', #11179 ) ;
#5752=ORIENTED_EDGE ( 'NONE', *, *, #8915, .F. ) ;
#5756=AXIS2_PLACEMENT_3D ( 'NONE', #7533, #5539, #9573 ) ;
#5760=EDGE_LOOP ( 'NONE', ( #5010, #7794, #10068, #7968 ) ) ;
#5761=ORIENTED_EDGE ( 'NONE', *, *, #12015, .T. ) ;
#5768=DIRECTION ( 'NONE',  ( 0.000000000000000000, 0.000000000000000000, 1.000000000000000000 ) ) ;
#5769=ORIENTED_EDGE ( 'NONE', *, *, #4486, .T. ) ;
#5770=DIRECTION ( 'NONE',  ( -1.000000000000000000, 1.010728034814421376E-30, 1.090846720500930387E-30 ) ) ;
#5781=ORIENTED_EDGE ( 'NONE', *, *, #2687, .F. ) ;
#5783=ORIENTED_EDGE ( 'NONE', *, *, #4464, .F. ) ;
#5786=CIRCLE ( 'NONE', #6416, 6.499000000000011212 ) ;
#5788=AXIS2_PLACEMENT_3D ( 'NONE', #9912, #267, #5876 ) ;
#5789=EDGE_CURVE ( 'NONE', #4412, #9489, #12093, .T. ) ;
#5792=CARTESIAN_POINT ( 'NONE',  ( 19.99999999999999645, -6.459281472512932609, -1.243290685169442966 ) ) ;
#5796=EDGE_CURVE ( 'NONE', #4162, #4793, #3850, .T. ) ;
#5797=CYLINDRICAL_SURFACE ( 'NONE', #6599, 6.499000000000010324 ) ;
#5799=CARTESIAN_POINT ( 'NONE',  ( 0.000000000000000000, 7.100173756228453037, -2.085073771204482007 ) ) ;
#5800=EDGE_CURVE ( 'NONE', #2961, #2884, #3249, .T. ) ;
#5802=DIRECTION ( 'NONE',  ( -1.000000000000000000, 1.010728034814421376E-30, 1.090846720500930387E-30 ) ) ;
#5804=LINE ( 'NONE', #2870, #2601 ) ;
#5812=ORIENTED_EDGE ( 'NONE', *, *, #646, .T. ) ;
#5813=ORIENTED_EDGE ( 'NONE', *, *, #10492, .T. ) ;
#5819=CARTESIAN_POINT ( 'NONE',  ( 19.99999999999997868, 3.975087478966734533, -6.241688836730180157 ) ) ;
#5820=ORIENTED_EDGE ( 'NONE', *, *, #5960, .F. ) ;
#5821=DIRECTION ( 'NONE',  ( 0.000000000000000000, 0.9195277725514489076, 0.3930250316539278255 ) ) ;
#5823=CARTESIAN_POINT ( 'NONE',  ( 0.000000000000000000, 5.670261409740643188, 3.175710400084689411 ) ) ;
#5827=VECTOR ( 'NONE', #3261, 1000.000000000000000 ) ;
#5839=AXIS2_PLACEMENT_3D ( 'NONE', #9654, #8708, #10691 ) ;
#5847=EDGE_CURVE ( 'NONE', #175, #3101, #3036, .T. ) ;
#5848=LINE ( 'NONE', #1143, #5611 ) ;
#5849=ORIENTED_EDGE ( 'NONE', *, *, #8477, .F. ) ;
#5850=CARTESIAN_POINT ( 'NONE',  ( 9.999999999999998224, 7.100173756228454813, -2.085073771204489113 ) ) ;
#5851=ORIENTED_EDGE ( 'NONE', *, *, #11926, .F. ) ;
#5855=EDGE_CURVE ( 'NONE', #5655, #229, #133, .T. ) ;
#5856=EDGE_CURVE ( 'NONE', #9808, #1261, #10192, .T. ) ;
#5858=DIRECTION ( 'NONE',  ( -1.140150527077241873E-30, 0.000000000000000000, 1.000000000000000000 ) ) ;
#5860=CARTESIAN_POINT ( 'NONE',  ( -10.00000000000000178, 0.000000000000000000, 0.000000000000000000 ) ) ;
#5861=CIRCLE ( 'NONE', #4638, 6.499000000000010324 ) ;
#5863=AXIS2_PLACEMENT_3D ( 'NONE', #5887, #4923, #1955 ) ;
#5864=CARTESIAN_POINT ( 'NONE',  ( 19.99999999999999645, 3.975087478966644383, 6.241688836730229006 ) ) ;
#5865=DIRECTION ( 'NONE',  ( 0.000000000000000000, 0.8345732537213000901, 0.5508969814521065267 ) ) ;
#5867=DIRECTION ( 'NONE',  ( -1.000000000000000000, 1.010728034814421376E-30, 1.090846720500930387E-30 ) ) ;
#5868=DIRECTION ( 'NONE',  ( 1.000000000000000000, -1.010728034814421376E-30, -1.090846720500930387E-30 ) ) ;
#5870=CARTESIAN_POINT ( 'NONE',  ( 19.99999999999999645, -4.155687294075622873, 5.098857909653524700 ) ) ;
#5871=CIRCLE ( 'NONE', #4443, 6.499000000000011212 ) ;
#5874=DIRECTION ( 'NONE',  ( 1.000000000000000000, -1.010728034814421376E-30, -1.090846720500930387E-30 ) ) ;
#5876=DIRECTION ( 'NONE',  ( 1.405158487424925001E-30, -0.3513748240813304724, -0.9362348706397417564 ) ) ;
#5880=DIRECTION ( 'NONE',  ( -1.000000000000000000, 1.010728034814421376E-30, 1.090846720500930387E-30 ) ) ;
#5881=DIRECTION ( 'NONE',  ( 0.000000000000000000, 0.000000000000000000, 1.000000000000000000 ) ) ;
#5884=EDGE_CURVE ( 'NONE', #802, #6992, #608, .T. ) ;
#5886=ORIENTED_EDGE ( 'NONE', *, *, #3155, .T. ) ;
#5887=CARTESIAN_POINT ( 'NONE',  ( 19.99999999999997868, 6.557268578288205418, -0.5199208220221240850 ) ) ;
#5888=EDGE_CURVE ( 'NONE', #3594, #5515, #7940, .T. ) ;
#5893=ORIENTED_EDGE ( 'NONE', *, *, #3470, .T. ) ;
#5894=VERTEX_POINT ( 'NONE', #4609 ) ;
#5896=ORIENTED_EDGE ( 'NONE', *, *, #9076, .T. ) ;
#5899=ORIENTED_EDGE ( 'NONE', *, *, #3893, .F. ) ;
#5900=VECTOR ( 'NONE', #6532, 1000.000000000000000 ) ;
#5901=CARTESIAN_POINT ( 'NONE',  ( 19.99999999999999645, 0.000000000000000000, 0.000000000000000000 ) ) ;
#5902=CYLINDRICAL_SURFACE ( 'NONE', #6471, 2.800000000000003819 ) ;
#5904=CARTESIAN_POINT ( 'NONE',  ( 19.99999999999997868, -0.8135880386782390339, -6.527339685683426929 ) ) ;
#5905=CARTESIAN_POINT ( 'NONE',  ( 0.000000000000000000, 5.670261409740692038, -3.175710400084609475 ) ) ;
#5907=VERTEX_POINT ( 'NONE', #12346 ) ;
#5908=CIRCLE ( 'NONE', #10824, 6.499000000000009436 ) ;
#5912=CARTESIAN_POINT ( 'NONE',  ( 19.99999999999999645, 0.000000000000000000, 0.000000000000000000 ) ) ;
#5915=ORIENTED_EDGE ( 'NONE', *, *, #4077, .F. ) ;
#5917=CARTESIAN_POINT ( 'NONE',  ( 19.99999999999999645, -5.148708580507705967, 3.965829163366258570 ) ) ;
#5919=VERTEX_POINT ( 'NONE', #9541 ) ;
#5920=DIRECTION ( 'NONE',  ( -1.000000000000000000, 1.010728034814421376E-30, 1.090846720500930387E-30 ) ) ;
#5921=ORIENTED_EDGE ( 'NONE', *, *, #9304, .F. ) ;
#5922=DIRECTION ( 'NONE',  ( -1.000000000000000000, 1.010728034814421376E-30, 1.090846720500930387E-30 ) ) ;
#5924=EDGE_CURVE ( 'NONE', #11920, #12737, #4040, .T. ) ;
#5928=CARTESIAN_POINT ( 'NONE',  ( 19.99999999999999645, -6.133480037816472219, -2.376659734729558160 ) ) ;
#5932=CARTESIAN_POINT ( 'NONE',  ( 0.000000000000000000, 4.596015818000147135, -4.705818469689461381 ) ) ;
#5933=LINE ( 'NONE', #9851, #10525 ) ;
#5940=ORIENTED_EDGE ( 'NONE', *, *, #4969, .T. ) ;
#5943=DIRECTION ( 'NONE',  ( -1.000000000000000000, 1.010728034814421376E-30, 1.090846720500930387E-30 ) ) ;
#5947=AXIS2_PLACEMENT_3D ( 'NONE', #1227, #202, #6191 ) ;
#5948=FACE_BOUND ( 'NONE', #10452, .T. ) ;
#5949=CARTESIAN_POINT ( 'NONE',  ( 19.99999999999999645, 0.000000000000000000, 0.000000000000000000 ) ) ;
#5951=CIRCLE ( 'NONE', #11931, 2.800000000000003375 ) ;
#5955=ORIENTED_EDGE ( 'NONE', *, *, #5847, .F. ) ;
#5960=EDGE_CURVE ( 'NONE', #9234, #3660, #6103, .T. ) ;
#5961=CIRCLE ( 'NONE', #4101, 2.800000000000002931 ) ;
#5962=DIRECTION ( 'NONE',  ( -1.000000000000000000, 1.010728034814421376E-30, 1.090846720500930387E-30 ) ) ;
#5964=ORIENTED_EDGE ( 'NONE', *, *, #8855, .F. ) ;
#5967=ORIENTED_EDGE ( 'NONE', *, *, #2569, .F. ) ;
#5970=DIRECTION ( 'NONE',  ( 0.000000000000000000, -0.08963930890344096181, 0.9959742939952382912 ) ) ;
#5972=ORIENTED_EDGE ( 'NONE', *, *, #65, .F. ) ;
#5973=VERTEX_POINT ( 'NONE', #2880 ) ;
#5975=DIRECTION ( 'NONE',  ( 0.000000000000000000, -0.6579387259397028176, -0.7530714660036194052 ) ) ;
#5978=DIRECTION ( 'NONE',  ( -1.000000000000000000, 1.010728034814421376E-30, 1.090846720500930387E-30 ) ) ;
#5984=ORIENTED_EDGE ( 'NONE', *, *, #5232, .F. ) ;
#5986=EDGE_LOOP ( 'NONE', ( #3285, #5752, #2081, #11496 ) ) ;
#5987=DIRECTION ( 'NONE',  ( -1.000000000000000000, 1.010728034814421376E-30, 1.090846720500930387E-30 ) ) ;
#5991=CIRCLE ( 'NONE', #1465, 2.800000000000002043 ) ;
#5997=DIRECTION ( 'NONE',  ( -1.000000000000000000, 1.010728034814421376E-30, 1.090846720500930387E-30 ) ) ;
#5998=CIRCLE ( 'NONE', #452, 6.499000000000008548 ) ;
#6000=VERTEX_POINT ( 'NONE', #3951 ) ;
#6002=LINE ( 'NONE', #9920, #8565 ) ;
#6005=DIRECTION ( 'NONE',  ( 1.000000000000000000, -1.010728034814421376E-30, -1.090846720500930387E-30 ) ) ;
#6007=EDGE_CURVE ( 'NONE', #8095, #6098, #6002, .T. ) ;
#6008=CARTESIAN_POINT ( 'NONE',  ( 0.000000000000000000, 2.520781513113648398, 6.075668640744193105 ) ) ;
#6010=ADVANCED_FACE ( 'NONE', ( #10704 ), #4982, .T. ) ;
#6014=ORIENTED_EDGE ( 'NONE', *, *, #7796, .T. ) ;
#6015=VERTEX_POINT ( 'NONE', #8721 ) ;
#6017=EDGE_LOOP ( 'NONE', ( #5373, #5598, #287, #346 ) ) ;
#6021=CIRCLE ( 'NONE', #468, 2.800000000000003819 ) ;
#6023=DIRECTION ( 'NONE',  ( 0.000000000000000000, -0.6579387259397028176, -0.7530714660036196273 ) ) ;
#6027=VERTEX_POINT ( 'NONE', #4919 ) ;
#6029=CARTESIAN_POINT ( 'NONE',  ( 9.999999999999998224, -3.399584271718289141, -6.572885726945646212 ) ) ;
#6033=ORIENTED_EDGE ( 'NONE', *, *, #3927, .F. ) ;
#6034=ORIENTED_EDGE ( 'NONE', *, *, #3986, .F. ) ;
#6037=CIRCLE ( 'NONE', #10554, 2.800000000000003375 ) ;
#6039=ORIENTED_EDGE ( 'NONE', *, *, #6040, .F. ) ;
#6040=EDGE_CURVE ( 'NONE', #2828, #6343, #957, .T. ) ;
#6042=ORIENTED_EDGE ( 'NONE', *, *, #2999, .F. ) ;
#6043=DIRECTION ( 'NONE',  ( 0.000000000000000000, 0.000000000000000000, 1.000000000000000000 ) ) ;
#6046=CARTESIAN_POINT ( 'NONE',  ( 0.000000000000000000, 0.000000000000000000, 0.000000000000000000 ) ) ;
#6048=DIRECTION ( 'NONE',  ( -1.000000000000000000, 1.010728034814421376E-30, 1.090846720500930387E-30 ) ) ;
#6051=EDGE_LOOP ( 'NONE', ( #5967, #5207, #2377, #10717 ) ) ;
#6052=CARTESIAN_POINT ( 'NONE',  ( 0.000000000000000000, 7.358375340957004518, -0.7837807994560929137 ) ) ;
#6057=EDGE_CURVE ( 'NONE', #4412, #5688, #7537, .T. ) ;
#6061=CIRCLE ( 'NONE', #9955, 2.800000000000002931 ) ;
#6063=DIRECTION ( 'NONE',  ( -2.280301054154483747E-31, -0.5877852522924802425, 0.8090169943749422332 ) ) ;
#6064=CARTESIAN_POINT ( 'NONE',  ( 0.000000000000000000, 3.238809497145290539, -5.634457741540130016 ) ) ;
#6065=EDGE_CURVE ( 'NONE', #7722, #3047, #12297, .T. ) ;
#6068=CIRCLE ( 'NONE', #521, 6.499000000000009436 ) ;
#6069=DIRECTION ( 'NONE',  ( -1.000000000000000000, 1.010728034814421376E-30, 1.090846720500930387E-30 ) ) ;
#6071=CARTESIAN_POINT ( 'NONE',  ( 19.99999999999999645, 0.000000000000000000, 0.000000000000000000 ) ) ;
#6076=CARTESIAN_POINT ( 'NONE',  ( 19.99999999999999645, 6.613766744932249253, 3.319350756342022368 ) ) ;
#6080=CARTESIAN_POINT ( 'NONE',  ( 0.000000000000000000, 0.000000000000000000, 0.000000000000000000 ) ) ;
#6085=CARTESIAN_POINT ( 'NONE',  ( 19.99999999999999645, 0.000000000000000000, 0.000000000000000000 ) ) ;
#6088=CARTESIAN_POINT ( 'NONE',  ( 19.99999999999999645, 0.000000000000000000, 0.000000000000000000 ) ) ;
#6090=ORIENTED_EDGE ( 'NONE', *, *, #9913, .T. ) ;
#6093=AXIS2_PLACEMENT_3D ( 'NONE', #5070, #5197, #232 ) ;
#6094=DIRECTION ( 'NONE',  ( -1.000000000000000000, 1.010728034814421376E-30, 1.090846720500930387E-30 ) ) ;
#6097=ORIENTED_EDGE ( 'NONE', *, *, #3310, .T. ) ;
#6098=VERTEX_POINT ( 'NONE', #4206 ) ;
#6100=ORIENTED_EDGE ( 'NONE', *, *, #8949, .T. ) ;
#6101=CIRCLE ( 'NONE', #9181, 7.400000000000009237 ) ;
#6103=CIRCLE ( 'NONE', #10816, 7.400000000000011902 ) ;
#6107=CARTESIAN_POINT ( 'NONE',  ( 0.000000000000000000, -2.171317488608455637, -7.074275960383735296 ) ) ;
#6108=ORIENTED_EDGE ( 'NONE', *, *, #9762, .F. ) ;
#6114=CARTESIAN_POINT ( 'NONE',  ( 9.999999999999994671, 1.764426149628142593, 7.186570834724209433 ) ) ;
#6117=ORIENTED_EDGE ( 'NONE', *, *, #7544, .F. ) ;
#6118=CARTESIAN_POINT ( 'NONE',  ( 19.99999999999999645, 0.000000000000000000, 0.000000000000000000 ) ) ;
#6119=SHAPE_REPRESENTATION_RELATIONSHIP ( 'NONE' , 'NONE' ,  #891, #1117 ) ;
#6120=ADVANCED_FACE ( 'NONE', ( #3386 ), #10111, .T. ) ;
#6124=DIRECTION ( 'NONE',  ( -1.000000000000000000, 1.010728034814421376E-30, 1.090846720500930387E-30 ) ) ;
#6126=EDGE_CURVE ( 'NONE', #3160, #9801, #5908, .T. ) ;
#6128=DIRECTION ( 'NONE',  ( -1.158639454543359162E-30, 0.08963930890342669544, 0.9959742939952396235 ) ) ;
#6129=DIRECTION ( 'NONE',  ( -1.000000000000000000, 1.010728034814421376E-30, 1.090846720500930387E-30 ) ) ;
#6132=VERTEX_POINT ( 'NONE', #147 ) ;
#6141=CARTESIAN_POINT ( 'NONE',  ( 19.99999999999997868, -1.623118704078857499, -6.293050665016890477 ) ) ;
#6143=CARTESIAN_POINT ( 'NONE',  ( 19.99999999999999645, 0.000000000000000000, 0.000000000000000000 ) ) ;
#6147=CARTESIAN_POINT ( 'NONE',  ( 19.99999999999999645, 5.362412286431453623, 3.809543717993933765 ) ) ;
#6148=VERTEX_POINT ( 'NONE', #4072 ) ;
#6149=CYLINDRICAL_SURFACE ( 'NONE', #1494, 2.800000000000003819 ) ;
#6150=ORIENTED_EDGE ( 'NONE', *, *, #9385, .F. ) ;
#6152=DIRECTION ( 'NONE',  ( -1.000000000000000000, 1.010728034814421376E-30, 1.090846720500930387E-30 ) ) ;
#6153=CARTESIAN_POINT ( 'NONE',  ( 19.99999999999999645, -6.484265599627167198, -1.105616797299011855 ) ) ;
#6156=VECTOR ( 'NONE', #6688, 1000.000000000000000 ) ;
#6157=ADVANCED_FACE ( 'NONE', ( #11945 ), #1175, .T. ) ;
#6159=ORIENTED_EDGE ( 'NONE', *, *, #10099, .F. ) ;
#6162=CIRCLE ( 'NONE', #2266, 6.499000000000008548 ) ;
#6164=VECTOR ( 'NONE', #11416, 1000.000000000000000 ) ;
#6165=CIRCLE ( 'NONE', #397, 2.800000000000003375 ) ;
#6166=DIRECTION ( 'NONE',  ( 0.000000000000000000, 0.000000000000000000, 1.000000000000000000 ) ) ;
#6168=ORIENTED_EDGE ( 'NONE', *, *, #6359, .T. ) ;
#6169=DIRECTION ( 'NONE',  ( 0.000000000000000000, 0.000000000000000000, -1.000000000000000000 ) ) ;
#6171=CARTESIAN_POINT ( 'NONE',  ( 0.000000000000000000, 5.025702764809073742, 5.431603052487396610 ) ) ;
#6172=AXIS2_PLACEMENT_3D ( 'NONE', #5860, #2861, #10682 ) ;
#6174=EDGE_CURVE ( 'NONE', #11698, #8908, #1985, .T. ) ;
#6175=DIRECTION ( 'NONE',  ( 0.000000000000000000, 0.000000000000000000, 1.000000000000000000 ) ) ;
#6176=EDGE_CURVE ( 'NONE', #12656, #8701, #5175, .T. ) ;
#6177=CARTESIAN_POINT ( 'NONE',  ( 19.99999999999997868, 1.764426149628238960, -7.186570834724189005 ) ) ;
#6178=ORIENTED_EDGE ( 'NONE', *, *, #340, .F. ) ;
#6179=LINE ( 'NONE', #8599, #10460 ) ;
#6180=ORIENTED_EDGE ( 'NONE', *, *, #8531, .F. ) ;
#6181=LINE ( 'NONE', #1345, #7861 ) ;
#6183=CIRCLE ( 'NONE', #10676, 6.499000000000010324 ) ;
#6186=CARTESIAN_POINT ( 'NONE',  ( 19.99999999999999645, -6.969736844459705871, 2.486517307195113879 ) ) ;
#6189=DIRECTION ( 'NONE',  ( 0.000000000000000000, 0.000000000000000000, 1.000000000000000000 ) ) ;
#6191=DIRECTION ( 'NONE',  ( 0.000000000000000000, -0.8805955318567323387, -0.4738686624730094610 ) ) ;
#6193=FACE_OUTER_BOUND ( 'NONE', #372, .T. ) ;
#6197=DIRECTION ( 'NONE',  ( 0.000000000000000000, -0.4338837391175658365, 0.9009688679024154823 ) ) ;
#6200=DIRECTION ( 'NONE',  ( -1.000000000000000000, 1.010728034814421376E-30, 1.090846720500930387E-30 ) ) ;
#6203=CIRCLE ( 'NONE', #8463, 7.400000000000009237 ) ;
#6205=CARTESIAN_POINT ( 'NONE',  ( -10.00000000000000178, 0.000000000000000000, 0.000000000000000000 ) ) ;
#6206=EDGE_CURVE ( 'NONE', #7420, #4162, #6594, .T. ) ;
#6208=ORIENTED_EDGE ( 'NONE', *, *, #4099, .T. ) ;
#6209=DIRECTION ( 'NONE',  ( 0.000000000000000000, 0.000000000000000000, 1.000000000000000000 ) ) ;
#6211=VERTEX_POINT ( 'NONE', #591 ) ;
#6213=ORIENTED_EDGE ( 'NONE', *, *, #8187, .T. ) ;
#6214=CARTESIAN_POINT ( 'NONE',  ( 19.99999999999999645, 0.000000000000000000, 0.000000000000000000 ) ) ;
#6215=VECTOR ( 'NONE', #2263, 1000.000000000000000 ) ;
#6216=CARTESIAN_POINT ( 'NONE',  ( 0.000000000000000000, 0.000000000000000000, 0.000000000000000000 ) ) ;
#6218=CARTESIAN_POINT ( 'NONE',  ( 19.99999999999999645, 2.180689217871860652, 6.122221454264574092 ) ) ;
#6223=ORIENTED_EDGE ( 'NONE', *, *, #9415, .T. ) ;
#6225=EDGE_CURVE ( 'NONE', #8279, #1374, #9183, .T. ) ;
#6226=ORIENTED_EDGE ( 'NONE', *, *, #296, .F. ) ;
#6230=ADVANCED_FACE ( 'NONE', ( #1689 ), #11289, .T. ) ;
#6233=FACE_OUTER_BOUND ( 'NONE', #6888, .T. ) ;
#6237=CARTESIAN_POINT ( 'NONE',  ( 19.99999999999999645, 0.000000000000000000, 0.000000000000000000 ) ) ;
#6247=EDGE_CURVE ( 'NONE', #3660, #11576, #7761, .T. ) ;
#6249=ADVANCED_FACE ( 'NONE', ( #5426 ), #8449, .T. ) ;
#6253=CARTESIAN_POINT ( 'NONE',  ( 19.99999999999997868, 6.496448636052932990, -0.1820882179769736653 ) ) ;
#6255=DIRECTION ( 'NONE',  ( 0.000000000000000000, -0.7818314824680222541, -0.6234898018587429203 ) ) ;
#6259=VERTEX_POINT ( 'NONE', #9340 ) ;
#6261=DIRECTION ( 'NONE',  ( -1.000000000000000000, 1.010728034814421376E-30, 1.090846720500930387E-30 ) ) ;
#6269=ADVANCED_FACE ( 'NONE', ( #5558 ), #8510, .T. ) ;
#6273=VECTOR ( 'NONE', #4896, 1000.000000000000000 ) ;
#6274=EDGE_LOOP ( 'NONE', ( #9487, #12026, #8897, #6090, #8034, #9664, #3518, #5812, #10137, #8011, #3303, #12052, #600, #4485, #11271, #7642, #7075, #7947, #11319, #887, #8097, #9927, #1185, #8156, #4054, #11449, #5624, #2179, #3033, #1633, #4375, #10623, #4979, #7639, #3418, #6496, #2891, #10329, #7559, #4302, #3725, #5769, #10745, #11851, #4248, #7013, #69, #667, #5512, #12465, #11631, #1518, #10257, #7661, #2108, #8071, #11472, #8471, #11109, #8910, #8912, #1070, #2903, #5761, #3077, #11651, #8031, #3383, #8789, #806, #4620, #5315, #510, #3037, #647, #5886, #7213, #1197, #8318, #4035, #12447, #3863, #6362, #9053, #4294, #5371, #7587, #3476, #3732, #3657, #3126, #1061, #5065, #2501, #7054, #5268, #10707, #1729, #3287, #5896, #6039, #10092, #10893, #11012, #3003, #10286, #10419, #1485, #5964, #1975, #7294, #9511, #7651, #3805, #10663, #11962, #11628, #10713, #12473, #7508, #8350, #6824, #8989, #12377, #9813, #9561, #12613, #4800, #678, #4102, #2409, #9757, #116, #5458, #3990, #6213, #11188, #3954, #2094, #2552, #6478, #10972, #150, #11499 ) ) ;
#6280=EDGE_CURVE ( 'NONE', #11478, #8279, #3448, .T. ) ;
#6283=CARTESIAN_POINT ( 'NONE',  ( 19.99999999999999645, -0.8732627748488548391, 7.348293143721422283 ) ) ;
#6284=ORIENTED_EDGE ( 'NONE', *, *, #9876, .T. ) ;
#6286=AXIS2_PLACEMENT_3D ( 'NONE', #4845, #10694, #5744 ) ;
#6287=EDGE_CURVE ( 'NONE', #87, #2228, #5282, .T. ) ;
#6291=VERTEX_POINT ( 'NONE', #3818 ) ;
#6293=CARTESIAN_POINT ( 'NONE',  ( 0.000000000000000000, 1.531833341630128409, 6.396997380212699369 ) ) ;
#6296=CIRCLE ( 'NONE', #3029, 6.499000000000009436 ) ;
#6297=CARTESIAN_POINT ( 'NONE',  ( -10.00000000000000178, 0.000000000000000000, 0.000000000000000000 ) ) ;
#6298=ORIENTED_EDGE ( 'NONE', *, *, #754, .T. ) ;
#6301=DIRECTION ( 'NONE',  ( 0.000000000000000000, 0.000000000000000000, 1.000000000000000000 ) ) ;
#6304=AXIS2_PLACEMENT_3D ( 'NONE', #6216, #356, #483 ) ;
#6309=LINE ( 'NONE', #12120, #5152 ) ;
#6312=CARTESIAN_POINT ( 'NONE',  ( 0.000000000000000000, 0.000000000000000000, 0.000000000000000000 ) ) ;
#6313=AXIS2_PLACEMENT_3D ( 'NONE', #7681, #12710, #1935 ) ;
#6318=VERTEX_POINT ( 'NONE', #4905 ) ;
#6320=EDGE_CURVE ( 'NONE', #125, #6740, #2634, .T. ) ;
#6322=VERTEX_POINT ( 'NONE', #9782 ) ;
#6323=DIRECTION ( 'NONE',  ( 1.000000000000000000, -1.010728034814421376E-30, -1.090846720500930387E-30 ) ) ;
#6324=DIRECTION ( 'NONE',  ( 0.000000000000000000, 0.9510565162951544194, -0.3090169943749445092 ) ) ;
#6325=DIRECTION ( 'NONE',  ( -1.000000000000000000, 1.010728034814421376E-30, 1.090846720500930387E-30 ) ) ;
#6327=CARTESIAN_POINT ( 'NONE',  ( 19.99999999999999645, 0.000000000000000000, 0.000000000000000000 ) ) ;
#6328=CARTESIAN_POINT ( 'NONE',  ( 19.99999999999999645, 0.000000000000000000, 0.000000000000000000 ) ) ;
#6334=ORIENTED_EDGE ( 'NONE', *, *, #1157, .F. ) ;
#6335=ORIENTED_EDGE ( 'NONE', *, *, #3547, .T. ) ;
#6337=CIRCLE ( 'NONE', #1015, 7.400000000000011902 ) ;
#6343=VERTEX_POINT ( 'NONE', #9715 ) ;
#6344=DIRECTION ( 'NONE',  ( 1.000000000000000000, -1.010728034814421376E-30, -1.090846720500930387E-30 ) ) ;
#6347=CARTESIAN_POINT ( 'NONE',  ( 19.99999999999999645, -0.8135880386783197471, 6.527339685683405612 ) ) ;
#6348=EDGE_LOOP ( 'NONE', ( #12360, #1601, #5136, #9462 ) ) ;
#6352=ADVANCED_FACE ( 'NONE', ( #5742 ), #6908, .T. ) ;
#6353=ORIENTED_EDGE ( 'NONE', *, *, #3364, .F. ) ;
#6354=FACE_OUTER_BOUND ( 'NONE', #2309, .T. ) ;
#6359=EDGE_CURVE ( 'NONE', #640, #1141, #6782, .T. ) ;
#6362=ORIENTED_EDGE ( 'NONE', *, *, #11241, .T. ) ;
#6363=DIRECTION ( 'NONE',  ( -1.000000000000000000, 1.010728034814421376E-30, 1.090846720500930387E-30 ) ) ;
#6365=DIRECTION ( 'NONE',  ( -1.000000000000000000, 1.010728034814421376E-30, 1.090846720500930387E-30 ) ) ;
#6366=AXIS2_PLACEMENT_3D ( 'NONE', #10620, #11727, #2924 ) ;
#6368=CIRCLE ( 'NONE', #8002, 2.500000000000003553 ) ;
#6370=DIRECTION ( 'NONE',  ( -1.000000000000000000, 1.010728034814421376E-30, 1.090846720500930387E-30 ) ) ;
#6376=CYLINDRICAL_SURFACE ( 'NONE', #5756, 2.800000000000003819 ) ;
#6377=VECTOR ( 'NONE', #2325, 1000.000000000000000 ) ;
#6382=DIRECTION ( 'NONE',  ( 1.000000000000000000, -1.010728034814421376E-30, -1.090846720500930387E-30 ) ) ;
#6383=CARTESIAN_POINT ( 'NONE',  ( 19.99999999999999645, -6.577476285968334224, -0.06996125000500313940 ) ) ;
#6387=AXIS2_PLACEMENT_3D ( 'NONE', #6297, #9187, #8232 ) ;
#6388=CYLINDRICAL_SURFACE ( 'NONE', #7853, 2.800000000000003819 ) ;
#6389=ADVANCED_FACE ( 'NONE', ( #14 ), #1032, .T. ) ;
#6391=EDGE_CURVE ( 'NONE', #8587, #4499, #2933, .T. ) ;
#6392=DIRECTION ( 'NONE',  ( -1.000000000000000000, 1.010728034814421376E-30, 1.090846720500930387E-30 ) ) ;
#6393=ORIENTED_EDGE ( 'NONE', *, *, #8248, .T. ) ;
#6400=DIRECTION ( 'NONE',  ( 1.380506584136768733E-30, -0.5128992774058949156, -0.8584487936018728726 ) ) ;
#6405=VECTOR ( 'NONE', #10312, 1000.000000000000000 ) ;
#6408=ORIENTED_EDGE ( 'NONE', *, *, #323, .T. ) ;
#6410=EDGE_CURVE ( 'NONE', #5127, #1397, #759, .T. ) ;
#6411=DIRECTION ( 'NONE',  ( -1.000000000000000000, 1.010728034814421376E-30, 1.090846720500930387E-30 ) ) ;
#6412=EDGE_CURVE ( 'NONE', #11656, #4395, #10427, .T. ) ;
#6414=DIRECTION ( 'NONE',  ( -1.000000000000000000, 1.010728034814421376E-30, 1.090846720500930387E-30 ) ) ;
#6415=ADVANCED_FACE ( 'NONE', ( #1878 ), #9841, .T. ) ;
#6416=AXIS2_PLACEMENT_3D ( 'NONE', #3556, #9450, #2528 ) ;
#6417=CARTESIAN_POINT ( 'NONE',  ( 19.99999999999999645, -6.133480037816503305, 2.376659734729468010 ) ) ;
#6418=ORIENTED_EDGE ( 'NONE', *, *, #9688, .T. ) ;
#6419=EDGE_CURVE ( 'NONE', #5144, #4279, #4972, .T. ) ;
#6424=EDGE_LOOP ( 'NONE', ( #8153, #3961, #12502, #10488 ) ) ;
#6426=ORIENTED_EDGE ( 'NONE', *, *, #9595, .T. ) ;
#6428=DIRECTION ( 'NONE',  ( 1.000000000000000000, 0.000000000000000000, 0.000000000000000000 ) ) ;
#6429=CIRCLE ( 'NONE', #659, 7.400000000000011902 ) ;
#6432=CARTESIAN_POINT ( 'NONE',  ( 19.99999999999997868, 4.596015818000145359, -4.705818469689468486 ) ) ;
#6433=DIRECTION ( 'NONE',  ( 0.000000000000000000, -0.2660368455666825005, 0.9639628606958513535 ) ) ;
#6434=EDGE_LOOP ( 'NONE', ( #5387, #4868, #9134, #4171 ) ) ;
#6435=EDGE_CURVE ( 'NONE', #2491, #11340, #3453, .T. ) ;
#6436=CARTESIAN_POINT ( 'NONE',  ( 19.99999999999997868, -3.426907987218776874, -5.522074125465566752 ) ) ;
#6437=CARTESIAN_POINT ( 'NONE',  ( 19.99999999999999645, 0.000000000000000000, 0.000000000000000000 ) ) ;
#6439=LINE ( 'NONE', #8483, #311 ) ;
#6440=CIRCLE ( 'NONE', #11166, 2.800000000000002931 ) ;
#6441=DIRECTION ( 'NONE',  ( 0.000000000000000000, 0.000000000000000000, 1.000000000000000000 ) ) ;
#6442=ADVANCED_FACE ( 'NONE', ( #3876 ), #7921, .T. ) ;
#6444=ORIENTED_EDGE ( 'NONE', *, *, #6834, .F. ) ;
#6447=CARTESIAN_POINT ( 'NONE',  ( 19.99999999999999645, -6.577476285968334224, -0.06996125000500313940 ) ) ;
#6448=VECTOR ( 'NONE', #1266, 1000.000000000000000 ) ;
#6452=CYLINDRICAL_SURFACE ( 'NONE', #299, 6.499000000000010324 ) ;
#6453=AXIS2_PLACEMENT_3D ( 'NONE', #9153, #11814, #3006 ) ;
#6454=DIRECTION ( 'NONE',  ( 0.000000000000000000, 0.000000000000000000, 1.000000000000000000 ) ) ;
#6456=CARTESIAN_POINT ( 'NONE',  ( 0.000000000000000000, 0.000000000000000000, 0.000000000000000000 ) ) ;
#6460=VERTEX_POINT ( 'NONE', #6968 ) ;
#6461=CARTESIAN_POINT ( 'NONE',  ( 19.99999999999999645, 0.000000000000000000, 0.000000000000000000 ) ) ;
#6462=DIRECTION ( 'NONE',  ( -1.000000000000000000, 1.010728034814421376E-30, 1.090846720500930387E-30 ) ) ;
#6465=CARTESIAN_POINT ( 'NONE',  ( 9.999999999999994671, -7.258495115966563382, -1.440225208600910634 ) ) ;
#6467=CIRCLE ( 'NONE', #8926, 6.499000000000011212 ) ;
#6468=CARTESIAN_POINT ( 'NONE',  ( 9.999999999999994671, -3.399584271718382844, 6.572885726945587592 ) ) ;
#6469=EDGE_CURVE ( 'NONE', #12527, #8854, #12302, .T. ) ;
#6471=AXIS2_PLACEMENT_3D ( 'NONE', #8859, #4812, #8676 ) ;
#6472=CARTESIAN_POINT ( 'NONE',  ( 0.000000000000000000, 0.000000000000000000, 0.000000000000000000 ) ) ;
#6475=CIRCLE ( 'NONE', #1335, 7.400000000000009237 ) ;
#6477=AXIS2_PLACEMENT_3D ( 'NONE', #12557, #3730, #4758 ) ;
#6478=ORIENTED_EDGE ( 'NONE', *, *, #12679, .T. ) ;
#6479=CARTESIAN_POINT ( 'NONE',  ( 0.000000000000000000, 0.000000000000000000, 0.000000000000000000 ) ) ;
#6480=DIRECTION ( 'NONE',  ( 0.000000000000000000, 0.8805955318567392220, -0.4738686624729965269 ) ) ;
#6481=DIRECTION ( 'NONE',  ( 1.140150527077241873E-30, 0.000000000000000000, -1.000000000000000000 ) ) ;
#6482=CARTESIAN_POINT ( 'NONE',  ( 0.000000000000000000, -5.492355906873351401, -4.959236492872013180 ) ) ;
#6483=ORIENTED_EDGE ( 'NONE', *, *, #7692, .F. ) ;
#6485=DIRECTION ( 'NONE',  ( 0.000000000000000000, 0.000000000000000000, 1.000000000000000000 ) ) ;
#6486=ORIENTED_EDGE ( 'NONE', *, *, #9838, .F. ) ;
#6487=CIRCLE ( 'NONE', #918, 2.800000000000004263 ) ;
#6490=EDGE_CURVE ( 'NONE', #1849, #479, #7339, .T. ) ;
#6493=ADVANCED_FACE ( 'NONE', ( #9191 ), #7980, .T. ) ;
#6494=ORIENTED_EDGE ( 'NONE', *, *, #4181, .T. ) ;
#6496=ORIENTED_EDGE ( 'NONE', *, *, #564, .T. ) ;
#6499=ORIENTED_EDGE ( 'NONE', *, *, #6685, .F. ) ;
#6500=CIRCLE ( 'NONE', #6286, 2.800000000000003819 ) ;
#6502=CARTESIAN_POINT ( 'NONE',  ( 0.000000000000000000, 5.895746314278404121, -2.916892913127026254 ) ) ;
#6503=CARTESIAN_POINT ( 'NONE',  ( 19.99999999999999645, 0.000000000000000000, 0.000000000000000000 ) ) ;
#6513=CARTESIAN_POINT ( 'NONE',  ( 19.99999999999997868, 6.496448636052932990, -0.1820882179769736653 ) ) ;
#6514=AXIS2_PLACEMENT_3D ( 'NONE', #9668, #3713, #4738 ) ;
#6516=CARTESIAN_POINT ( 'NONE',  ( 19.99999999999999645, 3.238809497145207494, 5.634457741540175313 ) ) ;
#6520=EDGE_CURVE ( 'NONE', #12630, #2783, #5238, .T. ) ;
#6521=CARTESIAN_POINT ( 'NONE',  ( 19.99999999999999645, -4.621065432155044839, -4.569765340993108715 ) ) ;
#6526=CARTESIAN_POINT ( 'NONE',  ( 19.99999999999999645, -4.046291478462229030, 5.186098161460289901 ) ) ;
#6530=CARTESIAN_POINT ( 'NONE',  ( -10.00000000000000178, 0.000000000000000000, 0.000000000000000000 ) ) ;
#6531=CARTESIAN_POINT ( 'NONE',  ( 19.99999999999999645, -4.046291478462170410, -5.186098161460359179 ) ) ;
#6532=DIRECTION ( 'NONE',  ( -1.000000000000000000, 1.010728034814421376E-30, 1.090846720500930387E-30 ) ) ;
#6537=VECTOR ( 'NONE', #908, 1000.000000000000000 ) ;
#6540=ORIENTED_EDGE ( 'NONE', *, *, #916, .F. ) ;
#6542=VERTEX_POINT ( 'NONE', #9251 ) ;
#6544=CARTESIAN_POINT ( 'NONE',  ( 19.99999999999999645, 0.000000000000000000, 0.000000000000000000 ) ) ;
#6547=FACE_OUTER_BOUND ( 'NONE', #2259, .T. ) ;
#6550=DIRECTION ( 'NONE',  ( -1.000000000000000000, 1.010728034814421376E-30, 1.090846720500930387E-30 ) ) ;
#6552=VERTEX_POINT ( 'NONE', #134 ) ;
#6557=ORIENTED_EDGE ( 'NONE', *, *, #7796, .F. ) ;
#6559=CARTESIAN_POINT ( 'NONE',  ( 0.000000000000000000, 1.764426149628130602, 7.186570834724196111 ) ) ;
#6563=DIRECTION ( 'NONE',  ( 0.000000000000000000, 0.000000000000000000, 1.000000000000000000 ) ) ;
#6565=CARTESIAN_POINT ( 'NONE',  ( 0.000000000000000000, -3.426907987218776430, -5.522074125465566752 ) ) ;
#6570=CARTESIAN_POINT ( 'NONE',  ( 19.99999999999997868, 1.395418990828298567, -6.428133065596409068 ) ) ;
#6572=ORIENTED_EDGE ( 'NONE', *, *, #3364, .T. ) ;
#6573=DIRECTION ( 'NONE',  ( 0.000000000000000000, 0.000000000000000000, 1.000000000000000000 ) ) ;
#6577=CIRCLE ( 'NONE', #2460, 2.800000000000004263 ) ;
#6578=VECTOR ( 'NONE', #11329, 1000.000000000000000 ) ;
#6581=FACE_OUTER_BOUND ( 'NONE', #7091, .T. ) ;
#6582=CIRCLE ( 'NONE', #783, 2.800000000000003819 ) ;
#6583=DIRECTION ( 'NONE',  ( 1.000000000000000000, -1.010728034814421376E-30, -1.090846720500930387E-30 ) ) ;
#6590=DIRECTION ( 'NONE',  ( -9.737501798821850460E-31, 0.9909497617679351444, -0.1342332658176521587 ) ) ;
#6593=DIRECTION ( 'NONE',  ( -3.266377185680748504E-31, 0.8805955318567392220, -0.4738686624729965824 ) ) ;
#6594=LINE ( 'NONE', #2675, #11051 ) ;
#6596=DIRECTION ( 'NONE',  ( 0.000000000000000000, 0.000000000000000000, 1.000000000000000000 ) ) ;
#6597=AXIS2_PLACEMENT_3D ( 'NONE', #2560, #9418, #6485 ) ;
#6599=AXIS2_PLACEMENT_3D ( 'NONE', #8706, #2989, #1030 ) ;
#6600=CARTESIAN_POINT ( 'NONE',  ( 0.000000000000000000, -6.133480037816475772, -2.376659734729558160 ) ) ;
#6603=UNCERTAINTY_MEASURE_WITH_UNIT (LENGTH_MEASURE( 1.000000000000000082E-05 ), #1565, 'distance_accuracy_value', 'NONE');
#6604=EDGE_CURVE ( 'NONE', #10994, #6460, #2154, .T. ) ;
#6605=CARTESIAN_POINT ( 'NONE',  ( 19.99999999999999645, 0.000000000000000000, 0.000000000000000000 ) ) ;
#6606=ORIENTED_EDGE ( 'NONE', *, *, #10578, .F. ) ;
#6607=ORIENTED_EDGE ( 'NONE', *, *, #9917, .T. ) ;
#6610=DIRECTION ( 'NONE',  ( -1.000000000000000000, 1.010728034814421376E-30, 1.090846720500930387E-30 ) ) ;
#6616=DIRECTION ( 'NONE',  ( -1.000000000000000000, 1.010728034814421376E-30, 1.090846720500930387E-30 ) ) ;
#6622=VERTEX_POINT ( 'NONE', #5465 ) ;
#6623=ORIENTED_EDGE ( 'NONE', *, *, #8111, .T. ) ;
#6625=CARTESIAN_POINT ( 'NONE',  ( 19.99999999999997868, -0.8135880386782390339, -6.527339685683426929 ) ) ;
#6626=VERTEX_POINT ( 'NONE', #9373 ) ;
#6632=DIRECTION ( 'NONE',  ( 1.140150527077241873E-30, 0.000000000000000000, -1.000000000000000000 ) ) ;
#6636=VERTEX_POINT ( 'NONE', #12494 ) ;
#6637=CIRCLE ( 'NONE', #4363, 2.800000000000003819 ) ;
#6649=ORIENTED_EDGE ( 'NONE', *, *, #5855, .T. ) ;
#6654=CIRCLE ( 'NONE', #1904, 6.499000000000008548 ) ;
#6658=LINE ( 'NONE', #13, #3743 ) ;
#6659=FACE_OUTER_BOUND ( 'NONE', #745, .T. ) ;
#6661=CARTESIAN_POINT ( 'NONE',  ( 19.99999999999999645, -5.932103089875941038, 2.654647609586679113 ) ) ;
#6662=DIRECTION ( 'NONE',  ( -1.380506584136768733E-30, 0.4338837391175525693, 0.9009688679024219216 ) ) ;
#6666=CARTESIAN_POINT ( 'NONE',  ( 19.99999999999997868, 2.649444137877677186, -6.020675595748665287 ) ) ;
#6667=VERTEX_POINT ( 'NONE', #756 ) ;
#6669=EDGE_LOOP ( 'NONE', ( #12670, #3714, #12419, #3719 ) ) ;
#6670=ORIENTED_EDGE ( 'NONE', *, *, #12134, .T. ) ;
#6671=DIRECTION ( 'NONE',  ( -1.000000000000000000, 1.010728034814421376E-30, 1.090846720500930387E-30 ) ) ;
#6672=DIRECTION ( 'NONE',  ( -1.000000000000000000, 1.010728034814421376E-30, 1.090846720500930387E-30 ) ) ;
#6674=CARTESIAN_POINT ( 'NONE',  ( 19.99999999999999645, -6.182645281642477286, -2.245659411033190445 ) ) ;
#6676=ADVANCED_FACE ( 'NONE', ( #2844 ), #1786, .T. ) ;
#6677=CARTESIAN_POINT ( 'NONE',  ( 9.999999999999998224, -2.401522331692811818, -6.999477872697428715 ) ) ;
#6681=ORIENTED_EDGE ( 'NONE', *, *, #894, .F. ) ;
#6683=EDGE_LOOP ( 'NONE', ( #823, #11143, #2947, #11222 ) ) ;
#6685=EDGE_CURVE ( 'NONE', #4490, #9929, #3411, .T. ) ;
#6688=DIRECTION ( 'NONE',  ( -1.000000000000000000, 1.010728034814421376E-30, 1.090846720500930387E-30 ) ) ;
#6689=ORIENTED_EDGE ( 'NONE', *, *, #8242, .F. ) ;
#6690=EDGE_CURVE ( 'NONE', #5492, #11154, #12035, .T. ) ;
#6693=ORIENTED_EDGE ( 'NONE', *, *, #12515, .T. ) ;
#6695=ADVANCED_FACE ( 'NONE', ( #2577 ), #7653, .T. ) ;
#6699=ORIENTED_EDGE ( 'NONE', *, *, #2647, .F. ) ;
#6700=CYLINDRICAL_SURFACE ( 'NONE', #5400, 2.800000000000003819 ) ;
#6704=VECTOR ( 'NONE', #9942, 1000.000000000000000 ) ;
#6705=DIRECTION ( 'NONE',  ( -1.000000000000000000, 1.010728034814421376E-30, 1.090846720500930387E-30 ) ) ;
#6707=DIRECTION ( 'NONE',  ( -1.140150527077241873E-30, 0.000000000000000000, 1.000000000000000000 ) ) ;
#6712=ORIENTED_EDGE ( 'NONE', *, *, #11725, .F. ) ;
#6718=DIRECTION ( 'NONE',  ( 0.000000000000000000, 0.000000000000000000, 1.000000000000000000 ) ) ;
#6719=CARTESIAN_POINT ( 'NONE',  ( -10.00000000000000178, 0.000000000000000000, 0.000000000000000000 ) ) ;
#6721=EDGE_CURVE ( 'NONE', #3292, #9808, #6895, .T. ) ;
#6723=LINE ( 'NONE', #10445, #2988 ) ;
#6724=CARTESIAN_POINT ( 'NONE',  ( 19.99999999999999645, 0.000000000000000000, 0.000000000000000000 ) ) ;
#6725=AXIS2_PLACEMENT_3D ( 'NONE', #9294, #485, #2496 ) ;
#6727=DIRECTION ( 'NONE',  ( -1.000000000000000000, 1.010728034814421376E-30, 1.090846720500930387E-30 ) ) ;
#6731=DIRECTION ( 'NONE',  ( 0.000000000000000000, 0.000000000000000000, 1.000000000000000000 ) ) ;
#6732=CARTESIAN_POINT ( 'NONE',  ( -10.00000000000000178, 0.000000000000000000, 0.000000000000000000 ) ) ;
#6733=CIRCLE ( 'NONE', #10415, 2.800000000000002043 ) ;
#6734=CARTESIAN_POINT ( 'NONE',  ( 19.99999999999999645, -5.932103089875909951, -2.654647609586772816 ) ) ;
#6736=AXIS2_PLACEMENT_3D ( 'NONE', #12205, #4268, #2348 ) ;
#6740=VERTEX_POINT ( 'NONE', #11526 ) ;
#6742=CARTESIAN_POINT ( 'NONE',  ( 19.99999999999997868, 6.544726022087268724, -0.6592800351836389794 ) ) ;
#6743=EDGE_LOOP ( 'NONE', ( #4407, #10089, #6335, #4044 ) ) ;
#6744=ORIENTED_EDGE ( 'NONE', *, *, #9688, .F. ) ;
#6750=ORIENTED_EDGE ( 'NONE', *, *, #10964, .T. ) ;
#6753=EDGE_CURVE ( 'NONE', #11058, #8301, #2996, .T. ) ;
#6757=ORIENTED_EDGE ( 'NONE', *, *, #4894, .F. ) ;
#6758=DIRECTION ( 'NONE',  ( -1.000000000000000000, 1.010728034814421376E-30, 1.090846720500930387E-30 ) ) ;
#6760=ORIENTED_EDGE ( 'NONE', *, *, #7518, .T. ) ;
#6763=ORIENTED_EDGE ( 'NONE', *, *, #8875, .T. ) ;
#6765=EDGE_CURVE ( 'NONE', #6626, #1327, #10580, .T. ) ;
#6770=CIRCLE ( 'NONE', #5529, 6.499000000000009436 ) ;
#6777=AXIS2_PLACEMENT_3D ( 'NONE', #57, #8687, #2916 ) ;
#6779=CARTESIAN_POINT ( 'NONE',  ( 19.99999999999997868, -1.268072931708450257, -6.374087545670231947 ) ) ;
#6780=DIRECTION ( 'NONE',  ( -1.000000000000000000, 1.010728034814421376E-30, 1.090846720500930387E-30 ) ) ;
#6782=LINE ( 'NONE', #10817, #9384 ) ;
#6785=DIRECTION ( 'NONE',  ( 0.000000000000000000, -0.9510565162951500895, -0.3090169943749582759 ) ) ;
#6788=VECTOR ( 'NONE', #4183, 1000.000000000000000 ) ;
#6790=AXIS2_PLACEMENT_3D ( 'NONE', #1841, #9807, #7709 ) ;
#6792=ADVANCED_FACE ( 'NONE', ( #1136 ), #4945, .T. ) ;
#6793=VERTEX_POINT ( 'NONE', #5905 ) ;
#6795=DIRECTION ( 'NONE',  ( -1.000000000000000000, 1.010728034814421376E-30, 1.090846720500930387E-30 ) ) ;
#6796=AXIS2_PLACEMENT_3D ( 'NONE', #1709, #5635, #2626 ) ;
#6800=CIRCLE ( 'NONE', #7000, 2.800000000000003375 ) ;
#6802=EDGE_LOOP ( 'NONE', ( #10083, #12703, #2024, #3094 ) ) ;
#6805=LINE ( 'NONE', #9485, #2063 ) ;
#6806=ORIENTED_EDGE ( 'NONE', *, *, #8317, .F. ) ;
#6813=ADVANCED_FACE ( 'NONE', ( #2907 ), #9815, .T. ) ;
#6814=EDGE_CURVE ( 'NONE', #9943, #490, #6061, .T. ) ;
#6815=DIRECTION ( 'NONE',  ( -1.000000000000000000, 1.010728034814421376E-30, 1.090846720500930387E-30 ) ) ;
#6816=EDGE_CURVE ( 'NONE', #6322, #7420, #514, .T. ) ;
#6817=EDGE_LOOP ( 'NONE', ( #7221, #4545, #544, #2983 ) ) ;
#6820=VERTEX_POINT ( 'NONE', #2175 ) ;
#6822=DIRECTION ( 'NONE',  ( 0.000000000000000000, 0.000000000000000000, 1.000000000000000000 ) ) ;
#6824=ORIENTED_EDGE ( 'NONE', *, *, #10672, .T. ) ;
#6827=AXIS2_PLACEMENT_3D ( 'NONE', #6472, #12337, #2612 ) ;
#6829=VERTEX_POINT ( 'NONE', #3916 ) ;
#6830=DIRECTION ( 'NONE',  ( 9.367723249499501176E-31, -0.9989930665413151445, 0.04486483035050446017 ) ) ;
#6833=AXIS2_PLACEMENT_3D ( 'NONE', #11475, #7415, #3621 ) ;
#6834=EDGE_CURVE ( 'NONE', #8908, #1778, #9342, .T. ) ;
#6839=ORIENTED_EDGE ( 'NONE', *, *, #11467, .T. ) ;
#6840=CYLINDRICAL_SURFACE ( 'NONE', #10493, 2.800000000000003819 ) ;
#6844=DIRECTION ( 'NONE',  ( -1.000000000000000000, 1.010728034814421376E-30, 1.090846720500930387E-30 ) ) ;
#6845=CIRCLE ( 'NONE', #4988, 6.499000000000009436 ) ;
#6848=CARTESIAN_POINT ( 'NONE',  ( 19.99999999999997868, 4.494880553659097444, -4.802513683199186367 ) ) ;
#6850=CARTESIAN_POINT ( 'NONE',  ( 19.99999999999999645, -1.268072931708538853, 6.374087545670210631 ) ) ;
#6851=DIRECTION ( 'NONE',  ( 1.140150527077241873E-30, 0.000000000000000000, -1.000000000000000000 ) ) ;
#6853=CIRCLE ( 'NONE', #1284, 2.800000000000004263 ) ;
#6858=CARTESIAN_POINT ( 'NONE',  ( 0.000000000000000000, 0.2252065540229633012, 6.573992004634855668 ) ) ;
#6862=LINE ( 'NONE', #6734, #10188 ) ;
#6867=CARTESIAN_POINT ( 'NONE',  ( 19.99999999999999645, 3.908107171477180675, 5.192658214849959819 ) ) ;
#6868=ORIENTED_EDGE ( 'NONE', *, *, #2224, .F. ) ;
#6875=CARTESIAN_POINT ( 'NONE',  ( 19.99999999999999645, -5.362766118793865111, 3.671204237728611819 ) ) ;
#6878=DIRECTION ( 'NONE',  ( -1.000000000000000000, 1.010728034814421376E-30, 1.090846720500930387E-30 ) ) ;
#6879=ORIENTED_EDGE ( 'NONE', *, *, #12643, .T. ) ;
#6883=EDGE_CURVE ( 'NONE', #490, #11656, #10988, .T. ) ;
#6885=CIRCLE ( 'NONE', #7084, 6.499000000000008548 ) ;
#6887=ORIENTED_EDGE ( 'NONE', *, *, #4790, .T. ) ;
#6888=EDGE_LOOP ( 'NONE', ( #10544, #8403, #2436, #523 ) ) ;
#6892=CARTESIAN_POINT ( 'NONE',  ( 19.99999999999999645, 0.000000000000000000, 0.000000000000000000 ) ) ;
#6893=ORIENTED_EDGE ( 'NONE', *, *, #8723, .F. ) ;
#6894=VECTOR ( 'NONE', #6382, 1000.000000000000000 ) ;
#6895=CIRCLE ( 'NONE', #1326, 7.400000000000011902 ) ;
#6900=VERTEX_POINT ( 'NONE', #1068 ) ;
#6903=EDGE_LOOP ( 'NONE', ( #379, #4517, #5453, #7913 ) ) ;
#6904=AXIS2_PLACEMENT_3D ( 'NONE', #4674, #9482, #9416 ) ;
#6905=CYLINDRICAL_SURFACE ( 'NONE', #4161, 7.400000000000010125 ) ;
#6906=LINE ( 'NONE', #12, #11325 ) ;
#6907=DIRECTION ( 'NONE',  ( 1.000000000000000000, -1.010728034814421376E-30, -1.090846720500930387E-30 ) ) ;
#6908=CYLINDRICAL_SURFACE ( 'NONE', #6313, 7.400000000000010125 ) ;
#6909=DIRECTION ( 'NONE',  ( -1.000000000000000000, 1.010728034814421376E-30, 1.090846720500930387E-30 ) ) ;
#6911=EDGE_CURVE ( 'NONE', #11649, #6322, #5006, .T. ) ;
#6913=EDGE_CURVE ( 'NONE', #5654, #7331, #3089, .T. ) ;
#6916=CARTESIAN_POINT ( 'NONE',  ( 19.99999999999997868, 4.772487208025196992, -4.411390579991299354 ) ) ;
#6919=AXIS2_PLACEMENT_3D ( 'NONE', #3374, #7291, #8182 ) ;
#6926=ORIENTED_EDGE ( 'NONE', *, *, #143, .F. ) ;
#6929=DIRECTION ( 'NONE',  ( 1.000000000000000000, -1.010728034814421376E-30, 1.140150527077241873E-30 ) ) ;
#6931=DIRECTION ( 'NONE',  ( -1.000000000000000000, 1.010728034814421376E-30, 1.090846720500930387E-30 ) ) ;
#6932=ORIENTED_EDGE ( 'NONE', *, *, #4358, .F. ) ;
#6933=ORIENTED_EDGE ( 'NONE', *, *, #8130, .F. ) ;
#6937=FACE_OUTER_BOUND ( 'NONE', #10793, .T. ) ;
#6939=AXIS2_PLACEMENT_3D ( 'NONE', #3572, #7550, #7368 ) ;
#6942=DIRECTION ( 'NONE',  ( -1.000000000000000000, 1.010728034814421376E-30, 1.090846720500930387E-30 ) ) ;
#6943=ORIENTED_EDGE ( 'NONE', *, *, #11083, .F. ) ;
#6948=CIRCLE ( 'NONE', #12714, 6.499000000000008548 ) ;
#6949=ORIENTED_EDGE ( 'NONE', *, *, #2005, .T. ) ;
#6953=ORIENTED_EDGE ( 'NONE', *, *, #6911, .T. ) ;
#6955=ORIENTED_EDGE ( 'NONE', *, *, #1559, .F. ) ;
#6956=DIRECTION ( 'NONE',  ( -1.000000000000000000, 1.010728034814421376E-30, 1.090846720500930387E-30 ) ) ;
#6959=LINE ( 'NONE', #12702, #8198 ) ;
#6961=LINE ( 'NONE', #1930, #7258 ) ;
#6963=EDGE_CURVE ( 'NONE', #6343, #6000, #3469, .T. ) ;
#6967=CARTESIAN_POINT ( 'NONE',  ( 0.000000000000000000, 0.000000000000000000, 0.000000000000000000 ) ) ;
#6968=CARTESIAN_POINT ( 'NONE',  ( 0.000000000000000000, -6.289597356626510205, 3.898841506334508988 ) ) ;
#6976=CIRCLE ( 'NONE', #4092, 2.800000000000003819 ) ;
#6982=DIRECTION ( 'NONE',  ( -1.000000000000000000, 1.010728034814421376E-30, 1.090846720500930387E-30 ) ) ;
#6984=CARTESIAN_POINT ( 'NONE',  ( 19.99999999999997868, 6.424561140605085541, 0.9808237102697028309 ) ) ;
#6992=VERTEX_POINT ( 'NONE', #11313 ) ;
#6994=ORIENTED_EDGE ( 'NONE', *, *, #4503, .F. ) ;
#6997=FACE_OUTER_BOUND ( 'NONE', #2973, .T. ) ;
#6999=EDGE_LOOP ( 'NONE', ( #1761, #5146, #8028, #1392 ) ) ;
#7000=AXIS2_PLACEMENT_3D ( 'NONE', #7740, #9652, #4970 ) ;
#7004=CYLINDRICAL_SURFACE ( 'NONE', #8293, 6.499000000000010324 ) ;
#7008=CARTESIAN_POINT ( 'NONE',  ( 19.99999999999999645, 0.000000000000000000, 0.000000000000000000 ) ) ;
#7013=ORIENTED_EDGE ( 'NONE', *, *, #9055, .T. ) ;
#7014=CARTESIAN_POINT ( 'NONE',  ( 0.000000000000000000, 6.359534927042326480, -1.339147681075104845 ) ) ;
#7015=ADVANCED_FACE ( 'NONE', ( #10258 ), #1514, .T. ) ;
#7017=ORIENTED_EDGE ( 'NONE', *, *, #7999, .F. ) ;
#7021=DIRECTION ( 'NONE',  ( 0.000000000000000000, 0.9510565162951545304, -0.3090169943749445092 ) ) ;
#7023=CARTESIAN_POINT ( 'NONE',  ( 19.99999999999999645, 0.000000000000000000, 0.000000000000000000 ) ) ;
#7024=LINE ( 'NONE', #9003, #2691 ) ;
#7029=FACE_OUTER_BOUND ( 'NONE', #5009, .T. ) ;
#7032=CIRCLE ( 'NONE', #5788, 2.800000000000003819 ) ;
#7036=EDGE_CURVE ( 'NONE', #5894, #11074, #7318, .T. ) ;
#7045=DIRECTION ( 'NONE',  ( -1.000000000000000000, 1.010728034814421376E-30, 1.090846720500930387E-30 ) ) ;
#7047=CARTESIAN_POINT ( 'NONE',  ( 0.000000000000000000, 0.000000000000000000, 0.000000000000000000 ) ) ;
#7049=DIRECTION ( 'NONE',  ( 1.140150527077241873E-30, 0.000000000000000000, -1.000000000000000000 ) ) ;
#7050=CIRCLE ( 'NONE', #7060, 2.800000000000004263 ) ;
#7054=ORIENTED_EDGE ( 'NONE', *, *, #3531, .T. ) ;
#7055=CARTESIAN_POINT ( 'NONE',  ( -10.00000000000000178, 0.000000000000000000, 0.000000000000000000 ) ) ;
#7057=CIRCLE ( 'NONE', #882, 7.400000000000011902 ) ;
#7060=AXIS2_PLACEMENT_3D ( 'NONE', #6570, #12438, #827 ) ;
#7062=VERTEX_POINT ( 'NONE', #7568 ) ;
#7063=DIRECTION ( 'NONE',  ( -1.000000000000000000, 1.010728034814421376E-30, 1.090846720500930387E-30 ) ) ;
#7064=VERTEX_POINT ( 'NONE', #10459 ) ;
#7069=CIRCLE ( 'NONE', #11174, 2.800000000000003819 ) ;
#7074=EDGE_CURVE ( 'NONE', #3160, #4761, #4553, .T. ) ;
#7075=ORIENTED_EDGE ( 'NONE', *, *, #4910, .T. ) ;
#7076=CARTESIAN_POINT ( 'NONE',  ( 19.99999999999999645, 1.528443194675403349, 7.240432404259460775 ) ) ;
#7080=ADVANCED_FACE ( 'NONE', ( #797 ), #8532, .T. ) ;
#7083=CARTESIAN_POINT ( 'NONE',  ( 0.000000000000000000, -4.707829255731177831, -5.709320773864598131 ) ) ;
#7084=AXIS2_PLACEMENT_3D ( 'NONE', #6328, #4211, #8264 ) ;
#7086=CIRCLE ( 'NONE', #3392, 2.800000000000002487 ) ;
#7088=DIRECTION ( 'NONE',  ( 0.000000000000000000, 0.000000000000000000, 1.000000000000000000 ) ) ;
#7089=EDGE_LOOP ( 'NONE', ( #3643, #3612, #3229, #3049 ) ) ;
#7091=EDGE_LOOP ( 'NONE', ( #9423, #11226, #949, #6693 ) ) ;
#7092=DIRECTION ( 'NONE',  ( 1.000000000000000000, -1.010728034814421376E-30, -1.090846720500930387E-30 ) ) ;
#7093=AXIS2_PLACEMENT_3D ( 'NONE', #8375, #12314, #2463 ) ;
#7094=FILL_AREA_STYLE ('',( #9774 ) ) ;
#7100=AXIS2_PLACEMENT_3D ( 'NONE', #3238, #11335, #9504 ) ;
#7105=AXIS2_PLACEMENT_3D ( 'NONE', #6503, #1598, #12304 ) ;
#7112=FACE_OUTER_BOUND ( 'NONE', #6051, .T. ) ;
#7114=DIRECTION ( 'NONE',  ( -1.000000000000000000, 1.010728034814421376E-30, 1.090846720500930387E-30 ) ) ;
#7119=CARTESIAN_POINT ( 'NONE',  ( 19.99999999999999645, 0.000000000000000000, 0.000000000000000000 ) ) ;
#7120=ORIENTED_EDGE ( 'NONE', *, *, #5924, .F. ) ;
#7121=ORIENTED_EDGE ( 'NONE', *, *, #2864, .F. ) ;
#7126=ADVANCED_FACE ( 'NONE', ( #10393 ), #9356, .T. ) ;
#7127=FACE_OUTER_BOUND ( 'NONE', #10873, .T. ) ;
#7129=ORIENTED_EDGE ( 'NONE', *, *, #6690, .T. ) ;
#7132=CIRCLE ( 'NONE', #2836, 6.499000000000008548 ) ;
#7139=DIRECTION ( 'NONE',  ( 0.000000000000000000, 0.000000000000000000, 1.000000000000000000 ) ) ;
#7146=ADVANCED_FACE ( 'NONE', ( #7506 ), #3528, .T. ) ;
#7147=CYLINDRICAL_SURFACE ( 'NONE', #3184, 2.800000000000003819 ) ;
#7149=ADVANCED_FACE ( 'NONE', ( #739 ), #1579, .T. ) ;
#7152=DIRECTION ( 'NONE',  ( -1.417484439069003486E-30, 0.9195277725514489076, 0.3930250316539278255 ) ) ;
#7155=VERTEX_POINT ( 'NONE', #2824 ) ;
#7161=EDGE_CURVE ( 'NONE', #10498, #9362, #2763, .T. ) ;
#7163=EDGE_CURVE ( 'NONE', #3101, #992, #6068, .T. ) ;
#7166=DIRECTION ( 'NONE',  ( -1.000000000000000000, 1.010728034814421376E-30, 1.090846720500930387E-30 ) ) ;
#7168=DIRECTION ( 'NONE',  ( 0.000000000000000000, 0.000000000000000000, 1.000000000000000000 ) ) ;
#7169=VERTEX_POINT ( 'NONE', #6984 ) ;
#7170=DIRECTION ( 'NONE',  ( 0.000000000000000000, 0.5877852522924684742, 0.8090169943749507819 ) ) ;
#7171=CARTESIAN_POINT ( 'NONE',  ( 0.000000000000000000, -6.459281472512953037, 1.243290685169352816 ) ) ;
#7174=CARTESIAN_POINT ( 'NONE',  ( 19.99999999999997868, 6.544726022087254513, 0.6592800351837256878 ) ) ;
#7177=CARTESIAN_POINT ( 'NONE',  ( 19.99999999999999645, 0.000000000000000000, 0.000000000000000000 ) ) ;
#7180=DIRECTION ( 'NONE',  ( 0.000000000000000000, 0.000000000000000000, 1.000000000000000000 ) ) ;
#7181=AXIS2_PLACEMENT_3D ( 'NONE', #6742, #12479, #9741 ) ;
#7183=DIRECTION ( 'NONE',  ( 1.140150527077241873E-30, 0.000000000000000000, -1.000000000000000000 ) ) ;
#7184=ORIENTED_EDGE ( 'NONE', *, *, #12679, .F. ) ;
#7188=CARTESIAN_POINT ( 'NONE',  ( 20.00000000000000000, 0.000000000000000000, 0.000000000000000000 ) ) ;
#7193=CIRCLE ( 'NONE', #1629, 2.800000000000004263 ) ;
#7197=CARTESIAN_POINT ( 'NONE',  ( -10.00000000000000178, 0.000000000000000000, 0.000000000000000000 ) ) ;
#7198=ORIENTED_EDGE ( 'NONE', *, *, #65, .T. ) ;
#7201=ORIENTED_EDGE ( 'NONE', *, *, #5800, .T. ) ;
#7202=CIRCLE ( 'NONE', #195, 2.800000000000002931 ) ;
#7206=CIRCLE ( 'NONE', #3322, 7.400000000000009237 ) ;
#7211=EDGE_LOOP ( 'NONE', ( #5275, #7406, #1521, #2766 ) ) ;
#7212=DIRECTION ( 'NONE',  ( -1.000000000000000000, 1.010728034814421376E-30, 1.090846720500930387E-30 ) ) ;
#7213=ORIENTED_EDGE ( 'NONE', *, *, #7611, .F. ) ;
#7214=DIRECTION ( 'NONE',  ( 0.000000000000000000, 0.9909497617679351444, -0.1342332658176521587 ) ) ;
#7220=CYLINDRICAL_SURFACE ( 'NONE', #5138, 6.499000000000010324 ) ;
#7221=ORIENTED_EDGE ( 'NONE', *, *, #11619, .T. ) ;
#7227=CARTESIAN_POINT ( 'NONE',  ( 19.99999999999997868, 5.280167904461786854, -3.922743398397314341 ) ) ;
#7228=DIRECTION ( 'NONE',  ( -1.000000000000000000, 1.010728034814421376E-30, 1.090846720500930387E-30 ) ) ;
#7229=EDGE_CURVE ( 'NONE', #12171, #5751, #7824, .T. ) ;
#7234=VERTEX_POINT ( 'NONE', #8904 ) ;
#7235=CARTESIAN_POINT ( 'NONE',  ( 19.99999999999997868, 5.956456411769428527, -2.790827096698922372 ) ) ;
#7236=EDGE_CURVE ( 'NONE', #11879, #6259, #5054, .T. ) ;
#7238=ADVANCED_FACE ( 'NONE', ( #90 ), #3955, .T. ) ;
#7240=ORIENTED_EDGE ( 'NONE', *, *, #2280, .F. ) ;
#7241=LINE ( 'NONE', #1173, #3159 ) ;
#7243=CARTESIAN_POINT ( 'NONE',  ( 19.99999999999997868, 6.359534927042317598, 1.339147681075194996 ) ) ;
#7247=AXIS2_PLACEMENT_3D ( 'NONE', #8181, #1222, #3116 ) ;
#7250=ORIENTED_EDGE ( 'NONE', *, *, #8875, .F. ) ;
#7253=EDGE_LOOP ( 'NONE', ( #10594, #1769, #8606, #7129 ) ) ;
#7254=ORIENTED_EDGE ( 'NONE', *, *, #8694, .F. ) ;
#7255=DIRECTION ( 'NONE',  ( -1.000000000000000000, 1.010728034814421376E-30, 1.090846720500930387E-30 ) ) ;
#7258=VECTOR ( 'NONE', #10874, 1000.000000000000000 ) ;
#7259=CYLINDRICAL_SURFACE ( 'NONE', #4450, 2.800000000000003819 ) ;
#7267=CIRCLE ( 'NONE', #9698, 2.800000000000004263 ) ;
#7269=AXIS2_PLACEMENT_3D ( 'NONE', #12627, #2786, #5656 ) ;
#7277=EDGE_CURVE ( 'NONE', #3589, #7374, #3429, .T. ) ;
#7280=CARTESIAN_POINT ( 'NONE',  ( 0.000000000000000000, 7.380072687735796499, -0.5427035320837090282 ) ) ;
#7281=CARTESIAN_POINT ( 'NONE',  ( 19.99999999999999645, 1.052479792859053020, 6.413211932068313637 ) ) ;
#7291=DIRECTION ( 'NONE',  ( -1.000000000000000000, 1.010728034814421376E-30, 1.090846720500930387E-30 ) ) ;
#7293=CYLINDRICAL_SURFACE ( 'NONE', #7798, 2.800000000000003819 ) ;
#7294=ORIENTED_EDGE ( 'NONE', *, *, #9146, .T. ) ;
#7295=DIRECTION ( 'NONE',  ( 0.000000000000000000, -0.5128992774058948045, -0.8584487936018728726 ) ) ;
#7297=CARTESIAN_POINT ( 'NONE',  ( 19.99999999999999645, -6.577476285968334224, -0.06996125000500313940 ) ) ;
#7301=DIRECTION ( 'NONE',  ( 0.000000000000000000, 0.000000000000000000, 1.000000000000000000 ) ) ;
#7302=VECTOR ( 'NONE', #7418, 1000.000000000000000 ) ;
#7304=ADVANCED_FACE ( 'NONE', ( #12667 ), #9095, .T. ) ;
#7306=AXIS2_PLACEMENT_3D ( 'NONE', #6237, #374, #10883 ) ;
#7308=EDGE_CURVE ( 'NONE', #2771, #9874, #1762, .T. ) ;
#7309=AXIS2_PLACEMENT_3D ( 'NONE', #516, #12382, #4382 ) ;
#7311=ORIENTED_EDGE ( 'NONE', *, *, #1595, .T. ) ;
#7313=CARTESIAN_POINT ( 'NONE',  ( 19.99999999999997868, 7.100173756228414845, 2.085073771204572157 ) ) ;
#7318=CIRCLE ( 'NONE', #12048, 6.499000000000009436 ) ;
#7324=ORIENTED_EDGE ( 'NONE', *, *, #3180, .F. ) ;
#7326=AXIS2_PLACEMENT_3D ( 'NONE', #7177, #5114, #2351 ) ;
#7327=CARTESIAN_POINT ( 'NONE',  ( 19.99999999999999645, 3.019282868015074506, 6.756029230465976809 ) ) ;
#7331=VERTEX_POINT ( 'NONE', #9156 ) ;
#7332=DIRECTION ( 'NONE',  ( 1.140150527077241873E-30, 0.000000000000000000, -1.000000000000000000 ) ) ;
#7336=CARTESIAN_POINT ( 'NONE',  ( 0.000000000000000000, 1.834336845376708602, 6.234758161925244124 ) ) ;
#7337=ORIENTED_EDGE ( 'NONE', *, *, #6247, .T. ) ;
#7338=DIRECTION ( 'NONE',  ( 0.000000000000000000, 0.5128992774059070170, -0.8584487936018656562 ) ) ;
#7339=LINE ( 'NONE', #2069, #5651 ) ;
#7343=CARTESIAN_POINT ( 'NONE',  ( 19.99999999999999645, 0.000000000000000000, 0.000000000000000000 ) ) ;
#7350=AXIS2_PLACEMENT_3D ( 'NONE', #5112, #8126, #2218 ) ;
#7352=AXIS2_PLACEMENT_3D ( 'NONE', #846, #2992, #3938 ) ;
#7354=DIRECTION ( 'NONE',  ( 1.140150527077241873E-30, 0.000000000000000000, -1.000000000000000000 ) ) ;
#7357=DIRECTION ( 'NONE',  ( 1.140150527077241873E-30, 0.000000000000000000, -1.000000000000000000 ) ) ;
#7360=CARTESIAN_POINT ( 'NONE',  ( 0.000000000000000000, 5.012092988314003073, -4.137139697483478429 ) ) ;
#7366=FACE_OUTER_BOUND ( 'NONE', #6802, .T. ) ;
#7367=DIRECTION ( 'NONE',  ( -1.000000000000000000, 1.010728034814421376E-30, 1.090846720500930387E-30 ) ) ;
#7368=DIRECTION ( 'NONE',  ( 5.115269932292490543E-31, -0.9195277725514543476, 0.3930250316539146693 ) ) ;
#7370=CARTESIAN_POINT ( 'NONE',  ( 0.000000000000000000, 3.565124043461764813, -5.527927226701604191 ) ) ;
#7374=VERTEX_POINT ( 'NONE', #11034 ) ;
#7376=ORIENTED_EDGE ( 'NONE', *, *, #12431, .F. ) ;
#7377=VERTEX_POINT ( 'NONE', #3202 ) ;
#7379=CARTESIAN_POINT ( 'NONE',  ( 0.000000000000000000, 0.000000000000000000, 0.000000000000000000 ) ) ;
#7386=CARTESIAN_POINT ( 'NONE',  ( 0.000000000000000000, -7.399010254356644722, 0.1210258481698957278 ) ) ;
#7387=VERTEX_POINT ( 'NONE', #1180 ) ;
#7392=DIRECTION ( 'NONE',  ( 0.000000000000000000, 0.000000000000000000, 1.000000000000000000 ) ) ;
#7393=ADVANCED_FACE ( 'NONE', ( #8129 ), #3266, .T. ) ;
#7394=CIRCLE ( 'NONE', #5737, 6.499000000000009436 ) ;
#7396=EDGE_LOOP ( 'NONE', ( #8835, #6649, #7812, #807 ) ) ;
#7397=CARTESIAN_POINT ( 'NONE',  ( 9.999999999999980460, -3.612733913993546597, -6.458185013351741333 ) ) ;
#7400=CARTESIAN_POINT ( 'NONE',  ( 9.999999999999998224, 6.057062246029580876, -4.251117141143418543 ) ) ;
#7406=ORIENTED_EDGE ( 'NONE', *, *, #7518, .F. ) ;
#7409=CARTESIAN_POINT ( 'NONE',  ( 9.999999999999998224, 7.358375340956999189, 0.7837807994561865055 ) ) ;
#7411=DIRECTION ( 'NONE',  ( 0.000000000000000000, 0.000000000000000000, 1.000000000000000000 ) ) ;
#7413=CIRCLE ( 'NONE', #7609, 2.800000000000002931 ) ;
#7414=AXIS2_PLACEMENT_3D ( 'NONE', #2865, #7860, #3051 ) ;
#7415=DIRECTION ( 'NONE',  ( -1.000000000000000000, 1.010728034814421376E-30, 1.090846720500930387E-30 ) ) ;
#7418=DIRECTION ( 'NONE',  ( -1.000000000000000000, 1.010728034814421376E-30, 1.090846720500930387E-30 ) ) ;
#7419=FACE_OUTER_BOUND ( 'NONE', #12406, .T. ) ;
#7420=VERTEX_POINT ( 'NONE', #1366 ) ;
#7425=CARTESIAN_POINT ( 'NONE',  ( 0.000000000000000000, 0.3649881613860921359, -6.567714405409697420 ) ) ;
#7428=DIRECTION ( 'NONE',  ( 0.000000000000000000, 0.000000000000000000, 1.000000000000000000 ) ) ;
#7429=CARTESIAN_POINT ( 'NONE',  ( -10.00000000000000178, 0.000000000000000000, 0.000000000000000000 ) ) ;
#7433=EDGE_CURVE ( 'NONE', #6622, #4036, #530, .T. ) ;
#7435=PRESENTATION_STYLE_ASSIGNMENT (( #9345 ) ) ;
#7437=VECTOR ( 'NONE', #9723, 1000.000000000000000 ) ;
#7440=ORIENTED_EDGE ( 'NONE', *, *, #9484, .F. ) ;
#7441=DIRECTION ( 'NONE',  ( 1.000000000000000000, -1.010728034814421376E-30, -1.090846720500930387E-30 ) ) ;
#7442=DIRECTION ( 'NONE',  ( -1.000000000000000000, 1.010728034814421376E-30, 1.090846720500930387E-30 ) ) ;
#7447=DIRECTION ( 'NONE',  ( 0.000000000000000000, 0.000000000000000000, 1.000000000000000000 ) ) ;
#7449=CYLINDRICAL_SURFACE ( 'NONE', #6597, 7.400000000000010125 ) ;
#7451=VERTEX_POINT ( 'NONE', #12208 ) ;
#7452=DIRECTION ( 'NONE',  ( 0.000000000000000000, 0.000000000000000000, 1.000000000000000000 ) ) ;
#7455=AXIS2_PLACEMENT_3D ( 'NONE', #3368, #11208, #3430 ) ;
#7461=CARTESIAN_POINT ( 'NONE',  ( 0.000000000000000000, 0.000000000000000000, 0.000000000000000000 ) ) ;
#7462=EDGE_CURVE ( 'NONE', #9064, #2371, #5871, .T. ) ;
#7464=DIRECTION ( 'NONE',  ( 0.000000000000000000, -0.08963930890344089242, 0.9959742939952382912 ) ) ;
#7466=EDGE_CURVE ( 'NONE', #11564, #2762, #11645, .T. ) ;
#7470=DIRECTION ( 'NONE',  ( 0.000000000000000000, 0.000000000000000000, 1.000000000000000000 ) ) ;
#7474=CYLINDRICAL_SURFACE ( 'NONE', #388, 7.400000000000010125 ) ;
#7476=CARTESIAN_POINT ( 'NONE',  ( 0.000000000000000000, -2.099089055167822071, 6.233932467347762518 ) ) ;
#7477=CIRCLE ( 'NONE', #7699, 6.499000000000011212 ) ;
#7480=CARTESIAN_POINT ( 'NONE',  ( 19.99999999999999645, -6.486618105788070743, -0.4009819817180210189 ) ) ;
#7482=DIRECTION ( 'NONE',  ( 0.000000000000000000, 0.7818314824680310249, -0.6234898018587319291 ) ) ;
#7486=DIRECTION ( 'NONE',  ( -1.000000000000000000, 1.010728034814421376E-30, 1.090846720500930387E-30 ) ) ;
#7488=DIRECTION ( 'NONE',  ( -1.000000000000000000, 1.010728034814421376E-30, 1.090846720500930387E-30 ) ) ;
#7491=CIRCLE ( 'NONE', #7894, 6.499000000000008548 ) ;
#7494=DIRECTION ( 'NONE',  ( 5.115269932292492295E-31, -0.9195277725514543476, 0.3930250316539147248 ) ) ;
#7495=EDGE_LOOP ( 'NONE', ( #8409, #12176, #9305, #2613 ) ) ;
#7498=ORIENTED_EDGE ( 'NONE', *, *, #2954, .T. ) ;
#7501=FACE_OUTER_BOUND ( 'NONE', #10181, .T. ) ;
#7503=DIRECTION ( 'NONE',  ( 0.000000000000000000, 0.6579387259397136978, -0.7530714660036098573 ) ) ;
#7505=VERTEX_POINT ( 'NONE', #2478 ) ;
#7506=FACE_OUTER_BOUND ( 'NONE', #10458, .T. ) ;
#7508=ORIENTED_EDGE ( 'NONE', *, *, #6225, .T. ) ;
#7509=CIRCLE ( 'NONE', #1946, 2.500000000000003553 ) ;
#7514=VERTEX_POINT ( 'NONE', #2677 ) ;
#7516=ADVANCED_FACE ( 'NONE', ( #12521 ), #2546, .T. ) ;
#7517=EDGE_CURVE ( 'NONE', #35, #11636, #9400, .T. ) ;
#7518=EDGE_CURVE ( 'NONE', #5416, #701, #11291, .T. ) ;
#7519=ORIENTED_EDGE ( 'NONE', *, *, #1914, .F. ) ;
#7521=CARTESIAN_POINT ( 'NONE',  ( 19.99999999999999645, 0.000000000000000000, 0.000000000000000000 ) ) ;
#7522=ORIENTED_EDGE ( 'NONE', *, *, #4759, .T. ) ;
#7525=CARTESIAN_POINT ( 'NONE',  ( 0.000000000000000000, 0.000000000000000000, 0.000000000000000000 ) ) ;
#7529=FACE_OUTER_BOUND ( 'NONE', #3110, .T. ) ;
#7530=VECTOR ( 'NONE', #9246, 1000.000000000000000 ) ;
#7533=CARTESIAN_POINT ( 'NONE',  ( 19.99999999999999645, 5.895746314278407674, 2.916892913127008935 ) ) ;
#7534=DIRECTION ( 'NONE',  ( 0.000000000000000000, 0.000000000000000000, 1.000000000000000000 ) ) ;
#7537=CIRCLE ( 'NONE', #9171, 7.400000000000011902 ) ;
#7539=CARTESIAN_POINT ( 'NONE',  ( 19.99999999999997868, 5.362412286431509578, -3.809543717993867595 ) ) ;
#7540=ORIENTED_EDGE ( 'NONE', *, *, #804, .F. ) ;
#7541=DIRECTION ( 'NONE',  ( -1.000000000000000000, 1.010728034814421376E-30, 1.090846720500930387E-30 ) ) ;
#7543=AXIS2_PLACEMENT_3D ( 'NONE', #8262, #1813, #781 ) ;
#7544=EDGE_CURVE ( 'NONE', #1466, #8041, #7551, .T. ) ;
#7546=FACE_OUTER_BOUND ( 'NONE', #4559, .T. ) ;
#7547=CARTESIAN_POINT ( 'NONE',  ( 19.99999999999997868, -7.258495115966583811, 1.440225208600806717 ) ) ;
#7548=CYLINDRICAL_SURFACE ( 'NONE', #81, 7.400000000000010125 ) ;
#7550=DIRECTION ( 'NONE',  ( -1.000000000000000000, 1.010728034814421376E-30, 1.090846720500930387E-30 ) ) ;
#7551=LINE ( 'NONE', #11557, #9357 ) ;
#7553=AXIS2_PLACEMENT_3D ( 'NONE', #11866, #3117, #4060 ) ;
#7555=AXIS2_PLACEMENT_3D ( 'NONE', #5904, #4757, #3975 ) ;
#7556=CYLINDRICAL_SURFACE ( 'NONE', #11519, 7.400000000000010125 ) ;
#7558=ORIENTED_EDGE ( 'NONE', *, *, #4468, .F. ) ;
#7559=ORIENTED_EDGE ( 'NONE', *, *, #6753, .T. ) ;
#7561=EDGE_CURVE ( 'NONE', #1901, #10923, #3697, .T. ) ;
#7568=CARTESIAN_POINT ( 'NONE',  ( 0.000000000000000000, 5.483475578891660263, -3.488337222187519515 ) ) ;
#7570=VERTEX_POINT ( 'NONE', #11491 ) ;
#7571=VERTEX_POINT ( 'NONE', #4658 ) ;
#7572=CYLINDRICAL_SURFACE ( 'NONE', #5533, 6.499000000000010324 ) ;
#7576=ORIENTED_EDGE ( 'NONE', *, *, #11338, .F. ) ;
#7585=DIRECTION ( 'NONE',  ( -1.000000000000000000, 1.010728034814421376E-30, 1.090846720500930387E-30 ) ) ;
#7587=ORIENTED_EDGE ( 'NONE', *, *, #9179, .T. ) ;
#7589=AXIS2_PLACEMENT_3D ( 'NONE', #765, #12503, #3677 ) ;
#7590=ORIENTED_EDGE ( 'NONE', *, *, #8905, .F. ) ;
#7595=EDGE_LOOP ( 'NONE', ( #6014, #8254, #11595, #8220 ) ) ;
#7596=FACE_OUTER_BOUND ( 'NONE', #9405, .T. ) ;
#7598=CIRCLE ( 'NONE', #11101, 2.800000000000003819 ) ;
#7599=CIRCLE ( 'NONE', #2470, 2.800000000000003375 ) ;
#7600=CARTESIAN_POINT ( 'NONE',  ( 0.000000000000000000, 0.000000000000000000, 0.000000000000000000 ) ) ;
#7601=VECTOR ( 'NONE', #7665, 1000.000000000000000 ) ;
#7603=DIRECTION ( 'NONE',  ( 0.000000000000000000, 0.000000000000000000, -1.000000000000000000 ) ) ;
#7607=CARTESIAN_POINT ( 'NONE',  ( 0.000000000000000000, -5.148708580507714849, 3.965829163366255017 ) ) ;
#7608=AXIS2_PLACEMENT_3D ( 'NONE', #9067, #11985, #7088 ) ;
#7609=AXIS2_PLACEMENT_3D ( 'NONE', #1420, #11087, #4324 ) ;
#7610=AXIS2_PLACEMENT_3D ( 'NONE', #12084, #11961, #12021 ) ;
#7611=EDGE_CURVE ( 'NONE', #865, #12067, #6500, .T. ) ;
#7612=DIRECTION ( 'NONE',  ( 0.000000000000000000, 0.000000000000000000, 1.000000000000000000 ) ) ;
#7617=DIRECTION ( 'NONE',  ( -1.000000000000000000, 1.010728034814421376E-30, 1.090846720500930387E-30 ) ) ;
#7624=DIRECTION ( 'NONE',  ( -1.000000000000000000, 1.010728034814421376E-30, 1.090846720500930387E-30 ) ) ;
#7625=CARTESIAN_POINT ( 'NONE',  ( 0.000000000000000000, 6.057062246029517816, 4.251117141143491374 ) ) ;
#7632=CARTESIAN_POINT ( 'NONE',  ( 19.99999999999999645, 5.012092988313947117, 4.137139697483554812 ) ) ;
#7638=LINE ( 'NONE', #2827, #1853 ) ;
#7639=ORIENTED_EDGE ( 'NONE', *, *, #5621, .T. ) ;
#7640=ORIENTED_EDGE ( 'NONE', *, *, #706, .F. ) ;
#7642=ORIENTED_EDGE ( 'NONE', *, *, #12431, .T. ) ;
#7645=CYLINDRICAL_SURFACE ( 'NONE', #11723, 7.400000000000010125 ) ;
#7647=AXIS2_PLACEMENT_3D ( 'NONE', #1810, #5739, #2741 ) ;
#7648=LINE ( 'NONE', #1658, #8817 ) ;
#7650=AXIS2_PLACEMENT_3D ( 'NONE', #10907, #2095, #7494 ) ;
#7651=ORIENTED_EDGE ( 'NONE', *, *, #11184, .F. ) ;
#7652=CARTESIAN_POINT ( 'NONE',  ( 10.00000000000000178, 6.718789039999964352, 3.101269713516805027 ) ) ;
#7653=CYLINDRICAL_SURFACE ( 'NONE', #6477, 2.800000000000003819 ) ;
#7654=ORIENTED_EDGE ( 'NONE', *, *, #10502, .F. ) ;
#7661=ORIENTED_EDGE ( 'NONE', *, *, #2067, .T. ) ;
#7665=DIRECTION ( 'NONE',  ( -1.000000000000000000, 1.010728034814421376E-30, 1.090846720500930387E-30 ) ) ;
#7670=DIRECTION ( 'NONE',  ( 0.000000000000000000, 0.000000000000000000, 1.000000000000000000 ) ) ;
#7671=ORIENTED_EDGE ( 'NONE', *, *, #3163, .T. ) ;
#7675=LINE ( 'NONE', #650, #1425 ) ;
#7678=CYLINDRICAL_SURFACE ( 'NONE', #11997, 7.400000000000010125 ) ;
#7680=CIRCLE ( 'NONE', #1089, 7.400000000000009237 ) ;
#7681=CARTESIAN_POINT ( 'NONE',  ( -10.00000000000000178, 0.000000000000000000, 0.000000000000000000 ) ) ;
#7682=DIRECTION ( 'NONE',  ( 1.133987551255203244E-30, -0.9909497617679332571, -0.1342332658176667859 ) ) ;
#7684=CARTESIAN_POINT ( 'NONE',  ( 0.000000000000000000, -6.310777386698730673, 1.552768423021301469 ) ) ;
#7686=CARTESIAN_POINT ( 'NONE',  ( 9.999999999999994671, -5.651611091574839207, 4.776954267060578019 ) ) ;
#7687=ORIENTED_EDGE ( 'NONE', *, *, #6963, .F. ) ;
#7690=ORIENTED_EDGE ( 'NONE', *, *, #1595, .F. ) ;
#7692=EDGE_CURVE ( 'NONE', #11033, #11719, #5804, .T. ) ;
#7699=AXIS2_PLACEMENT_3D ( 'NONE', #465, #6462, #6324 ) ;
#7701=ORIENTED_EDGE ( 'NONE', *, *, #9385, .T. ) ;
#7705=CIRCLE ( 'NONE', #2149, 7.400000000000009237 ) ;
#7707=VECTOR ( 'NONE', #1436, 1000.000000000000000 ) ;
#7709=DIRECTION ( 'NONE',  ( 0.000000000000000000, 0.000000000000000000, 1.000000000000000000 ) ) ;
#7715=ORIENTED_EDGE ( 'NONE', *, *, #2925, .F. ) ;
#7718=CIRCLE ( 'NONE', #11219, 2.800000000000004263 ) ;
#7719=AXIS2_PLACEMENT_3D ( 'NONE', #8742, #4628, #10478 ) ;
#7721=ORIENTED_EDGE ( 'NONE', *, *, #3132, .T. ) ;
#7722=VERTEX_POINT ( 'NONE', #11613 ) ;
#7723=CARTESIAN_POINT ( 'NONE',  ( 19.99999999999999645, 0.000000000000000000, 0.000000000000000000 ) ) ;
#7724=CIRCLE ( 'NONE', #10382, 7.400000000000009237 ) ;
#7728=CARTESIAN_POINT ( 'NONE',  ( 19.99999999999999645, -1.966014849757073968, 6.277170897746257694 ) ) ;
#7730=LINE ( 'NONE', #4829, #7601 ) ;
#7735=LINE ( 'NONE', #9829, #350 ) ;
#7736=ORIENTED_EDGE ( 'NONE', *, *, #8947, .T. ) ;
#7739=CARTESIAN_POINT ( 'NONE',  ( 0.000000000000000000, 1.052479792859058128, 6.413211932068317189 ) ) ;
#7740=CARTESIAN_POINT ( 'NONE',  ( 0.000000000000000000, -3.178467454237101197, -5.758943784352613449 ) ) ;
#7742=CARTESIAN_POINT ( 'NONE',  ( 0.000000000000000000, 0.000000000000000000, 0.000000000000000000 ) ) ;
#7743=DIRECTION ( 'NONE',  ( -1.000000000000000000, 1.010728034814421376E-30, 1.090846720500930387E-30 ) ) ;
#7745=CARTESIAN_POINT ( 'NONE',  ( 19.99999999999999645, 0.000000000000000000, 0.000000000000000000 ) ) ;
#7749=EDGE_CURVE ( 'NONE', #11074, #1327, #12649, .T. ) ;
#7750=EDGE_CURVE ( 'NONE', #10716, #3178, #10755, .T. ) ;
#7751=AXIS2_PLACEMENT_3D ( 'NONE', #6674, #2946, #3771 ) ;
#7758=DIRECTION ( 'NONE',  ( -1.000000000000000000, 1.010728034814421376E-30, 1.090846720500930387E-30 ) ) ;
#7761=CIRCLE ( 'NONE', #8785, 2.800000000000004263 ) ;
#7763=DIRECTION ( 'NONE',  ( -1.000000000000000000, 1.010728034814421376E-30, 1.090846720500930387E-30 ) ) ;
#7765=EDGE_LOOP ( 'NONE', ( #6606, #10341, #12356, #9360 ) ) ;
#7767=ORIENTED_EDGE ( 'NONE', *, *, #4151, .F. ) ;
#7768=ORIENTED_EDGE ( 'NONE', *, *, #10599, .F. ) ;
#7770=LINE ( 'NONE', #3724, #6156 ) ;
#7772=DIRECTION ( 'NONE',  ( -1.000000000000000000, 1.010728034814421376E-30, 1.090846720500930387E-30 ) ) ;
#7774=CARTESIAN_POINT ( 'NONE',  ( 19.99999999999997868, -1.268072931708450257, -6.374087545670231947 ) ) ;
#7777=ADVANCED_FACE ( 'NONE', ( #10221 ), #7983, .T. ) ;
#7780=ORIENTED_EDGE ( 'NONE', *, *, #4969, .F. ) ;
#7783=EDGE_LOOP ( 'NONE', ( #2714, #7895, #788, #7640 ) ) ;
#7784=DIRECTION ( 'NONE',  ( 1.000000000000000000, -1.010728034814421376E-30, -1.090846720500930387E-30 ) ) ;
#7787=ORIENTED_EDGE ( 'NONE', *, *, #11606, .T. ) ;
#7789=DIRECTION ( 'NONE',  ( -1.000000000000000000, 1.010728034814421376E-30, 1.090846720500930387E-30 ) ) ;
#7790=DIRECTION ( 'NONE',  ( 0.000000000000000000, -0.9749279121818259508, 0.2225209339563040400 ) ) ;
#7794=ORIENTED_EDGE ( 'NONE', *, *, #296, .T. ) ;
#7796=EDGE_CURVE ( 'NONE', #9165, #276, #9205, .T. ) ;
#7797=FACE_OUTER_BOUND ( 'NONE', #6743, .T. ) ;
#7798=AXIS2_PLACEMENT_3D ( 'NONE', #11221, #10222, #5351 ) ;
#7799=AXIS2_PLACEMENT_3D ( 'NONE', #6892, #10801, #1982 ) ;
#7800=AXIS2_PLACEMENT_3D ( 'NONE', #6724, #7624, #10510 ) ;
#7801=LINE ( 'NONE', #6779, #8674 ) ;
#7802=AXIS2_PLACEMENT_3D ( 'NONE', #11581, #8672, #5768 ) ;
#7808=CIRCLE ( 'NONE', #12345, 2.800000000000003819 ) ;
#7809=AXIS2_PLACEMENT_3D ( 'NONE', #11548, #12511, #5548 ) ;
#7810=AXIS2_PLACEMENT_3D ( 'NONE', #10628, #3752, #8642 ) ;
#7811=CARTESIAN_POINT ( 'NONE',  ( 9.999999999999994671, -2.401522331692915735, 6.999477872697376313 ) ) ;
#7812=ORIENTED_EDGE ( 'NONE', *, *, #12574, .F. ) ;
#7815=CARTESIAN_POINT ( 'NONE',  ( 19.99999999999997868, 6.321830586517925177, 1.817291089601345888 ) ) ;
#7822=CARTESIAN_POINT ( 'NONE',  ( 19.99999999999999645, 0.000000000000000000, 0.000000000000000000 ) ) ;
#7824=LINE ( 'NONE', #2948, #3213 ) ;
#7827=ORIENTED_EDGE ( 'NONE', *, *, #537, .T. ) ;
#7836=DIRECTION ( 'NONE',  ( -1.000000000000000000, 1.010728034814421376E-30, 1.090846720500930387E-30 ) ) ;
#7838=ORIENTED_EDGE ( 'NONE', *, *, #6412, .F. ) ;
#7841=STYLED_ITEM ( 'NONE', ( #5030 ), #1117 ) ;
#7843=ORIENTED_EDGE ( 'NONE', *, *, #2110, .F. ) ;
#7844=VERTEX_POINT ( 'NONE', #390 ) ;
#7846=CIRCLE ( 'NONE', #9275, 7.400000000000011902 ) ;
#7848=FACE_OUTER_BOUND ( 'NONE', #7943, .T. ) ;
#7853=AXIS2_PLACEMENT_3D ( 'NONE', #459, #9209, #7168 ) ;
#7856=ORIENTED_EDGE ( 'NONE', *, *, #6065, .T. ) ;
#7857=CARTESIAN_POINT ( 'NONE',  ( 19.99999999999999645, 3.681899619563770543, 5.450844343808956438 ) ) ;
#7860=DIRECTION ( 'NONE',  ( -1.000000000000000000, 1.010728034814421376E-30, 1.090846720500930387E-30 ) ) ;
#7861=VECTOR ( 'NONE', #8366, 1000.000000000000000 ) ;
#7862=DIRECTION ( 'NONE',  ( -1.000000000000000000, 1.010728034814421376E-30, 1.090846720500930387E-30 ) ) ;
#7863=DIRECTION ( 'NONE',  ( 1.140150527077241873E-30, 0.000000000000000000, -1.000000000000000000 ) ) ;
#7864=DIRECTION ( 'NONE',  ( -1.000000000000000000, 1.010728034814421376E-30, 1.090846720500930387E-30 ) ) ;
#7866=DIRECTION ( 'NONE',  ( 1.000000000000000000, -1.010728034814421376E-30, -1.090846720500930387E-30 ) ) ;
#7868=CIRCLE ( 'NONE', #11589, 2.800000000000004263 ) ;
#7871=ORIENTED_EDGE ( 'NONE', *, *, #6913, .F. ) ;
#7872=DIRECTION ( 'NONE',  ( -6.532754371361493504E-31, 0.9510565162951545304, -0.3090169943749445092 ) ) ;
#7873=CYLINDRICAL_SURFACE ( 'NONE', #6453, 6.499000000000010324 ) ;
#7877=ORIENTED_EDGE ( 'NONE', *, *, #12321, .F. ) ;
#7883=VERTEX_POINT ( 'NONE', #2208 ) ;
#7884=CYLINDRICAL_SURFACE ( 'NONE', #10513, 2.800000000000003819 ) ;
#7890=ORIENTED_EDGE ( 'NONE', *, *, #12582, .F. ) ;
#7891=CIRCLE ( 'NONE', #1730, 6.499000000000009436 ) ;
#7894=AXIS2_PLACEMENT_3D ( 'NONE', #8132, #4146, #11233 ) ;
#7895=ORIENTED_EDGE ( 'NONE', *, *, #11006, .T. ) ;
#7904=ORIENTED_EDGE ( 'NONE', *, *, #3180, .T. ) ;
#7908=LINE ( 'NONE', #9577, #6273 ) ;
#7912=CIRCLE ( 'NONE', #1123, 7.400000000000009237 ) ;
#7913=ORIENTED_EDGE ( 'NONE', *, *, #12574, .T. ) ;
#7914=AXIS2_PLACEMENT_3D ( 'NONE', #4487, #3715, #9605 ) ;
#7915=CYLINDRICAL_SURFACE ( 'NONE', #7455, 2.800000000000003819 ) ;
#7921=CYLINDRICAL_SURFACE ( 'NONE', #9332, 2.800000000000003819 ) ;
#7925=CARTESIAN_POINT ( 'NONE',  ( 19.99999999999997868, 4.192831774279055068, -4.965597920955358902 ) ) ;
#7927=EDGE_CURVE ( 'NONE', #12067, #7722, #8311, .T. ) ;
#7929=ADVANCED_FACE ( 'NONE', ( #2729 ), #519, .T. ) ;
#7932=CARTESIAN_POINT ( 'NONE',  ( 0.000000000000000000, 5.483475578891600755, 3.488337222187588793 ) ) ;
#7934=CARTESIAN_POINT ( 'NONE',  ( 19.99999999999999645, 2.918117354836642363, 5.807029542149858337 ) ) ;
#7935=DIRECTION ( 'NONE',  ( -1.000000000000000000, 1.010728034814421376E-30, 1.090846720500930387E-30 ) ) ;
#7936=ORIENTED_EDGE ( 'NONE', *, *, #7611, .T. ) ;
#7938=AXIS2_PLACEMENT_3D ( 'NONE', #3891, #9731, #9603 ) ;
#7940=CIRCLE ( 'NONE', #8363, 7.400000000000009237 ) ;
#7941=EDGE_CURVE ( 'NONE', #9038, #640, #11417, .T. ) ;
#7943=EDGE_LOOP ( 'NONE', ( #10992, #10528, #731, #11108 ) ) ;
#7946=VERTEX_POINT ( 'NONE', #4645 ) ;
#7947=ORIENTED_EDGE ( 'NONE', *, *, #3275, .T. ) ;
#7949=CARTESIAN_POINT ( 'NONE',  ( 9.999999999999994671, 2.796709610837350812, 6.851161606081866751 ) ) ;
#7951=AXIS2_PLACEMENT_3D ( 'NONE', #4719, #972, #6662 ) ;
#7953=AXIS2_PLACEMENT_3D ( 'NONE', #4000, #4718, #8646 ) ;
#7955=FACE_OUTER_BOUND ( 'NONE', #11683, .T. ) ;
#7956=ORIENTED_EDGE ( 'NONE', *, *, #6765, .F. ) ;
#7958=DIRECTION ( 'NONE',  ( 1.000000000000000000, -1.010728034814421376E-30, -1.090846720500930387E-30 ) ) ;
#7959=VERTEX_POINT ( 'NONE', #1609 ) ;
#7960=CIRCLE ( 'NONE', #11652, 6.499000000000008548 ) ;
#7961=ORIENTED_EDGE ( 'NONE', *, *, #2971, .T. ) ;
#7962=VERTEX_POINT ( 'NONE', #6516 ) ;
#7963=EDGE_CURVE ( 'NONE', #2491, #9566, #5604, .T. ) ;
#7967=CARTESIAN_POINT ( 'NONE',  ( 19.99999999999999645, 1.764426149628130602, 7.186570834724196111 ) ) ;
#7968=ORIENTED_EDGE ( 'NONE', *, *, #8229, .F. ) ;
#7970=EDGE_CURVE ( 'NONE', #2762, #10498, #7705, .T. ) ;
#7974=EDGE_LOOP ( 'NONE', ( #3617, #12116, #1657, #10213 ) ) ;
#7975=CARTESIAN_POINT ( 'NONE',  ( 19.99999999999999645, -2.171317488608541346, 7.074275960383707762 ) ) ;
#7977=CARTESIAN_POINT ( 'NONE',  ( 0.000000000000000000, 6.321830586517925177, 1.817291089601352772 ) ) ;
#7978=LINE ( 'NONE', #3814, #10494 ) ;
#7979=CYLINDRICAL_SURFACE ( 'NONE', #11976, 2.800000000000003819 ) ;
#7980=CYLINDRICAL_SURFACE ( 'NONE', #7306, 6.499000000000010324 ) ;
#7982=CARTESIAN_POINT ( 'NONE',  ( 19.99999999999997868, -0.9522442067290397549, -6.508557431545724192 ) ) ;
#7983=CYLINDRICAL_SURFACE ( 'NONE', #11829, 2.800000000000003819 ) ;
#7984=CARTESIAN_POINT ( 'NONE',  ( 0.000000000000000000, -3.178467454237179801, 5.758943784352561046 ) ) ;
#7985=CARTESIAN_POINT ( 'NONE',  ( 0.000000000000000000, 0.000000000000000000, 0.000000000000000000 ) ) ;
#7988=AXIS2_PLACEMENT_3D ( 'NONE', #4241, #1528, #6433 ) ;
#7995=ADVANCED_FACE ( 'NONE', ( #6581 ), #3437, .T. ) ;
#7999=EDGE_CURVE ( 'NONE', #11730, #12228, #3800, .T. ) ;
#8000=CIRCLE ( 'NONE', #9241, 7.400000000000009237 ) ;
#8002=AXIS2_PLACEMENT_3D ( 'NONE', #7188, #5190, #1490 ) ;
#8006=AXIS2_PLACEMENT_3D ( 'NONE', #422, #4350, #4670 ) ;
#8010=EDGE_LOOP ( 'NONE', ( #11390, #12358, #11967, #3235 ) ) ;
#8011=ORIENTED_EDGE ( 'NONE', *, *, #10607, .T. ) ;
#8013=CIRCLE ( 'NONE', #2479, 7.400000000000011902 ) ;
#8014=DIRECTION ( 'NONE',  ( 0.000000000000000000, 0.000000000000000000, 1.000000000000000000 ) ) ;
#8015=CIRCLE ( 'NONE', #3511, 2.800000000000004263 ) ;
#8016=ORIENTED_EDGE ( 'NONE', *, *, #3893, .T. ) ;
#8019=DIRECTION ( 'NONE',  ( -1.000000000000000000, 1.010728034814421376E-30, 1.090846720500930387E-30 ) ) ;
#8021=CARTESIAN_POINT ( 'NONE',  ( 0.000000000000000000, -1.268072931708452922, -6.374087545670245269 ) ) ;
#8023=DIRECTION ( 'NONE',  ( 0.000000000000000000, 0.5877852522924684742, 0.8090169943749506709 ) ) ;
#8026=ORIENTED_EDGE ( 'NONE', *, *, #1801, .F. ) ;
#8028=ORIENTED_EDGE ( 'NONE', *, *, #3811, .T. ) ;
#8029=DIRECTION ( 'NONE',  ( -1.000000000000000000, 1.010728034814421376E-30, 1.090846720500930387E-30 ) ) ;
#8031=ORIENTED_EDGE ( 'NONE', *, *, #4954, .T. ) ;
#8034=ORIENTED_EDGE ( 'NONE', *, *, #2074, .T. ) ;
#8035=DIRECTION ( 'NONE',  ( -1.000000000000000000, 1.010728034814421376E-30, 1.090846720500930387E-30 ) ) ;
#8037=CYLINDRICAL_SURFACE ( 'NONE', #7608, 2.500000000000003553 ) ;
#8039=AXIS2_PLACEMENT_3D ( 'NONE', #1183, #8138, #7183 ) ;
#8041=VERTEX_POINT ( 'NONE', #2531 ) ;
#8042=CARTESIAN_POINT ( 'NONE',  ( -10.00000000000000178, 0.000000000000000000, 0.000000000000000000 ) ) ;
#8043=ADVANCED_FACE ( 'NONE', ( #11476 ), #6452, .T. ) ;
#8051=CARTESIAN_POINT ( 'NONE',  ( 0.000000000000000000, -3.612733913993642965, 6.458185013351672055 ) ) ;
#8052=AXIS2_PLACEMENT_3D ( 'NONE', #4967, #9900, #70 ) ;
#8054=VERTEX_POINT ( 'NONE', #8497 ) ;
#8055=DIRECTION ( 'NONE',  ( -1.000000000000000000, 1.010728034814421376E-30, 1.090846720500930387E-30 ) ) ;
#8057=DIRECTION ( 'NONE',  ( 0.000000000000000000, 0.000000000000000000, 1.000000000000000000 ) ) ;
#8059=DIRECTION ( 'NONE',  ( 0.000000000000000000, -0.8345732537213078617, 0.5508969814520944253 ) ) ;
#8061=AXIS2_PLACEMENT_3D ( 'NONE', #8447, #1492, #8577 ) ;
#8062=CARTESIAN_POINT ( 'NONE',  ( 0.000000000000000000, 0.000000000000000000, 0.000000000000000000 ) ) ;
#8063=AXIS2_PLACEMENT_3D ( 'NONE', #4105, #8029, #3164 ) ;
#8064=CYLINDRICAL_SURFACE ( 'NONE', #88, 7.400000000000010125 ) ;
#8068=DIRECTION ( 'NONE',  ( -1.000000000000000000, 1.010728034814421376E-30, 1.090846720500930387E-30 ) ) ;
#8069=VERTEX_POINT ( 'NONE', #3679 ) ;
#8070=AXIS2_PLACEMENT_3D ( 'NONE', #2168, #355, #10128 ) ;
#8071=ORIENTED_EDGE ( 'NONE', *, *, #8073, .T. ) ;
#8073=EDGE_CURVE ( 'NONE', #276, #4606, #6475, .T. ) ;
#8074=CIRCLE ( 'NONE', #2545, 2.800000000000002487 ) ;
#8075=AXIS2_PLACEMENT_3D ( 'NONE', #9555, #3661, #9364 ) ;
#8076=EDGE_CURVE ( 'NONE', #6900, #2828, #4769, .T. ) ;
#8077=CARTESIAN_POINT ( 'NONE',  ( 19.99999999999999645, 0.000000000000000000, 0.000000000000000000 ) ) ;
#8080=CYLINDRICAL_SURFACE ( 'NONE', #4386, 6.499000000000010324 ) ;
#8083=DIRECTION ( 'NONE',  ( -1.000000000000000000, 1.010728034814421376E-30, 1.090846720500930387E-30 ) ) ;
#8091=ADVANCED_FACE ( 'NONE', ( #10806 ), #3045, .T. ) ;
#8092=CYLINDRICAL_SURFACE ( 'NONE', #9096, 7.400000000000010125 ) ;
#8095=VERTEX_POINT ( 'NONE', #11598 ) ;
#8096=DIRECTION ( 'NONE',  ( 0.000000000000000000, 0.000000000000000000, 1.000000000000000000 ) ) ;
#8097=ORIENTED_EDGE ( 'NONE', *, *, #10599, .T. ) ;
#8098=FACE_OUTER_BOUND ( 'NONE', #3536, .T. ) ;
#8102=ORIENTED_EDGE ( 'NONE', *, *, #754, .F. ) ;
#8111=EDGE_CURVE ( 'NONE', #11957, #4395, #7908, .T. ) ;
#8112=PRODUCT_DEFINITION_SHAPE ( 'NONE', 'NONE',  #10818 ) ;
#8113=DIRECTION ( 'NONE',  ( -1.454462294001239290E-30, 0.7227948638273881121, 0.6910626489868684219 ) ) ;
#8123=DIRECTION ( 'NONE',  ( -1.000000000000000000, 1.010728034814421376E-30, 1.090846720500930387E-30 ) ) ;
#8125=CARTESIAN_POINT ( 'NONE',  ( 19.99999999999999645, 0.000000000000000000, 0.000000000000000000 ) ) ;
#8126=DIRECTION ( 'NONE',  ( -1.000000000000000000, 1.010728034814421376E-30, 1.090846720500930387E-30 ) ) ;
#8127=ORIENTED_EDGE ( 'NONE', *, *, #10446, .T. ) ;
#8129=FACE_OUTER_BOUND ( 'NONE', #3259, .T. ) ;
#8130=EDGE_CURVE ( 'NONE', #156, #7571, #719, .T. ) ;
#8132=CARTESIAN_POINT ( 'NONE',  ( 0.000000000000000000, 0.000000000000000000, 0.000000000000000000 ) ) ;
#8133=EDGE_CURVE ( 'NONE', #11698, #9285, #4830, .T. ) ;
#8134=SURFACE_SIDE_STYLE ('',( #5303 ) ) ;
#8135=AXIS2_PLACEMENT_3D ( 'NONE', #7476, #11413, #7354 ) ;
#8138=DIRECTION ( 'NONE',  ( 1.000000000000000000, -1.010728034814421376E-30, -1.090846720500930387E-30 ) ) ;
#8145=FACE_OUTER_BOUND ( 'NONE', #7595, .T. ) ;
#8148=DIRECTION ( 'NONE',  ( -1.000000000000000000, 1.010728034814421376E-30, 1.090846720500930387E-30 ) ) ;
#8152=EDGE_CURVE ( 'NONE', #1263, #3837, #512, .T. ) ;
#8153=ORIENTED_EDGE ( 'NONE', *, *, #2261, .F. ) ;
#8154=ORIENTED_EDGE ( 'NONE', *, *, #5398, .T. ) ;
#8156=ORIENTED_EDGE ( 'NONE', *, *, #11926, .T. ) ;
#8157=AXIS2_PLACEMENT_3D ( 'NONE', #11361, #12331, #2544 ) ;
#8163=ORIENTED_EDGE ( 'NONE', *, *, #12001, .F. ) ;
#8166=DIRECTION ( 'NONE',  ( -1.000000000000000000, 1.010728034814421376E-30, 1.090846720500930387E-30 ) ) ;
#8167=CIRCLE ( 'NONE', #8823, 6.499000000000008548 ) ;
#8168=CIRCLE ( 'NONE', #2633, 2.800000000000002931 ) ;
#8169=EDGE_CURVE ( 'NONE', #955, #568, #8320, .T. ) ;
#8171=CARTESIAN_POINT ( 'NONE',  ( 19.99999999999999645, -4.907279493584762342, 4.380262188593320616 ) ) ;
#8175=VERTEX_POINT ( 'NONE', #2125 ) ;
#8176=CARTESIAN_POINT ( 'NONE',  ( 0.000000000000000000, -6.453973581750240385, 0.7636923504068595658 ) ) ;
#8178=DIRECTION ( 'NONE',  ( 1.133987551255203069E-30, -0.9909497617679331460, -0.1342332658176667304 ) ) ;
#8181=CARTESIAN_POINT ( 'NONE',  ( 19.99999999999997868, 6.321830586517925177, 1.817291089601345888 ) ) ;
#8182=DIRECTION ( 'NONE',  ( 0.000000000000000000, 0.000000000000000000, 1.000000000000000000 ) ) ;
#8185=DIRECTION ( 'NONE',  ( -1.000000000000000000, 1.010728034814421376E-30, 1.090846720500930387E-30 ) ) ;
#8186=FACE_OUTER_BOUND ( 'NONE', #4154, .T. ) ;
#8187=EDGE_CURVE ( 'NONE', #7946, #6318, #3210, .T. ) ;
#8189=ORIENTED_EDGE ( 'NONE', *, *, #11467, .F. ) ;
#8190=CARTESIAN_POINT ( 'NONE',  ( 19.99999999999999645, 7.164568425986781897, -1.851744925564387856 ) ) ;
#8191=CARTESIAN_POINT ( 'NONE',  ( 19.99999999999997868, 5.483475578891663815, -3.488337222187519515 ) ) ;
#8196=CARTESIAN_POINT ( 'NONE',  ( 0.000000000000000000, 2.918117354836644139, 5.807029542149858337 ) ) ;
#8197=DIRECTION ( 'NONE',  ( 1.000000000000000000, -1.010728034814421376E-30, -1.090846720500930387E-30 ) ) ;
#8198=VECTOR ( 'NONE', #10872, 1000.000000000000000 ) ;
#8201=CARTESIAN_POINT ( 'NONE',  ( -10.00000000000000178, 0.000000000000000000, 0.000000000000000000 ) ) ;
#8202=ORIENTED_EDGE ( 'NONE', *, *, #2814, .T. ) ;
#8204=VERTEX_POINT ( 'NONE', #4305 ) ;
#8206=EDGE_CURVE ( 'NONE', #11576, #3412, #5245, .T. ) ;
#8207=ADVANCED_FACE ( 'NONE', ( #12111 ), #1085, .T. ) ;
#8209=DIRECTION ( 'NONE',  ( -1.000000000000000000, 1.010728034814421376E-30, 1.090846720500930387E-30 ) ) ;
#8210=DIRECTION ( 'NONE',  ( -1.140150527077241873E-30, 0.000000000000000000, 1.000000000000000000 ) ) ;
#8212=CIRCLE ( 'NONE', #906, 2.800000000000004263 ) ;
#8213=DIRECTION ( 'NONE',  ( 1.140150527077241873E-30, 0.000000000000000000, -1.000000000000000000 ) ) ;
#8214=CARTESIAN_POINT ( 'NONE',  ( 19.99999999999999645, -6.213893036447818652, 1.903820982021499297 ) ) ;
#8215=VECTOR ( 'NONE', #10310, 1000.000000000000000 ) ;
#8219=DIRECTION ( 'NONE',  ( 6.902532920683844539E-31, -0.9749279121818259508, 0.2225209339563041233 ) ) ;
#8220=ORIENTED_EDGE ( 'NONE', *, *, #1914, .T. ) ;
#8222=ORIENTED_EDGE ( 'NONE', *, *, #1164, .T. ) ;
#8225=AXIS2_PLACEMENT_3D ( 'NONE', #7235, #2274, #6255 ) ;
#8229=EDGE_CURVE ( 'NONE', #2119, #2228, #7912, .T. ) ;
#8231=VERTEX_POINT ( 'NONE', #5213 ) ;
#8232=DIRECTION ( 'NONE',  ( 0.000000000000000000, 0.000000000000000000, 1.000000000000000000 ) ) ;
#8234=CARTESIAN_POINT ( 'NONE',  ( 9.999999999999994671, -0.8732627748488634989, 7.348293143721422283 ) ) ;
#8235=DIRECTION ( 'NONE',  ( -1.000000000000000000, 1.010728034814421376E-30, 1.090846720500930387E-30 ) ) ;
#8238=DIRECTION ( 'NONE',  ( -1.000000000000000000, 1.010728034814421376E-30, 1.090846720500930387E-30 ) ) ;
#8242=EDGE_CURVE ( 'NONE', #4356, #2884, #2584, .T. ) ;
#8248=EDGE_CURVE ( 'NONE', #11074, #2378, #7718, .T. ) ;
#8254=ORIENTED_EDGE ( 'NONE', *, *, #12483, .F. ) ;
#8255=DIRECTION ( 'NONE',  ( 0.000000000000000000, -0.5128992774058948045, -0.8584487936018729837 ) ) ;
#8259=DIRECTION ( 'NONE',  ( 0.000000000000000000, 0.000000000000000000, 1.000000000000000000 ) ) ;
#8262=CARTESIAN_POINT ( 'NONE',  ( -10.00000000000000178, 0.000000000000000000, 0.000000000000000000 ) ) ;
#8264=DIRECTION ( 'NONE',  ( 0.000000000000000000, -0.7227948638273978821, 0.6910626489868579858 ) ) ;
#8266=ORIENTED_EDGE ( 'NONE', *, *, #11757, .T. ) ;
#8268=ORIENTED_EDGE ( 'NONE', *, *, #4910, .F. ) ;
#8271=VERTEX_POINT ( 'NONE', #11007 ) ;
#8274=DIRECTION ( 'NONE',  ( 0.000000000000000000, 0.000000000000000000, 1.000000000000000000 ) ) ;
#8275=AXIS2_PLACEMENT_3D ( 'NONE', #6118, #3933, #3993 ) ;
#8277=DIRECTION ( 'NONE',  ( -8.073498326871282186E-31, -0.2660368455666824450, 0.9639628606958512425 ) ) ;
#8278=CARTESIAN_POINT ( 'NONE',  ( 19.99999999999997868, -3.612733913993553703, -6.458185013351741333 ) ) ;
#8279=VERTEX_POINT ( 'NONE', #5153 ) ;
#8284=AXIS2_PLACEMENT_3D ( 'NONE', #4461, #5556, #9463 ) ;
#8285=ORIENTED_EDGE ( 'NONE', *, *, #9531, .T. ) ;
#8286=AXIS2_PLACEMENT_3D ( 'NONE', #7723, #6758, #7470 ) ;
#8288=CARTESIAN_POINT ( 'NONE',  ( 0.000000000000000000, -4.046291478462172186, -5.186098161460352074 ) ) ;
#8293=AXIS2_PLACEMENT_3D ( 'NONE', #5002, #7063, #9167 ) ;
#8295=CARTESIAN_POINT ( 'NONE',  ( 0.000000000000000000, -6.484265599627184073, 1.105616797298897280 ) ) ;
#8296=EDGE_CURVE ( 'NONE', #8271, #5523, #3807, .T. ) ;
#8297=DIRECTION ( 'NONE',  ( 0.000000000000000000, 0.8805955318567392220, -0.4738686624729965824 ) ) ;
#8298=EDGE_CURVE ( 'NONE', #1836, #640, #11002, .T. ) ;
#8301=VERTEX_POINT ( 'NONE', #7280 ) ;
#8309=AXIS2_PLACEMENT_3D ( 'NONE', #5147, #12049, #6043 ) ;
#8310=CARTESIAN_POINT ( 'NONE',  ( 19.99999999999999645, -6.884685972239648066, -2.713134545806132003 ) ) ;
#8311=LINE ( 'NONE', #10293, #6894 ) ;
#8312=CARTESIAN_POINT ( 'NONE',  ( 0.000000000000000000, -6.969736844459714753, 2.486517307195110327 ) ) ;
#8315=VECTOR ( 'NONE', #3513, 1000.000000000000000 ) ;
#8317=EDGE_CURVE ( 'NONE', #742, #6542, #10577, .T. ) ;
#8318=ORIENTED_EDGE ( 'NONE', *, *, #7466, .T. ) ;
#8320=CIRCLE ( 'NONE', #5038, 2.800000000000003819 ) ;
#8321=DIRECTION ( 'NONE',  ( -1.000000000000000000, 1.010728034814421376E-30, 1.090846720500930387E-30 ) ) ;
#8323=AXIS2_PLACEMENT_3D ( 'NONE', #8295, #12239, #3423 ) ;
#8325=EDGE_CURVE ( 'NONE', #3019, #3594, #6487, .T. ) ;
#8326=DIRECTION ( 'NONE',  ( 1.140150527077240122E-30, -1.776356839400250465E-15, -1.000000000000000000 ) ) ;
#8327=EDGE_CURVE ( 'NONE', #3589, #6992, #5861, .T. ) ;
#8332=EDGE_LOOP ( 'NONE', ( #12019, #5380, #5626, #10399 ) ) ;
#8334=VERTEX_POINT ( 'NONE', #2388 ) ;
#8337=ORIENTED_EDGE ( 'NONE', *, *, #5499, .T. ) ;
#8338=CARTESIAN_POINT ( 'NONE',  ( -10.00000000000000178, 0.000000000000000000, 0.000000000000000000 ) ) ;
#8346=FACE_OUTER_BOUND ( 'NONE', #4916, .T. ) ;
#8349=ORIENTED_EDGE ( 'NONE', *, *, #5148, .T. ) ;
#8350=ORIENTED_EDGE ( 'NONE', *, *, #5219, .T. ) ;
#8352=EDGE_CURVE ( 'NONE', #9071, #2762, #6439, .T. ) ;
#8353=CARTESIAN_POINT ( 'NONE',  ( 50.00005079999998969, 5.510332127717259942E-15, -2.500000000000010658 ) ) ;
#8354=VERTEX_POINT ( 'NONE', #8424 ) ;
#8358=CARTESIAN_POINT ( 'NONE',  ( 19.99999999999999645, -5.610543508060415796, -3.433640984893324699 ) ) ;
#8361=AXIS2_PLACEMENT_3D ( 'NONE', #10049, #1044, #4074 ) ;
#8362=CARTESIAN_POINT ( 'NONE',  ( 19.99999999999999645, -6.182645281642477286, -2.245659411033190445 ) ) ;
#8363=AXIS2_PLACEMENT_3D ( 'NONE', #7379, #11566, #2692 ) ;
#8366=DIRECTION ( 'NONE',  ( -1.000000000000000000, 1.010728034814421376E-30, 1.090846720500930387E-30 ) ) ;
#8367=EDGE_CURVE ( 'NONE', #7959, #7387, #7509, .T. ) ;
#8368=FACE_OUTER_BOUND ( 'NONE', #12193, .T. ) ;
#8375=CARTESIAN_POINT ( 'NONE',  ( 19.99999999999997868, -1.966014849756994254, -6.277170897746295886 ) ) ;
#8381=CARTESIAN_POINT ( 'NONE',  ( 19.99999999999999645, -6.413745496774120092, 3.691052519622234129 ) ) ;
#8382=DIRECTION ( 'NONE',  ( -1.000000000000000000, 1.010728034814421376E-30, 1.090846720500930387E-30 ) ) ;
#8383=EDGE_CURVE ( 'NONE', #11905, #8539, #9143, .T. ) ;
#8384=ORIENTED_EDGE ( 'NONE', *, *, #445, .T. ) ;
#8385=DIRECTION ( 'NONE',  ( 0.000000000000000000, 0.000000000000000000, 1.000000000000000000 ) ) ;
#8386=CARTESIAN_POINT ( 'NONE',  ( 19.99999999999997868, 6.718789039999997215, -3.101269713516725091 ) ) ;
#8388=CARTESIAN_POINT ( 'NONE',  ( 19.99999999999999645, 5.483475578891613189, 3.488337222187588793 ) ) ;
#8390=CARTESIAN_POINT ( 'NONE',  ( 19.99999999999999645, -4.621065432155107011, 4.569765340993028779 ) ) ;
#8391=CARTESIAN_POINT ( 'NONE',  ( 0.000000000000000000, -3.612733913993552815, -6.458185013351741333 ) ) ;
#8393=EDGE_LOOP ( 'NONE', ( #5, #6757, #3579, #7904 ) ) ;
#8395=ORIENTED_EDGE ( 'NONE', *, *, #11408, .T. ) ;
#8398=DIRECTION ( 'NONE',  ( 0.000000000000000000, 0.000000000000000000, 1.000000000000000000 ) ) ;
#8402=DIRECTION ( 'NONE',  ( 0.000000000000000000, 0.3513748240813435175, -0.9362348706397368714 ) ) ;
#8403=ORIENTED_EDGE ( 'NONE', *, *, #4914, .T. ) ;
#8406=AXIS2_PLACEMENT_3D ( 'NONE', #5901, #7772, #4811 ) ;
#8407=CARTESIAN_POINT ( 'NONE',  ( 19.99999999999997868, 6.018220532833812975, -2.453165835849195453 ) ) ;
#8409=ORIENTED_EDGE ( 'NONE', *, *, #4335, .F. ) ;
#8412=ORIENTED_EDGE ( 'NONE', *, *, #2971, .F. ) ;
#8414=VECTOR ( 'NONE', #9206, 1000.000000000000000 ) ;
#8418=CARTESIAN_POINT ( 'NONE',  ( 0.000000000000000000, 3.019282868015085164, 6.756029230465983026 ) ) ;
#8422=DIRECTION ( 'NONE',  ( 1.000000000000000000, -1.010728034814421376E-30, -1.090846720500930387E-30 ) ) ;
#8424=CARTESIAN_POINT ( 'NONE',  ( 19.99999999999997868, 5.025702764809158118, -5.431603052487340655 ) ) ;
#8428=CARTESIAN_POINT ( 'NONE',  ( 19.99999999999997868, 6.146182963951668299, 2.112211157443887100 ) ) ;
#8434=AXIS2_PLACEMENT_3D ( 'NONE', #584, #709, #4518 ) ;
#8436=DIRECTION ( 'NONE',  ( -1.140150527077241873E-30, 0.000000000000000000, 1.000000000000000000 ) ) ;
#8437=DIRECTION ( 'NONE',  ( 0.000000000000000000, 0.000000000000000000, 1.000000000000000000 ) ) ;
#8438=DIRECTION ( 'NONE',  ( -1.000000000000000000, 1.010728034814421376E-30, 1.090846720500930387E-30 ) ) ;
#8441=DIRECTION ( 'NONE',  ( -3.266377185680748504E-31, 0.8805955318567392220, -0.4738686624729964159 ) ) ;
#8442=AXIS2_PLACEMENT_3D ( 'NONE', #3652, #1897, #9607 ) ;
#8443=CARTESIAN_POINT ( 'NONE',  ( 19.99999999999999645, 5.280167904461726458, 3.922743398397384063 ) ) ;
#8446=ORIENTED_EDGE ( 'NONE', *, *, #9108, .T. ) ;
#8447=CARTESIAN_POINT ( 'NONE',  ( 19.99999999999999645, 0.000000000000000000, 0.000000000000000000 ) ) ;
#8448=LINE ( 'NONE', #3447, #8909 ) ;
#8449=CYLINDRICAL_SURFACE ( 'NONE', #9586, 7.400000000000010125 ) ;
#8452=CYLINDRICAL_SURFACE ( 'NONE', #12023, 2.800000000000003819 ) ;
#8454=EDGE_CURVE ( 'NONE', #7962, #12032, #10590, .T. ) ;
#8457=ORIENTED_EDGE ( 'NONE', *, *, #3565, .T. ) ;
#8459=VERTEX_POINT ( 'NONE', #2449 ) ;
#8460=DIRECTION ( 'NONE',  ( 1.000000000000000000, -1.010728034814421376E-30, -1.090846720500930387E-30 ) ) ;
#8463=AXIS2_PLACEMENT_3D ( 'NONE', #7742, #8766, #9839 ) ;
#8465=ORIENTED_EDGE ( 'NONE', *, *, #603, .T. ) ;
#8468=VERTEX_POINT ( 'NONE', #6565 ) ;
#8471=ORIENTED_EDGE ( 'NONE', *, *, #8868, .T. ) ;
#8476=DIRECTION ( 'NONE',  ( 0.000000000000000000, 0.2660368455666689003, 0.9639628606958551282 ) ) ;
#8477=EDGE_CURVE ( 'NONE', #7420, #6820, #2176, .T. ) ;
#8478=DIRECTION ( 'NONE',  ( 0.000000000000000000, -0.1785568947986227173, -0.9839295885986321100 ) ) ;
#8479=ORIENTED_EDGE ( 'NONE', *, *, #11241, .F. ) ;
#8480=CYLINDRICAL_SURFACE ( 'NONE', #541, 2.800000000000003819 ) ;
#8482=CIRCLE ( 'NONE', #8284, 2.800000000000004263 ) ;
#8483=CARTESIAN_POINT ( 'NONE',  ( 9.999999999999998224, -2.171317488608444535, -7.074275960383742401 ) ) ;
#8485=ADVANCED_FACE ( 'NONE', ( #10282 ), #10479, .T. ) ;
#8486=DIRECTION ( 'NONE',  ( -1.000000000000000000, 1.010728034814421376E-30, 1.090846720500930387E-30 ) ) ;
#8487=ADVANCED_FACE ( 'NONE', ( #1666 ), #5593, .T. ) ;
#8490=CARTESIAN_POINT ( 'NONE',  ( 0.000000000000000000, 0.000000000000000000, 0.000000000000000000 ) ) ;
#8491=AXIS2_PLACEMENT_3D ( 'NONE', #6479, #1447, #5375 ) ;
#8493=ORIENTED_EDGE ( 'NONE', *, *, #4942, .F. ) ;
#8497=CARTESIAN_POINT ( 'NONE',  ( 19.99999999999999645, 2.180689217871860652, 6.122221454264574092 ) ) ;
#8498=CIRCLE ( 'NONE', #10752, 2.800000000000002931 ) ;
#8502=CARTESIAN_POINT ( 'NONE',  ( 9.999999999999998224, -0.8732627748487576946, -7.348293143721449816 ) ) ;
#8504=ADVANCED_FACE ( 'NONE', ( #5948, #987 ), #8787, .F. ) ;
#8505=DIRECTION ( 'NONE',  ( 0.000000000000000000, 0.2660368455666689003, 0.9639628606958551282 ) ) ;
#8506=CIRCLE ( 'NONE', #5839, 6.499000000000006771 ) ;
#8509=CARTESIAN_POINT ( 'NONE',  ( 19.99999999999999645, 0.000000000000000000, 0.000000000000000000 ) ) ;
#8510=CYLINDRICAL_SURFACE ( 'NONE', #12497, 7.400000000000010125 ) ;
#8511=DIRECTION ( 'NONE',  ( 1.140150527077241873E-30, 0.000000000000000000, -1.000000000000000000 ) ) ;
#8513=CIRCLE ( 'NONE', #4817, 2.800000000000003819 ) ;
#8517=EDGE_CURVE ( 'NONE', #12737, #8539, #7724, .T. ) ;
#8521=ORIENTED_EDGE ( 'NONE', *, *, #3132, .F. ) ;
#8523=ORIENTED_EDGE ( 'NONE', *, *, #8692, .T. ) ;
#8525=CARTESIAN_POINT ( 'NONE',  ( 19.99999999999997868, 6.496448636052932990, 0.1820882179769736653 ) ) ;
#8529=DIRECTION ( 'NONE',  ( 0.000000000000000000, 0.000000000000000000, 1.000000000000000000 ) ) ;
#8531=EDGE_CURVE ( 'NONE', #3047, #8975, #5462, .T. ) ;
#8532=CYLINDRICAL_SURFACE ( 'NONE', #7914, 6.499000000000010324 ) ;
#8533=FACE_OUTER_BOUND ( 'NONE', #2423, .T. ) ;
#8534=ORIENTED_EDGE ( 'NONE', *, *, #132, .T. ) ;
#8537=LINE ( 'NONE', #10715, #2248 ) ;
#8539=VERTEX_POINT ( 'NONE', #5115 ) ;
#8541=ORIENTED_EDGE ( 'NONE', *, *, #11482, .F. ) ;
#8543=DIRECTION ( 'NONE',  ( -1.417484439069003136E-30, 0.9195277725514489076, 0.3930250316539277144 ) ) ;
#8544=ORIENTED_EDGE ( 'NONE', *, *, #2030, .T. ) ;
#8546=AXIS2_PLACEMENT_3D ( 'NONE', #9027, #4336, #3388 ) ;
#8549=CARTESIAN_POINT ( 'NONE',  ( 0.000000000000000000, 1.395418990828293460, -6.428133065596405515 ) ) ;
#8559=VERTEX_POINT ( 'NONE', #5823 ) ;
#8560=DIRECTION ( 'NONE',  ( -1.000000000000000000, 1.010728034814421376E-30, 1.090846720500930387E-30 ) ) ;
#8564=CIRCLE ( 'NONE', #332, 6.499000000000009436 ) ;
#8565=VECTOR ( 'NONE', #859, 1000.000000000000000 ) ;
#8567=CYLINDRICAL_SURFACE ( 'NONE', #2040, 6.499000000000010324 ) ;
#8569=VERTEX_POINT ( 'NONE', #6076 ) ;
#8572=LINE ( 'NONE', #12513, #5389 ) ;
#8573=AXIS2_PLACEMENT_3D ( 'NONE', #9269, #4131, #329 ) ;
#8576=CARTESIAN_POINT ( 'NONE',  ( 0.000000000000000000, 0.4528593230175778639, -7.386130139224209579 ) ) ;
#8577=DIRECTION ( 'NONE',  ( 0.000000000000000000, 0.000000000000000000, 1.000000000000000000 ) ) ;
#8585=DIRECTION ( 'NONE',  ( -1.000000000000000000, 1.010728034814421376E-30, 1.090846720500930387E-30 ) ) ;
#8587=VERTEX_POINT ( 'NONE', #31 ) ;
#8595=DIRECTION ( 'NONE',  ( 0.000000000000000000, 0.000000000000000000, 1.000000000000000000 ) ) ;
#8596=ORIENTED_EDGE ( 'NONE', *, *, #11784, .T. ) ;
#8599=CARTESIAN_POINT ( 'NONE',  ( 19.99999999999999645, -4.357840574720623472, 4.821434073521965402 ) ) ;
#8603=ORIENTED_EDGE ( 'NONE', *, *, #12134, .F. ) ;
#8605=DIRECTION ( 'NONE',  ( 0.000000000000000000, 0.000000000000000000, 1.000000000000000000 ) ) ;
#8606=ORIENTED_EDGE ( 'NONE', *, *, #8845, .F. ) ;
#8609=ORIENTED_EDGE ( 'NONE', *, *, #2000, .F. ) ;
#8611=CARTESIAN_POINT ( 'NONE',  ( 19.99999999999999645, 0.000000000000000000, 0.000000000000000000 ) ) ;
#8616=AXIS2_PLACEMENT_3D ( 'NONE', #9695, #5978, #11657 ) ;
#8619=CYLINDRICAL_SURFACE ( 'NONE', #8286, 6.499000000000010324 ) ;
#8630=EDGE_CURVE ( 'NONE', #7387, #7959, #503, .T. ) ;
#8632=ORIENTED_EDGE ( 'NONE', *, *, #5621, .F. ) ;
#8637=EDGE_CURVE ( 'NONE', #490, #11957, #6885, .T. ) ;
#8642=DIRECTION ( 'NONE',  ( 1.503766100577551477E-30, -0.6579387259397028176, -0.7530714660036194052 ) ) ;
#8644=EDGE_CURVE ( 'NONE', #5144, #5654, #1736, .T. ) ;
#8645=DIRECTION ( 'NONE',  ( -1.000000000000000000, 1.010728034814421376E-30, 1.090846720500930387E-30 ) ) ;
#8646=DIRECTION ( 'NONE',  ( 0.000000000000000000, 0.000000000000000000, 1.000000000000000000 ) ) ;
#8647=FACE_OUTER_BOUND ( 'NONE', #4739, .T. ) ;
#8649=AXIS2_PLACEMENT_3D ( 'NONE', #10134, #9174, #9237 ) ;
#8654=CARTESIAN_POINT ( 'NONE',  ( 19.99999999999999645, -5.932103089875941038, 2.654647609586679113 ) ) ;
#8655=ADVANCED_FACE ( 'NONE', ( #2290 ), #8064, .T. ) ;
#8657=VERTEX_POINT ( 'NONE', #9097 ) ;
#8658=VERTEX_POINT ( 'NONE', #3390 ) ;
#8664=CARTESIAN_POINT ( 'NONE',  ( 19.99999999999999645, 0.000000000000000000, 0.000000000000000000 ) ) ;
#8672=DIRECTION ( 'NONE',  ( -1.000000000000000000, 1.010728034814421376E-30, 1.090846720500930387E-30 ) ) ;
#8674=VECTOR ( 'NONE', #842, 1000.000000000000000 ) ;
#8675=DIRECTION ( 'NONE',  ( -1.000000000000000000, 1.010728034814421376E-30, 1.090846720500930387E-30 ) ) ;
#8676=DIRECTION ( 'NONE',  ( 0.000000000000000000, 0.000000000000000000, 1.000000000000000000 ) ) ;
#8683=CIRCLE ( 'NONE', #2748, 7.400000000000009237 ) ;
#8686=VERTEX_POINT ( 'NONE', #8196 ) ;
#8687=DIRECTION ( 'NONE',  ( -1.000000000000000000, 1.010728034814421376E-30, 1.090846720500930387E-30 ) ) ;
#8691=CIRCLE ( 'NONE', #5408, 2.800000000000003819 ) ;
#8692=EDGE_CURVE ( 'NONE', #5655, #8777, #5240, .T. ) ;
#8694=EDGE_CURVE ( 'NONE', #245, #10621, #7491, .T. ) ;
#8697=ORIENTED_EDGE ( 'NONE', *, *, #8644, .F. ) ;
#8699=CIRCLE ( 'NONE', #8070, 2.800000000000002487 ) ;
#8701=VERTEX_POINT ( 'NONE', #11168 ) ;
#8704=VECTOR ( 'NONE', #12231, 1000.000000000000000 ) ;
#8706=CARTESIAN_POINT ( 'NONE',  ( 19.99999999999999645, 0.000000000000000000, 0.000000000000000000 ) ) ;
#8707=CARTESIAN_POINT ( 'NONE',  ( 19.99999999999997868, 1.531833341630222112, -6.396997380212695816 ) ) ;
#8708=DIRECTION ( 'NONE',  ( -1.000000000000000000, 1.010728034814421376E-30, 1.090846720500930387E-30 ) ) ;
#8709=AXIS2_PLACEMENT_3D ( 'NONE', #1888, #6671, #5881 ) ;
#8710=DIRECTION ( 'NONE',  ( 0.000000000000000000, 0.000000000000000000, 1.000000000000000000 ) ) ;
#8715=DIRECTION ( 'NONE',  ( -1.000000000000000000, 1.010728034814421376E-30, 1.090846720500930387E-30 ) ) ;
#8718=ORIENTED_EDGE ( 'NONE', *, *, #2404, .F. ) ;
#8721=CARTESIAN_POINT ( 'NONE',  ( 19.99999999999997868, 6.613766744932294550, -3.319350756341939324 ) ) ;
#8723=EDGE_CURVE ( 'NONE', #7062, #6148, #904, .T. ) ;
#8728=ORIENTED_EDGE ( 'NONE', *, *, #12698, .F. ) ;
#8736=CARTESIAN_POINT ( 'NONE',  ( 0.000000000000000000, -6.133480037816505082, 2.376659734729468010 ) ) ;
#8738=CARTESIAN_POINT ( 'NONE',  ( 0.000000000000000000, 6.544726022087258066, 0.6592800351837291295 ) ) ;
#8739=CYLINDRICAL_SURFACE ( 'NONE', #9735, 2.500000000000003553 ) ;
#8742=CARTESIAN_POINT ( 'NONE',  ( 19.99999999999999645, -3.178467454237171363, 5.758943784352557493 ) ) ;
#8750=ORIENTED_EDGE ( 'NONE', *, *, #11401, .F. ) ;
#8755=DIRECTION ( 'NONE',  ( -4.683861624749751464E-31, -0.4338837391175658365, 0.9009688679024154823 ) ) ;
#8756=CARTESIAN_POINT ( 'NONE',  ( 19.99999999999997868, 6.321830586517952710, -1.817291089601262621 ) ) ;
#8760=CARTESIAN_POINT ( 'NONE',  ( 19.99999999999999645, 0.000000000000000000, 0.000000000000000000 ) ) ;
#8764=CARTESIAN_POINT ( 'NONE',  ( 0.000000000000000000, 0.2110513566294476284, -7.396989747516558467 ) ) ;
#8765=VECTOR ( 'NONE', #4799, 1000.000000000000000 ) ;
#8766=DIRECTION ( 'NONE',  ( -1.000000000000000000, 1.010728034814421376E-30, 1.090846720500930387E-30 ) ) ;
#8768=DIRECTION ( 'NONE',  ( 0.000000000000000000, 0.3513748240813434620, -0.9362348706397368714 ) ) ;
#8773=AXIS2_PLACEMENT_3D ( 'NONE', #4207, #6200, #9155 ) ;
#8777=VERTEX_POINT ( 'NONE', #12333 ) ;
#8778=ORIENTED_EDGE ( 'NONE', *, *, #3549, .F. ) ;
#8784=ORIENTED_EDGE ( 'NONE', *, *, #10392, .F. ) ;
#8785=AXIS2_PLACEMENT_3D ( 'NONE', #654, #9397, #5495 ) ;
#8787=PLANE ( 'NONE',  #11011 ) ;
#8788=ORIENTED_EDGE ( 'NONE', *, *, #9954, .F. ) ;
#8789=ORIENTED_EDGE ( 'NONE', *, *, #5150, .F. ) ;
#8790=DIRECTION ( 'NONE',  ( -1.000000000000000000, 1.010728034814421376E-30, 1.090846720500930387E-30 ) ) ;
#8797=FACE_OUTER_BOUND ( 'NONE', #1130, .T. ) ;
#8799=DIRECTION ( 'NONE',  ( -1.140150527077241873E-30, 0.000000000000000000, 1.000000000000000000 ) ) ;
#8802=CYLINDRICAL_SURFACE ( 'NONE', #5708, 7.400000000000010125 ) ;
#8808=CARTESIAN_POINT ( 'NONE',  ( 0.000000000000000000, 6.544726022087268724, -0.6592800351836389794 ) ) ;
#8810=FACE_OUTER_BOUND ( 'NONE', #9495, .T. ) ;
#8812=EDGE_LOOP ( 'NONE', ( #2048, #10914, #11972, #10775 ) ) ;
#8816=ORIENTED_EDGE ( 'NONE', *, *, #3741, .T. ) ;
#8817=VECTOR ( 'NONE', #12489, 1000.000000000000000 ) ;
#8823=AXIS2_PLACEMENT_3D ( 'NONE', #7521, #4566, #8478 ) ;
#8829=DIRECTION ( 'NONE',  ( -1.000000000000000000, 1.010728034814421376E-30, 1.090846720500930387E-30 ) ) ;
#8831=CIRCLE ( 'NONE', #3708, 2.800000000000003819 ) ;
#8835=ORIENTED_EDGE ( 'NONE', *, *, #8692, .F. ) ;
#8836=CARTESIAN_POINT ( 'NONE',  ( 0.000000000000000000, 4.596015818000077857, 4.705818469689517336 ) ) ;
#8838=CIRCLE ( 'NONE', #4946, 2.800000000000003819 ) ;
#8840=VECTOR ( 'NONE', #11763, 1000.000000000000000 ) ;
#8841=CARTESIAN_POINT ( 'NONE',  ( 19.99999999999999645, -2.401522331692910850, 6.999477872697376313 ) ) ;
#8843=ADVANCED_FACE ( 'NONE', ( #2679 ), #8452, .T. ) ;
#8845=EDGE_CURVE ( 'NONE', #5492, #8301, #1758, .T. ) ;
#8848=LINE ( 'NONE', #6867, #11334 ) ;
#8849=ORIENTED_EDGE ( 'NONE', *, *, #4952, .F. ) ;
#8850=EDGE_LOOP ( 'NONE', ( #5191, #5248, #2778, #6887 ) ) ;
#8854=VERTEX_POINT ( 'NONE', #7684 ) ;
#8855=EDGE_CURVE ( 'NONE', #6259, #9874, #8513, .T. ) ;
#8856=DIRECTION ( 'NONE',  ( 0.000000000000000000, -0.6579387259397027066, -0.7530714660036197383 ) ) ;
#8859=CARTESIAN_POINT ( 'NONE',  ( 19.99999999999999645, 0.3649881613860001539, 6.567714405409708078 ) ) ;
#8861=CARTESIAN_POINT ( 'NONE',  ( 0.000000000000000000, -4.621065432155046615, -4.569765340993108715 ) ) ;
#8862=DIRECTION ( 'NONE',  ( -1.000000000000000000, 1.010728034814421376E-30, 1.090846720500930387E-30 ) ) ;
#8863=( GEOMETRIC_REPRESENTATION_CONTEXT ( 3 ) GLOBAL_UNCERTAINTY_ASSIGNED_CONTEXT ( ( #5594 ) ) GLOBAL_UNIT_ASSIGNED_CONTEXT ( ( #2132, #4968, #5161 ) ) REPRESENTATION_CONTEXT ( 'NONE', 'WORKASPACE' ) );
#8868=EDGE_CURVE ( 'NONE', #8334, #3019, #6467, .T. ) ;
#8870=ORIENTED_EDGE ( 'NONE', *, *, #8296, .T. ) ;
#8875=EDGE_CURVE ( 'NONE', #1901, #5655, #5228, .T. ) ;
#8877=CIRCLE ( 'NONE', #2940, 2.800000000000004263 ) ;
#8884=AXIS2_PLACEMENT_3D ( 'NONE', #8760, #11799, #2986 ) ;
#8886=DIRECTION ( 'NONE',  ( -1.000000000000000000, 1.010728034814421376E-30, 1.090846720500930387E-30 ) ) ;
#8889=DIRECTION ( 'NONE',  ( 1.405158487424925176E-30, -0.3513748240813304724, -0.9362348706397417564 ) ) ;
#8890=AXIS2_PLACEMENT_3D ( 'NONE', #3505, #5424, #12262 ) ;
#8891=EDGE_CURVE ( 'NONE', #10207, #1374, #6723, .T. ) ;
#8894=CARTESIAN_POINT ( 'NONE',  ( 19.99999999999997868, -7.399010254356654492, 0.1210258481698887889 ) ) ;
#8897=ORIENTED_EDGE ( 'NONE', *, *, #7941, .F. ) ;
#8898=CYLINDRICAL_SURFACE ( 'NONE', #1699, 2.800000000000003819 ) ;
#8899=DIRECTION ( 'NONE',  ( -1.000000000000000000, 1.010728034814421376E-30, 1.090846720500930387E-30 ) ) ;
#8900=CARTESIAN_POINT ( 'NONE',  ( 0.000000000000000000, -4.907279493584705499, -4.380262188593400552 ) ) ;
#8901=DIRECTION ( 'NONE',  ( -1.244921116051907329E-30, 0.2660368455666687892, 0.9639628606958550172 ) ) ;
#8902=DIRECTION ( 'NONE',  ( -1.000000000000000000, 1.010728034814421376E-30, 1.090846720500930387E-30 ) ) ;
#8904=CARTESIAN_POINT ( 'NONE',  ( 0.000000000000000000, 6.018220532833765901, 2.453165835849275389 ) ) ;
#8905=EDGE_CURVE ( 'NONE', #9566, #4626, #3399, .T. ) ;
#8906=CARTESIAN_POINT ( 'NONE',  ( 0.000000000000000000, 0.000000000000000000, 0.000000000000000000 ) ) ;
#8908=VERTEX_POINT ( 'NONE', #5745 ) ;
#8909=VECTOR ( 'NONE', #1363, 1000.000000000000000 ) ;
#8910=ORIENTED_EDGE ( 'NONE', *, *, #5888, .T. ) ;
#8911=CARTESIAN_POINT ( 'NONE',  ( 19.99999999999999645, -4.999339924971525129, -4.274890546384038537 ) ) ;
#8912=ORIENTED_EDGE ( 'NONE', *, *, #9386, .F. ) ;
#8915=EDGE_CURVE ( 'NONE', #12228, #11905, #4470, .T. ) ;
#8916=DIRECTION ( 'NONE',  ( -1.000000000000000000, 1.010728034814421376E-30, 1.090846720500930387E-30 ) ) ;
#8917=EDGE_CURVE ( 'NONE', #5257, #175, #2547, .T. ) ;
#8925=CARTESIAN_POINT ( 'NONE',  ( 19.99999999999999645, -4.357840574720558635, -4.821434073522041786 ) ) ;
#8926=AXIS2_PLACEMENT_3D ( 'NONE', #5564, #594, #11429 ) ;
#8930=DIRECTION ( 'NONE',  ( 1.140150527077241873E-30, 0.000000000000000000, -1.000000000000000000 ) ) ;
#8933=CYLINDRICAL_SURFACE ( 'NONE', #6777, 6.499000000000010324 ) ;
#8935=AXIS2_PLACEMENT_3D ( 'NONE', #2793, #3803, #6707 ) ;
#8936=AXIS2_PLACEMENT_3D ( 'NONE', #4816, #11461, #2642 ) ;
#8937=DIRECTION ( 'NONE',  ( -1.140150527077241873E-30, 0.000000000000000000, 1.000000000000000000 ) ) ;
#8938=EDGE_CURVE ( 'NONE', #3010, #477, #10879, .T. ) ;
#8941=ORIENTED_EDGE ( 'NONE', *, *, #6280, .F. ) ;
#8943=AXIS2_PLACEMENT_3D ( 'NONE', #897, #6956, #10866 ) ;
#8947=EDGE_CURVE ( 'NONE', #6820, #6211, #4723, .T. ) ;
#8948=FACE_OUTER_BOUND ( 'NONE', #12423, .T. ) ;
#8949=EDGE_CURVE ( 'NONE', #5688, #9218, #12547, .T. ) ;
#8955=DIRECTION ( 'NONE',  ( 0.000000000000000000, 0.1785568947986370392, -0.9839295885986295565 ) ) ;
#8960=ORIENTED_EDGE ( 'NONE', *, *, #4861, .F. ) ;
#8962=DIRECTION ( 'NONE',  ( -1.000000000000000000, 1.010728034814421376E-30, 1.090846720500930387E-30 ) ) ;
#8963=CARTESIAN_POINT ( 'NONE',  ( 19.99999999999999645, 0.000000000000000000, 0.000000000000000000 ) ) ;
#8965=CARTESIAN_POINT ( 'NONE',  ( 0.000000000000000000, 5.956456411769377901, 2.790827096699005416 ) ) ;
#8970=AXIS2_PLACEMENT_3D ( 'NONE', #12159, #4284, #8213 ) ;
#8975=VERTEX_POINT ( 'NONE', #10696 ) ;
#8976=ORIENTED_EDGE ( 'NONE', *, *, #9225, .T. ) ;
#8980=CIRCLE ( 'NONE', #2620, 7.400000000000011902 ) ;
#8982=CYLINDRICAL_SURFACE ( 'NONE', #11383, 2.800000000000003819 ) ;
#8983=ORIENTED_EDGE ( 'NONE', *, *, #4062, .F. ) ;
#8984=CARTESIAN_POINT ( 'NONE',  ( 19.99999999999999645, 5.012092988313947117, 4.137139697483554812 ) ) ;
#8985=LINE ( 'NONE', #6218, #4893 ) ;
#8986=CARTESIAN_POINT ( 'NONE',  ( 19.99999999999997868, -1.966014849756994254, -6.277170897746295886 ) ) ;
#8989=ORIENTED_EDGE ( 'NONE', *, *, #6604, .F. ) ;
#8994=LINE ( 'NONE', #1074, #4998 ) ;
#9000=DIRECTION ( 'NONE',  ( -1.000000000000000000, 1.010728034814421376E-30, 1.090846720500930387E-30 ) ) ;
#9001=EDGE_CURVE ( 'NONE', #5654, #4676, #12130, .T. ) ;
#9003=CARTESIAN_POINT ( 'NONE',  ( 9.999999999999998224, 7.164568425986761468, 1.851744925564471123 ) ) ;
#9006=ORIENTED_EDGE ( 'NONE', *, *, #2187, .F. ) ;
#9007=CARTESIAN_POINT ( 'NONE',  ( 0.000000000000000000, 0.000000000000000000, 0.000000000000000000 ) ) ;
#9010=CARTESIAN_POINT ( 'NONE',  ( 0.000000000000000000, -1.966014849757081073, 6.277170897746257694 ) ) ;
#9014=DIRECTION ( 'NONE',  ( -1.000000000000000000, 1.010728034814421376E-30, 1.090846720500930387E-30 ) ) ;
#9015=EDGE_CURVE ( 'NONE', #7169, #11765, #6577, .T. ) ;
#9016=DIRECTION ( 'NONE',  ( 1.000000000000000000, -1.010728034814421376E-30, -1.090846720500930387E-30 ) ) ;
#9021=ORIENTED_EDGE ( 'NONE', *, *, #9001, .F. ) ;
#9025=DIRECTION ( 'NONE',  ( -2.126226658603505754E-31, 0.7818314824680310249, -0.6234898018587319291 ) ) ;
#9027=CARTESIAN_POINT ( 'NONE',  ( 0.000000000000000000, 1.395418990828199757, 6.428133065596412621 ) ) ;
#9029=( GEOMETRIC_REPRESENTATION_CONTEXT ( 3 ) GLOBAL_UNCERTAINTY_ASSIGNED_CONTEXT ( ( #6603 ) ) GLOBAL_UNIT_ASSIGNED_CONTEXT ( ( #1565, #12078, #3330 ) ) REPRESENTATION_CONTEXT ( 'NONE', 'WORKASPACE' ) );
#9030=AXIS2_PLACEMENT_3D ( 'NONE', #6147, #286, #9873 ) ;
#9031=EDGE_CURVE ( 'NONE', #2105, #2119, #10821, .T. ) ;
#9036=CYLINDRICAL_SURFACE ( 'NONE', #10294, 7.400000000000010125 ) ;
#9038=VERTEX_POINT ( 'NONE', #4006 ) ;
#9042=CIRCLE ( 'NONE', #10889, 6.499000000000009436 ) ;
#9046=DIRECTION ( 'NONE',  ( 0.000000000000000000, 0.000000000000000000, 1.000000000000000000 ) ) ;
#9049=DIRECTION ( 'NONE',  ( 0.000000000000000000, -0.8345732537213080837, 0.5508969814520944253 ) ) ;
#9050=DIRECTION ( 'NONE',  ( -1.140150527077241873E-30, 0.000000000000000000, 1.000000000000000000 ) ) ;
#9053=ORIENTED_EDGE ( 'NONE', *, *, #9491, .T. ) ;
#9055=EDGE_CURVE ( 'NONE', #4761, #10601, #7394, .T. ) ;
#9056=ORIENTED_EDGE ( 'NONE', *, *, #3740, .T. ) ;
#9058=CARTESIAN_POINT ( 'NONE',  ( 19.99999999999999645, -6.133480037816472219, -2.376659734729558160 ) ) ;
#9059=EDGE_CURVE ( 'NONE', #8468, #10149, #2886, .T. ) ;
#9062=CYLINDRICAL_SURFACE ( 'NONE', #10868, 7.400000000000010125 ) ;
#9063=MECHANICAL_DESIGN_GEOMETRIC_PRESENTATION_REPRESENTATION('',(#7841),#8863);
#9064=VERTEX_POINT ( 'NONE', #7925 ) ;
#9065=CARTESIAN_POINT ( 'NONE',  ( 19.99999999999999645, -2.099089055167807860, 6.233932467347772288 ) ) ;
#9066=DIRECTION ( 'NONE',  ( -1.000000000000000000, 1.010728034814421376E-30, 1.090846720500930387E-30 ) ) ;
#9067=CARTESIAN_POINT ( 'NONE',  ( 50.00005079999998969, 5.204170427930421283E-15, -6.938893903907228378E-15 ) ) ;
#9069=CIRCLE ( 'NONE', #1678, 7.400000000000011902 ) ;
#9071=VERTEX_POINT ( 'NONE', #78 ) ;
#9072=CARTESIAN_POINT ( 'NONE',  ( 19.99999999999999645, 0.000000000000000000, 0.000000000000000000 ) ) ;
#9076=EDGE_CURVE ( 'NONE', #7377, #6343, #9228, .T. ) ;
#9079=AXIS2_PLACEMENT_3D ( 'NONE', #9646, #649, #12580 ) ;
#9084=CARTESIAN_POINT ( 'NONE',  ( 0.000000000000000000, -7.301715115245771770, -1.202063382601599395 ) ) ;
#9088=ORIENTED_EDGE ( 'NONE', *, *, #4895, .F. ) ;
#9090=CARTESIAN_POINT ( 'NONE',  ( 19.99999999999999645, -5.651611091574776147, -4.776954267060665060 ) ) ;
#9091=DIRECTION ( 'NONE',  ( -1.000000000000000000, 1.010728034814421376E-30, 1.090846720500930387E-30 ) ) ;
#9092=DIRECTION ( 'NONE',  ( -1.000000000000000000, 1.010728034814421376E-30, 1.090846720500930387E-30 ) ) ;
#9093=ORIENTED_EDGE ( 'NONE', *, *, #2169, .T. ) ;
#9095=CYLINDRICAL_SURFACE ( 'NONE', #5463, 2.800000000000003819 ) ;
#9096=AXIS2_PLACEMENT_3D ( 'NONE', #1330, #9245, #7139 ) ;
#9097=CARTESIAN_POINT ( 'NONE',  ( 0.000000000000000000, -6.213893036447822205, 1.903820982021506403 ) ) ;
#9102=AXIS2_PLACEMENT_3D ( 'NONE', #10916, #5126, #9046 ) ;
#9105=CIRCLE ( 'NONE', #8075, 7.400000000000009237 ) ;
#9106=CARTESIAN_POINT ( 'NONE',  ( 19.99999999999997868, 2.520781513113738548, -6.075668640744172677 ) ) ;
#9108=EDGE_CURVE ( 'NONE', #753, #11058, #3438, .T. ) ;
#9109=CARTESIAN_POINT ( 'NONE',  ( 10.00000000000000178, 6.613766744932252806, 3.319350756342029474 ) ) ;
#9110=CARTESIAN_POINT ( 'NONE',  ( 0.000000000000000000, -6.289597356626462243, -3.898841506334620011 ) ) ;
#9122=CIRCLE ( 'NONE', #8309, 7.400000000000011902 ) ;
#9124=ORIENTED_EDGE ( 'NONE', *, *, #6057, .F. ) ;
#9126=VERTEX_POINT ( 'NONE', #8312 ) ;
#9127=DIRECTION ( 'NONE',  ( -1.000000000000000000, 1.010728034814421376E-30, 1.090846720500930387E-30 ) ) ;
#9129=EDGE_CURVE ( 'NONE', #3793, #6015, #1010, .T. ) ;
#9130=DIRECTION ( 'NONE',  ( -1.140150527077241873E-30, 0.000000000000000000, 1.000000000000000000 ) ) ;
#9133=FACE_OUTER_BOUND ( 'NONE', #3497, .T. ) ;
#9134=ORIENTED_EDGE ( 'NONE', *, *, #7692, .T. ) ;
#9135=DIRECTION ( 'NONE',  ( -1.000000000000000000, 1.010728034814421376E-30, 1.090846720500930387E-30 ) ) ;
#9137=AXIS2_PLACEMENT_3D ( 'NONE', #8611, #5716, #6563 ) ;
#9141=DIRECTION ( 'NONE',  ( 0.000000000000000000, 0.08963930890342669544, 0.9959742939952396235 ) ) ;
#9143=CIRCLE ( 'NONE', #1751, 2.800000000000003819 ) ;
#9146=EDGE_CURVE ( 'NONE', #10923, #8777, #3093, .T. ) ;
#9148=ADVANCED_FACE ( 'NONE', ( #4195 ), #12255, .T. ) ;
#9153=CARTESIAN_POINT ( 'NONE',  ( 19.99999999999999645, 0.000000000000000000, 0.000000000000000000 ) ) ;
#9154=DIRECTION ( 'NONE',  ( 0.000000000000000000, 0.000000000000000000, 1.000000000000000000 ) ) ;
#9155=DIRECTION ( 'NONE',  ( 0.000000000000000000, 0.000000000000000000, 1.000000000000000000 ) ) ;
#9156=CARTESIAN_POINT ( 'NONE',  ( 0.000000000000000000, -3.399584271718293582, -6.572885726945646212 ) ) ;
#9162=CARTESIAN_POINT ( 'NONE',  ( 9.999999999999994671, -6.884685972239644514, -2.713134545806128450 ) ) ;
#9163=ORIENTED_EDGE ( 'NONE', *, *, #6435, .T. ) ;
#9165=VERTEX_POINT ( 'NONE', #12062 ) ;
#9166=DIRECTION ( 'NONE',  ( 0.000000000000000000, -0.2660368455666824450, 0.9639628606958512425 ) ) ;
#9167=DIRECTION ( 'NONE',  ( 0.000000000000000000, 0.000000000000000000, 1.000000000000000000 ) ) ;
#9169=VECTOR ( 'NONE', #11440, 1000.000000000000000 ) ;
#9170=CARTESIAN_POINT ( 'NONE',  ( 19.99999999999999645, -3.426907987218856810, 5.522074125465504579 ) ) ;
#9171=AXIS2_PLACEMENT_3D ( 'NONE', #8963, #1364, #338 ) ;
#9174=DIRECTION ( 'NONE',  ( -1.000000000000000000, 1.010728034814421376E-30, 1.090846720500930387E-30 ) ) ;
#9176=EDGE_CURVE ( 'NONE', #6667, #12656, #596, .T. ) ;
#9177=ORIENTED_EDGE ( 'NONE', *, *, #9176, .F. ) ;
#9179=EDGE_CURVE ( 'NONE', #6636, #9475, #798, .T. ) ;
#9180=VERTEX_POINT ( 'NONE', #1352 ) ;
#9181=AXIS2_PLACEMENT_3D ( 'NONE', #7047, #10962, #4015 ) ;
#9183=CIRCLE ( 'NONE', #3859, 6.499000000000009436 ) ;
#9184=CARTESIAN_POINT ( 'NONE',  ( 0.000000000000000000, 0.000000000000000000, 0.000000000000000000 ) ) ;
#9187=DIRECTION ( 'NONE',  ( -1.000000000000000000, 1.010728034814421376E-30, 1.090846720500930387E-30 ) ) ;
#9189=DIRECTION ( 'NONE',  ( 0.000000000000000000, 0.000000000000000000, 1.000000000000000000 ) ) ;
#9191=FACE_OUTER_BOUND ( 'NONE', #4424, .T. ) ;
#9193=AXIS2_PLACEMENT_3D ( 'NONE', #5252, #9233, #9050 ) ;
#9196=ORIENTED_EDGE ( 'NONE', *, *, #4614, .F. ) ;
#9202=DIRECTION ( 'NONE',  ( -1.000000000000000000, 1.010728034814421376E-30, 1.090846720500930387E-30 ) ) ;
#9203=DIRECTION ( 'NONE',  ( -1.000000000000000000, 1.010728034814421376E-30, 1.090846720500930387E-30 ) ) ;
#9205=LINE ( 'NONE', #12126, #4827 ) ;
#9206=DIRECTION ( 'NONE',  ( 1.000000000000000000, -1.010728034814421376E-30, -1.090846720500930387E-30 ) ) ;
#9209=DIRECTION ( 'NONE',  ( -1.000000000000000000, 1.010728034814421376E-30, 1.090846720500930387E-30 ) ) ;
#9211=DIRECTION ( 'NONE',  ( 0.000000000000000000, 0.000000000000000000, 1.000000000000000000 ) ) ;
#9212=CARTESIAN_POINT ( 'NONE',  ( 19.99999999999999645, -6.459281472512932609, 1.556709314830556412 ) ) ;
#9218=VERTEX_POINT ( 'NONE', #11022 ) ;
#9220=ORIENTED_EDGE ( 'NONE', *, *, #10392, .T. ) ;
#9224=ORIENTED_EDGE ( 'NONE', *, *, #11193, .F. ) ;
#9225=EDGE_CURVE ( 'NONE', #12043, #11154, #5226, .T. ) ;
#9227=ADVANCED_FACE ( 'NONE', ( #12192 ), #7293, .T. ) ;
#9228=CIRCLE ( 'NONE', #11914, 7.400000000000009237 ) ;
#9230=CYLINDRICAL_SURFACE ( 'NONE', #8006, 6.499000000000010324 ) ;
#9232=AXIS2_PLACEMENT_3D ( 'NONE', #5553, #586, #7482 ) ;
#9233=DIRECTION ( 'NONE',  ( -1.000000000000000000, 1.010728034814421376E-30, 1.090846720500930387E-30 ) ) ;
#9234=VERTEX_POINT ( 'NONE', #3625 ) ;
#9235=DIRECTION ( 'NONE',  ( -1.000000000000000000, 1.010728034814421376E-30, 1.090846720500930387E-30 ) ) ;
#9237=DIRECTION ( 'NONE',  ( -1.392832535780847392E-30, 0.8345732537213000901, 0.5508969814521065267 ) ) ;
#9240=ORIENTED_EDGE ( 'NONE', *, *, #2202, .F. ) ;
#9241=AXIS2_PLACEMENT_3D ( 'NONE', #11546, #10555, #11477 ) ;
#9243=AXIS2_PLACEMENT_3D ( 'NONE', #3254, #8185, #2340 ) ;
#9245=DIRECTION ( 'NONE',  ( -1.000000000000000000, 1.010728034814421376E-30, 1.090846720500930387E-30 ) ) ;
#9246=DIRECTION ( 'NONE',  ( -1.000000000000000000, 1.010728034814421376E-30, 1.090846720500930387E-30 ) ) ;
#9248=DIRECTION ( 'NONE',  ( -1.000000000000000000, 1.010728034814421376E-30, 1.090846720500930387E-30 ) ) ;
#9250=CARTESIAN_POINT ( 'NONE',  ( 0.000000000000000000, 4.177097350749788163, 6.108343287861209170 ) ) ;
#9251=CARTESIAN_POINT ( 'NONE',  ( 19.99999999999999645, 4.192831774278975132, 4.965597920955411304 ) ) ;
#9252=CIRCLE ( 'NONE', #10896, 6.499000000000008548 ) ;
#9257=EDGE_LOOP ( 'NONE', ( #6839, #7715, #2651, #3666 ) ) ;
#9265=ADVANCED_FACE ( 'NONE', ( #9388 ), #4703, .T. ) ;
#9267=CARTESIAN_POINT ( 'NONE',  ( 19.99999999999997868, 6.544726022087268724, 2.140719964816364840 ) ) ;
#9269=CARTESIAN_POINT ( 'NONE',  ( 0.000000000000000000, -5.682309657208322484, -3.313524683562052431 ) ) ;
#9272=DIRECTION ( 'NONE',  ( -1.244921116051907679E-30, 0.2660368455666687337, 0.9639628606958550172 ) ) ;
#9275=AXIS2_PLACEMENT_3D ( 'NONE', #6605, #12720, #9596 ) ;
#9284=CIRCLE ( 'NONE', #9079, 2.800000000000003819 ) ;
#9285=VERTEX_POINT ( 'NONE', #4516 ) ;
#9289=ORIENTED_EDGE ( 'NONE', *, *, #1789, .F. ) ;
#9294=CARTESIAN_POINT ( 'NONE',  ( 19.99999999999999645, 0.000000000000000000, 0.000000000000000000 ) ) ;
#9299=ORIENTED_EDGE ( 'NONE', *, *, #7462, .F. ) ;
#9301=ADVANCED_FACE ( 'NONE', ( #7419 ), #8567, .T. ) ;
#9303=AXIS2_PLACEMENT_3D ( 'NONE', #10860, #7784, #8930 ) ;
#9304=EDGE_CURVE ( 'NONE', #753, #5492, #7598, .T. ) ;
#9305=ORIENTED_EDGE ( 'NONE', *, *, #4711, .F. ) ;
#9309=CARTESIAN_POINT ( 'NONE',  ( 20.00000000000000000, 0.000000000000000000, 0.000000000000000000 ) ) ;
#9314=DIRECTION ( 'NONE',  ( 7.241496590895994765E-32, 0.6579387259397138088, -0.7530714660036099684 ) ) ;
#9316=EDGE_LOOP ( 'NONE', ( #7576, #5701, #7687, #2080 ) ) ;
#9317=CIRCLE ( 'NONE', #1515, 6.499000000000006771 ) ;
#9322=FACE_OUTER_BOUND ( 'NONE', #1648, .T. ) ;
#9323=AXIS2_PLACEMENT_3D ( 'NONE', #5182, #4337, #12012 ) ;
#9326=FACE_OUTER_BOUND ( 'NONE', #1453, .T. ) ;
#9329=ORIENTED_EDGE ( 'NONE', *, *, #6320, .T. ) ;
#9332=AXIS2_PLACEMENT_3D ( 'NONE', #6848, #4501, #4437 ) ;
#9333=DIRECTION ( 'NONE',  ( -1.000000000000000000, 1.010728034814421376E-30, 1.090846720500930387E-30 ) ) ;
#9334=EDGE_CURVE ( 'NONE', #8301, #12043, #8000, .T. ) ;
#9335=CARTESIAN_POINT ( 'NONE',  ( 0.000000000000000000, -4.999339924971583748, 4.274890546383969259 ) ) ;
#9336=ORIENTED_EDGE ( 'NONE', *, *, #6287, .T. ) ;
#9337=DIRECTION ( 'NONE',  ( -1.000000000000000000, 1.010728034814421376E-30, 1.090846720500930387E-30 ) ) ;
#9339=DIRECTION ( 'NONE',  ( -1.000000000000000000, 1.010728034814421376E-30, 1.090846720500930387E-30 ) ) ;
#9340=CARTESIAN_POINT ( 'NONE',  ( 0.000000000000000000, -6.486618105788065414, 0.4009819817179204327 ) ) ;
#9342=CIRCLE ( 'NONE', #12651, 2.800000000000003819 ) ;
#9345=SURFACE_STYLE_USAGE ( .BOTH. , #8134 ) ;
#9351=DIRECTION ( 'NONE',  ( -1.000000000000000000, 1.010728034814421376E-30, 1.090846720500930387E-30 ) ) ;
#9353=CARTESIAN_POINT ( 'NONE',  ( 0.000000000000000000, -6.577476285968329783, -0.06996125000500660884 ) ) ;
#9355=EDGE_LOOP ( 'NONE', ( #11785, #3331, #4083, #12279 ) ) ;
#9356=CYLINDRICAL_SURFACE ( 'NONE', #10159, 6.499000000000010324 ) ;
#9357=VECTOR ( 'NONE', #1497, 1000.000000000000000 ) ;
#9360=ORIENTED_EDGE ( 'NONE', *, *, #1006, .T. ) ;
#9362=VERTEX_POINT ( 'NONE', #3746 ) ;
#9364=DIRECTION ( 'NONE',  ( -1.140150527077241873E-30, 0.000000000000000000, 1.000000000000000000 ) ) ;
#9366=ORIENTED_EDGE ( 'NONE', *, *, #3854, .T. ) ;
#9367=DIRECTION ( 'NONE',  ( -1.140150527077241873E-30, 0.000000000000000000, 1.000000000000000000 ) ) ;
#9370=EDGE_LOOP ( 'NONE', ( #10060, #796, #3603, #10906 ) ) ;
#9371=CYLINDRICAL_SURFACE ( 'NONE', #1800, 2.800000000000003819 ) ;
#9373=CARTESIAN_POINT ( 'NONE',  ( 0.000000000000000000, -1.623118704078954533, 6.293050665016855838 ) ) ;
#9376=AXIS2_PLACEMENT_3D ( 'NONE', #4797, #1951, #6731 ) ;
#9377=EDGE_LOOP ( 'NONE', ( #8596, #10930, #3983, #8222 ) ) ;
#9379=DIRECTION ( 'NONE',  ( 0.000000000000000000, -0.2660368455666825005, 0.9639628606958513535 ) ) ;
#9383=CARTESIAN_POINT ( 'NONE',  ( 0.000000000000000000, 0.4528593230174703388, 7.386130139224202473 ) ) ;
#9384=VECTOR ( 'NONE', #5868, 1000.000000000000000 ) ;
#9385=EDGE_CURVE ( 'NONE', #4888, #6667, #7202, .T. ) ;
#9386=EDGE_CURVE ( 'NONE', #11644, #5515, #8831, .T. ) ;
#9387=DIRECTION ( 'NONE',  ( 0.000000000000000000, 0.000000000000000000, 1.000000000000000000 ) ) ;
#9388=FACE_OUTER_BOUND ( 'NONE', #8332, .T. ) ;
#9391=DIRECTION ( 'NONE',  ( 0.000000000000000000, 0.000000000000000000, 1.000000000000000000 ) ) ;
#9395=CYLINDRICAL_SURFACE ( 'NONE', #8890, 2.800000000000003819 ) ;
#9396=LINE ( 'NONE', #8191, #5012 ) ;
#9397=DIRECTION ( 'NONE',  ( -1.000000000000000000, 1.010728034814421376E-30, 1.090846720500930387E-30 ) ) ;
#9399=DIRECTION ( 'NONE',  ( 1.000000000000000000, -1.010728034814421376E-30, -1.090846720500930387E-30 ) ) ;
#9400=LINE ( 'NONE', #6465, #934 ) ;
#9401=EDGE_CURVE ( 'NONE', #3832, #11920, #1804, .T. ) ;
#9405=EDGE_LOOP ( 'NONE', ( #12037, #8202, #8544, #6408 ) ) ;
#9415=EDGE_CURVE ( 'NONE', #5515, #4888, #7735, .T. ) ;
#9416=DIRECTION ( 'NONE',  ( 0.000000000000000000, 0.000000000000000000, 1.000000000000000000 ) ) ;
#9418=DIRECTION ( 'NONE',  ( -1.000000000000000000, 1.010728034814421376E-30, 1.090846720500930387E-30 ) ) ;
#9420=EDGE_LOOP ( 'NONE', ( #12085, #1313, #12036, #1140 ) ) ;
#9423=ORIENTED_EDGE ( 'NONE', *, *, #3685, .T. ) ;
#9431=VECTOR ( 'NONE', #2960, 1000.000000000000000 ) ;
#9439=CIRCLE ( 'NONE', #7809, 7.400000000000009237 ) ;
#9440=DIRECTION ( 'NONE',  ( 1.140150527077241873E-30, 0.000000000000000000, -1.000000000000000000 ) ) ;
#9441=EDGE_CURVE ( 'NONE', #9126, #8587, #12559, .T. ) ;
#9444=CARTESIAN_POINT ( 'NONE',  ( 9.999999999999998224, 4.177097350749886751, -6.108343287861160320 ) ) ;
#9446=ORIENTED_EDGE ( 'NONE', *, *, #1349, .F. ) ;
#9449=AXIS2_PLACEMENT_3D ( 'NONE', #6526, #8382, #10501 ) ;
#9450=DIRECTION ( 'NONE',  ( -1.000000000000000000, 1.010728034814421376E-30, 1.090846720500930387E-30 ) ) ;
#9451=ADVANCED_FACE ( 'NONE', ( #5023 ), #12700, .T. ) ;
#9453=CARTESIAN_POINT ( 'NONE',  ( 19.99999999999997868, 5.895746314278407674, -2.916892913127022702 ) ) ;
#9457=DIRECTION ( 'NONE',  ( -1.000000000000000000, 1.010728034814421376E-30, 1.090846720500930387E-30 ) ) ;
#9461=FACE_OUTER_BOUND ( 'NONE', #1142, .T. ) ;
#9462=ORIENTED_EDGE ( 'NONE', *, *, #8855, .T. ) ;
#9463=DIRECTION ( 'NONE',  ( 0.000000000000000000, 0.3513748240813434620, -0.9362348706397368714 ) ) ;
#9468=DIRECTION ( 'NONE',  ( -1.000000000000000000, 1.010728034814421376E-30, 1.090846720500930387E-30 ) ) ;
#9470=CARTESIAN_POINT ( 'NONE',  ( 19.99999999999997868, -0.1095571986794155184, -6.498076501567039642 ) ) ;
#9474=ORIENTED_EDGE ( 'NONE', *, *, #6721, .F. ) ;
#9475=VERTEX_POINT ( 'NONE', #3046 ) ;
#9476=DIRECTION ( 'NONE',  ( -1.000000000000000000, 1.010728034814421376E-30, 1.090846720500930387E-30 ) ) ;
#9477=CARTESIAN_POINT ( 'NONE',  ( 19.99999999999999645, -4.999339924971576643, 4.274890546383965706 ) ) ;
#9482=DIRECTION ( 'NONE',  ( -1.000000000000000000, 1.010728034814421376E-30, 1.090846720500930387E-30 ) ) ;
#9483=VECTOR ( 'NONE', #9521, 1000.000000000000000 ) ;
#9484=EDGE_CURVE ( 'NONE', #8975, #9071, #7808, .T. ) ;
#9485=CARTESIAN_POINT ( 'NONE',  ( 19.99999999999999645, 0.6915992404089836842, 6.462096524400245734 ) ) ;
#9487=ORIENTED_EDGE ( 'NONE', *, *, #1716, .T. ) ;
#9489=VERTEX_POINT ( 'NONE', #4051 ) ;
#9491=EDGE_CURVE ( 'NONE', #7331, #10149, #4522, .T. ) ;
#9494=LINE ( 'NONE', #8353, #7530 ) ;
#9495=EDGE_LOOP ( 'NONE', ( #2097, #3, #4763, #12018 ) ) ;
#9496=EDGE_CURVE ( 'NONE', #5504, #3477, #7024, .T. ) ;
#9500=CARTESIAN_POINT ( 'NONE',  ( 19.99999999999997868, -0.1095571986794155184, -6.498076501567039642 ) ) ;
#9502=DIRECTION ( 'NONE',  ( 0.000000000000000000, 0.000000000000000000, 1.000000000000000000 ) ) ;
#9503=AXIS2_PLACEMENT_3D ( 'NONE', #3384, #6069, #9211 ) ;
#9504=DIRECTION ( 'NONE',  ( 0.000000000000000000, 0.7818314824680310249, -0.6234898018587319291 ) ) ;
#9505=CIRCLE ( 'NONE', #10543, 6.499000000000009436 ) ;
#9506=ORIENTED_EDGE ( 'NONE', *, *, #3391, .T. ) ;
#9507=ORIENTED_EDGE ( 'NONE', *, *, #687, .F. ) ;
#9509=AXIS2_PLACEMENT_3D ( 'NONE', #12280, #8460, #5508 ) ;
#9511=ORIENTED_EDGE ( 'NONE', *, *, #3273, .T. ) ;
#9512=CARTESIAN_POINT ( 'NONE',  ( 9.999999999999998224, 1.764426149628241625, -7.186570834724189005 ) ) ;
#9516=AXIS2_PLACEMENT_3D ( 'NONE', #7171, #8962, #2216 ) ;
#9520=VERTEX_POINT ( 'NONE', #6177 ) ;
#9521=DIRECTION ( 'NONE',  ( -1.000000000000000000, 1.010728034814421376E-30, 1.090846720500930387E-30 ) ) ;
#9522=DIRECTION ( 'NONE',  ( 1.140150527077241873E-30, 0.000000000000000000, -1.000000000000000000 ) ) ;
#9523=CIRCLE ( 'NONE', #11194, 2.800000000000002931 ) ;
#9525=CARTESIAN_POINT ( 'NONE',  ( 19.99999999999997868, -0.4733669331951446679, -6.481737787550303942 ) ) ;
#9527=DIRECTION ( 'NONE',  ( 0.000000000000000000, 0.000000000000000000, 1.000000000000000000 ) ) ;
#9529=ADVANCED_FACE ( 'NONE', ( #1276 ), #7220, .T. ) ;
#9531=EDGE_CURVE ( 'NONE', #2884, #2783, #1405, .T. ) ;
#9532=DIRECTION ( 'NONE',  ( 0.000000000000000000, 0.08963930890342669544, 0.9959742939952396235 ) ) ;
#9541=CARTESIAN_POINT ( 'NONE',  ( 19.99999999999999645, -0.1095571986795048497, 6.498076501567022767 ) ) ;
#9542=CYLINDRICAL_SURFACE ( 'NONE', #10662, 2.800000000000003819 ) ;
#9549=ORIENTED_EDGE ( 'NONE', *, *, #8296, .F. ) ;
#9550=VECTOR ( 'NONE', #10587, 1000.000000000000000 ) ;
#9552=FACE_OUTER_BOUND ( 'NONE', #365, .T. ) ;
#9554=ORIENTED_EDGE ( 'NONE', *, *, #2739, .T. ) ;
#9555=CARTESIAN_POINT ( 'NONE',  ( 0.000000000000000000, 0.000000000000000000, 0.000000000000000000 ) ) ;
#9561=ORIENTED_EDGE ( 'NONE', *, *, #8517, .T. ) ;
#9562=LINE ( 'NONE', #7400, #2559 ) ;
#9564=ADVANCED_FACE ( 'NONE', ( #188 ), #8037, .F. ) ;
#9565=EDGE_CURVE ( 'NONE', #12421, #2328, #5961, .T. ) ;
#9566=VERTEX_POINT ( 'NONE', #11139 ) ;
#9567=ORIENTED_EDGE ( 'NONE', *, *, #8352, .T. ) ;
#9570=VECTOR ( 'NONE', #3219, 1000.000000000000000 ) ;
#9572=ORIENTED_EDGE ( 'NONE', *, *, #8248, .F. ) ;
#9573=DIRECTION ( 'NONE',  ( 0.000000000000000000, 0.000000000000000000, 1.000000000000000000 ) ) ;
#9575=CIRCLE ( 'NONE', #1160, 2.800000000000002931 ) ;
#9577=CARTESIAN_POINT ( 'NONE',  ( 19.99999999999999645, -4.621065432155044839, -4.569765340993108715 ) ) ;
#9580=DIRECTION ( 'NONE',  ( -1.140150527077241873E-30, 0.000000000000000000, 1.000000000000000000 ) ) ;
#9581=ORIENTED_EDGE ( 'NONE', *, *, #2028, .T. ) ;
#9583=VERTEX_POINT ( 'NONE', #2772 ) ;
#9585=CIRCLE ( 'NONE', #11258, 7.400000000000011902 ) ;
#9586=AXIS2_PLACEMENT_3D ( 'NONE', #7429, #10506, #3633 ) ;
#9587=DIRECTION ( 'NONE',  ( 1.000000000000000000, -1.010728034814421376E-30, -1.090846720500930387E-30 ) ) ;
#9588=CYLINDRICAL_SURFACE ( 'NONE', #5378, 2.800000000000003819 ) ;
#9589=CARTESIAN_POINT ( 'NONE',  ( 0.000000000000000000, 5.362412286431451847, 3.809543717993933765 ) ) ;
#9591=DIRECTION ( 'NONE',  ( 0.000000000000000000, 0.000000000000000000, 1.000000000000000000 ) ) ;
#9594=CIRCLE ( 'NONE', #4681, 6.499000000000005883 ) ;
#9595=EDGE_CURVE ( 'NONE', #10909, #11856, #249, .T. ) ;
#9596=DIRECTION ( 'NONE',  ( 0.000000000000000000, 0.000000000000000000, 1.000000000000000000 ) ) ;
#9597=ORIENTED_EDGE ( 'NONE', *, *, #5150, .T. ) ;
#9598=EDGE_LOOP ( 'NONE', ( #11798, #12441, #362, #5330 ) ) ;
#9600=LINE ( 'NONE', #858, #4605 ) ;
#9603=DIRECTION ( 'NONE',  ( 1.368180632492690949E-30, -0.8805955318567323387, -0.4738686624730092944 ) ) ;
#9605=DIRECTION ( 'NONE',  ( 0.000000000000000000, 0.000000000000000000, 1.000000000000000000 ) ) ;
#9607=DIRECTION ( 'NONE',  ( 0.000000000000000000, 0.000000000000000000, 1.000000000000000000 ) ) ;
#9608=EDGE_LOOP ( 'NONE', ( #11171, #11949, #8163, #7827 ) ) ;
#9612=VECTOR ( 'NONE', #10551, 1000.000000000000000 ) ;
#9616=CARTESIAN_POINT ( 'NONE',  ( 9.999999999999998224, -5.492355906873347848, -4.959236492872019397 ) ) ;
#9622=DIRECTION ( 'NONE',  ( 0.000000000000000000, 0.9989930665413145894, 0.04486483035051865020 ) ) ;
#9625=ORIENTED_EDGE ( 'NONE', *, *, #9001, .T. ) ;
#9626=VERTEX_POINT ( 'NONE', #11071 ) ;
#9637=CIRCLE ( 'NONE', #2268, 2.800000000000003819 ) ;
#9640=AXIS2_PLACEMENT_3D ( 'NONE', #11055, #8148, #8277 ) ;
#9642=EDGE_CURVE ( 'NONE', #6291, #4508, #6162, .T. ) ;
#9646=CARTESIAN_POINT ( 'NONE',  ( 0.000000000000000000, -6.577476285968329783, -0.06996125000500660884 ) ) ;
#9647=CIRCLE ( 'NONE', #3720, 7.400000000000009237 ) ;
#9652=DIRECTION ( 'NONE',  ( -1.000000000000000000, 1.010728034814421376E-30, 1.090846720500930387E-30 ) ) ;
#9654=CARTESIAN_POINT ( 'NONE',  ( 0.000000000000000000, 0.000000000000000000, 0.000000000000000000 ) ) ;
#9657=CARTESIAN_POINT ( 'NONE',  ( 9.999999999999994671, -6.289597356626455138, -3.898841506334599138 ) ) ;
#9660=FACE_OUTER_BOUND ( 'NONE', #1297, .T. ) ;
#9664=ORIENTED_EDGE ( 'NONE', *, *, #8242, .T. ) ;
#9668=CARTESIAN_POINT ( 'NONE',  ( 0.000000000000000000, -5.610543508060412243, -3.433640984893328252 ) ) ;
#9669=ORIENTED_EDGE ( 'NONE', *, *, #10502, .T. ) ;
#9681=VERTEX_POINT ( 'NONE', #2450 ) ;
#9683=DIRECTION ( 'NONE',  ( 1.000000000000000000, -1.010728034814421376E-30, -1.090846720500930387E-30 ) ) ;
#9685=ORIENTED_EDGE ( 'NONE', *, *, #12400, .F. ) ;
#9688=EDGE_CURVE ( 'NONE', #9180, #4888, #8013, .T. ) ;
#9694=VERTEX_POINT ( 'NONE', #8428 ) ;
#9695=CARTESIAN_POINT ( 'NONE',  ( 0.000000000000000000, 0.000000000000000000, 0.000000000000000000 ) ) ;
#9697=DIRECTION ( 'NONE',  ( -1.000000000000000000, 1.010728034814421376E-30, 1.090846720500930387E-30 ) ) ;
#9698=AXIS2_PLACEMENT_3D ( 'NONE', #11941, #11029, #272 ) ;
#9699=CIRCLE ( 'NONE', #3372, 6.499000000000009436 ) ;
#9702=EDGE_CURVE ( 'NONE', #11575, #5257, #9647, .T. ) ;
#9712=CARTESIAN_POINT ( 'NONE',  ( 19.99999999999999645, -5.682309657208357123, 3.313524683561968942 ) ) ;
#9714=CIRCLE ( 'NONE', #2975, 2.800000000000003819 ) ;
#9715=CARTESIAN_POINT ( 'NONE',  ( 0.000000000000000000, -6.969736844459680114, -2.486517307195217796 ) ) ;
#9717=DIRECTION ( 'NONE',  ( -1.000000000000000000, 1.010728034814421376E-30, 1.090846720500930387E-30 ) ) ;
#9719=CARTESIAN_POINT ( 'NONE',  ( 19.99999999999999645, -6.133480037816503305, 2.376659734729468010 ) ) ;
#9720=EDGE_CURVE ( 'NONE', #10576, #11388, #4534, .T. ) ;
#9721=DIRECTION ( 'NONE',  ( -1.000000000000000000, 1.010728034814421376E-30, 1.090846720500930387E-30 ) ) ;
#9722=EDGE_CURVE ( 'NONE', #2041, #11058, #204, .T. ) ;
#9723=DIRECTION ( 'NONE',  ( -1.000000000000000000, 1.010728034814421376E-30, 1.090846720500930387E-30 ) ) ;
#9724=VECTOR ( 'NONE', #10343, 1000.000000000000000 ) ;
#9725=ADVANCED_FACE ( 'NONE', ( #2580 ), #10416, .T. ) ;
#9727=EDGE_LOOP ( 'NONE', ( #12722, #1694, #6494, #8446 ) ) ;
#9731=DIRECTION ( 'NONE',  ( -1.000000000000000000, 1.010728034814421376E-30, 1.090846720500930387E-30 ) ) ;
#9735=AXIS2_PLACEMENT_3D ( 'NONE', #2840, #6878, #12554 ) ;
#9740=EDGE_LOOP ( 'NONE', ( #8285, #2952, #618, #7201 ) ) ;
#9741=DIRECTION ( 'NONE',  ( 0.000000000000000000, 0.000000000000000000, 1.000000000000000000 ) ) ;
#9751=DIRECTION ( 'NONE',  ( 0.000000000000000000, 0.000000000000000000, 1.000000000000000000 ) ) ;
#9757=ORIENTED_EDGE ( 'NONE', *, *, #8694, .T. ) ;
#9762=EDGE_CURVE ( 'NONE', #10785, #5894, #8838, .T. ) ;
#9763=DIRECTION ( 'NONE',  ( 1.000000000000000000, -1.010728034814421376E-30, -1.090846720500930387E-30 ) ) ;
#9766=DIRECTION ( 'NONE',  ( -1.000000000000000000, 1.010728034814421376E-30, 1.090846720500930387E-30 ) ) ;
#9774=FILL_AREA_STYLE_COLOUR ( '', #12577 ) ;
#9776=CYLINDRICAL_SURFACE ( 'NONE', #1231, 2.800000000000003819 ) ;
#9779=CIRCLE ( 'NONE', #6514, 2.800000000000003819 ) ;
#9782=CARTESIAN_POINT ( 'NONE',  ( 19.99999999999997868, -7.301715115245761112, -1.202063382601588959 ) ) ;
#9785=CARTESIAN_POINT ( 'NONE',  ( 19.99999999999999645, 0.000000000000000000, 0.000000000000000000 ) ) ;
#9789=VERTEX_POINT ( 'NONE', #4555 ) ;
#9798=ADVANCED_FACE ( 'NONE', ( #8346 ), #1389, .T. ) ;
#9799=CYLINDRICAL_SURFACE ( 'NONE', #10073, 7.400000000000010125 ) ;
#9801=VERTEX_POINT ( 'NONE', #8407 ) ;
#9803=ORIENTED_EDGE ( 'NONE', *, *, #3587, .F. ) ;
#9807=DIRECTION ( 'NONE',  ( -1.000000000000000000, 1.010728034814421376E-30, 1.090846720500930387E-30 ) ) ;
#9808=VERTEX_POINT ( 'NONE', #7327 ) ;
#9811=EDGE_CURVE ( 'NONE', #10621, #11575, #11944, .T. ) ;
#9812=CARTESIAN_POINT ( 'NONE',  ( 19.99999999999999645, -5.362766118793823367, -3.671204237728701969 ) ) ;
#9813=ORIENTED_EDGE ( 'NONE', *, *, #5924, .T. ) ;
#9814=CARTESIAN_POINT ( 'NONE',  ( -10.00000000000000178, 0.000000000000000000, 0.000000000000000000 ) ) ;
#9815=CYLINDRICAL_SURFACE ( 'NONE', #4422, 6.499000000000010324 ) ;
#9817=ORIENTED_EDGE ( 'NONE', *, *, #6469, .T. ) ;
#9820=ORIENTED_EDGE ( 'NONE', *, *, #6816, .T. ) ;
#9821=CARTESIAN_POINT ( 'NONE',  ( 0.000000000000000000, -6.182645281642484392, -2.245659411033197550 ) ) ;
#9822=VECTOR ( 'NONE', #10643, 1000.000000000000000 ) ;
#9823=ORIENTED_EDGE ( 'NONE', *, *, #7963, .T. ) ;
#9828=VECTOR ( 'NONE', #9763, 1000.000000000000000 ) ;
#9829=CARTESIAN_POINT ( 'NONE',  ( 9.999999999999998224, 3.975087478966743415, -6.241688836730176604 ) ) ;
#9831=ORIENTED_EDGE ( 'NONE', *, *, #448, .T. ) ;
#9833=DIRECTION ( 'NONE',  ( 0.000000000000000000, 0.000000000000000000, 1.000000000000000000 ) ) ;
#9837=AXIS2_PLACEMENT_3D ( 'NONE', #9719, #4846, #10886 ) ;
#9838=EDGE_CURVE ( 'NONE', #865, #11564, #3114, .T. ) ;
#9839=DIRECTION ( 'NONE',  ( -1.140150527077241873E-30, 0.000000000000000000, 1.000000000000000000 ) ) ;
#9841=CYLINDRICAL_SURFACE ( 'NONE', #968, 7.400000000000010125 ) ;
#9845=DIRECTION ( 'NONE',  ( -1.000000000000000000, 1.010728034814421376E-30, 1.090846720500930387E-30 ) ) ;
#9849=CIRCLE ( 'NONE', #2481, 6.499000000000009436 ) ;
#9850=AXIS2_PLACEMENT_3D ( 'NONE', #6085, #8916, #100 ) ;
#9851=CARTESIAN_POINT ( 'NONE',  ( 9.999999999999994671, 1.528443194675403349, 7.240432404259464327 ) ) ;
#9854=ORIENTED_EDGE ( 'NONE', *, *, #4181, .F. ) ;
#9856=CIRCLE ( 'NONE', #6796, 6.499000000000008548 ) ;
#9866=EDGE_LOOP ( 'NONE', ( #8541, #10957, #4805, #2311 ) ) ;
#9868=DIRECTION ( 'NONE',  ( 0.000000000000000000, 0.000000000000000000, 1.000000000000000000 ) ) ;
#9871=VERTEX_POINT ( 'NONE', #3472 ) ;
#9873=DIRECTION ( 'NONE',  ( 0.000000000000000000, 0.000000000000000000, 1.000000000000000000 ) ) ;
#9874=VERTEX_POINT ( 'NONE', #7386 ) ;
#9875=DIRECTION ( 'NONE',  ( 0.000000000000000000, 0.3513748240813434620, -0.9362348706397368714 ) ) ;
#9876=EDGE_CURVE ( 'NONE', #6211, #11663, #5149, .T. ) ;
#9878=ORIENTED_EDGE ( 'NONE', *, *, #4335, .T. ) ;
#9884=ADVANCED_FACE ( 'NONE', ( #3529 ), #7449, .T. ) ;
#9887=DIRECTION ( 'NONE',  ( -1.000000000000000000, 1.010728034814421376E-30, 1.090846720500930387E-30 ) ) ;
#9893=ORIENTED_EDGE ( 'NONE', *, *, #8630, .T. ) ;
#9894=CARTESIAN_POINT ( 'NONE',  ( 19.99999999999999645, 0.000000000000000000, 0.000000000000000000 ) ) ;
#9896=DIRECTION ( 'NONE',  ( -1.000000000000000000, 1.010728034814421376E-30, 1.090846720500930387E-30 ) ) ;
#9898=FACE_OUTER_BOUND ( 'NONE', #10465, .T. ) ;
#9899=ORIENTED_EDGE ( 'NONE', *, *, #9531, .F. ) ;
#9900=DIRECTION ( 'NONE',  ( -1.000000000000000000, 1.010728034814421376E-30, 1.090846720500930387E-30 ) ) ;
#9902=DIRECTION ( 'NONE',  ( 1.140150527077241873E-30, 0.000000000000000000, -1.000000000000000000 ) ) ;
#9906=CARTESIAN_POINT ( 'NONE',  ( 19.99999999999997868, 1.052479792859146723, -6.413211932068299426 ) ) ;
#9912=CARTESIAN_POINT ( 'NONE',  ( 0.000000000000000000, 4.494880553659092115, -4.802513683199192585 ) ) ;
#9913=EDGE_CURVE ( 'NONE', #9038, #11856, #9856, .T. ) ;
#9917=EDGE_CURVE ( 'NONE', #568, #9126, #7638, .T. ) ;
#9920=CARTESIAN_POINT ( 'NONE',  ( 9.999999999999998224, 7.380072687735817816, 0.5427035320837020338 ) ) ;
#9921=LINE ( 'NONE', #2013, #4289 ) ;
#9923=ORIENTED_EDGE ( 'NONE', *, *, #12486, .T. ) ;
#9924=DIRECTION ( 'NONE',  ( -1.000000000000000000, 1.010728034814421376E-30, 1.090846720500930387E-30 ) ) ;
#9927=ORIENTED_EDGE ( 'NONE', *, *, #9720, .T. ) ;
#9929=VERTEX_POINT ( 'NONE', #2765 ) ;
#9936=CYLINDRICAL_SURFACE ( 'NONE', #8406, 6.499000000000010324 ) ;
#9937=CARTESIAN_POINT ( 'NONE',  ( 19.99999999999999645, 0.000000000000000000, 0.000000000000000000 ) ) ;
#9938=ADVANCED_FACE ( 'NONE', ( #741 ), #1646, .T. ) ;
#9940=CIRCLE ( 'NONE', #2784, 2.800000000000003375 ) ;
#9942=DIRECTION ( 'NONE',  ( -1.000000000000000000, 1.010728034814421376E-30, 1.090846720500930387E-30 ) ) ;
#9943=VERTEX_POINT ( 'NONE', #864 ) ;
#9945=ORIENTED_EDGE ( 'NONE', *, *, #6174, .F. ) ;
#9947=ORIENTED_EDGE ( 'NONE', *, *, #9957, .F. ) ;
#9948=DIRECTION ( 'NONE',  ( 1.000000000000000000, -1.010728034814421376E-30, -1.090846720500930387E-30 ) ) ;
#9950=ADVANCED_FACE ( 'NONE', ( #3775 ), #4802, .T. ) ;
#9951=FACE_OUTER_BOUND ( 'NONE', #9316, .T. ) ;
#9952=ORIENTED_EDGE ( 'NONE', *, *, #1847, .F. ) ;
#9953=AXIS2_PLACEMENT_3D ( 'NONE', #4244, #9000, #9130 ) ;
#9954=EDGE_CURVE ( 'NONE', #12437, #9038, #6805, .T. ) ;
#9955=AXIS2_PLACEMENT_3D ( 'NONE', #8986, #1007, #3855 ) ;
#9956=CARTESIAN_POINT ( 'NONE',  ( 19.99999999999997868, 6.557268578288196537, 0.5199208220222073518 ) ) ;
#9957=EDGE_CURVE ( 'NONE', #12437, #10909, #9252, .T. ) ;
#9958=DIRECTION ( 'NONE',  ( 0.000000000000000000, 0.2660368455666687892, 0.9639628606958550172 ) ) ;
#9959=DIRECTION ( 'NONE',  ( 0.000000000000000000, 0.8345732537212999791, 0.5508969814521064157 ) ) ;
#9960=EDGE_CURVE ( 'NONE', #11636, #11649, #11742, .T. ) ;
#9963=AXIS2_PLACEMENT_3D ( 'NONE', #2645, #4372, #8297 ) ;
#9967=ADVANCED_FACE ( 'NONE', ( #8533 ), #1773, .T. ) ;
#9970=DIRECTION ( 'NONE',  ( -1.000000000000000000, 1.010728034814421376E-30, 1.090846720500930387E-30 ) ) ;
#9972=CARTESIAN_POINT ( 'NONE',  ( 19.99999999999997868, 5.895746314278407674, -2.916892913127022702 ) ) ;
#9981=CARTESIAN_POINT ( 'NONE',  ( 19.99999999999999645, 0.000000000000000000, 0.000000000000000000 ) ) ;
#9982=CARTESIAN_POINT ( 'NONE',  ( 19.99999999999999645, 0.000000000000000000, 0.000000000000000000 ) ) ;
#9986=VECTOR ( 'NONE', #6005, 1000.000000000000000 ) ;
#9987=CARTESIAN_POINT ( 'NONE',  ( 0.000000000000000000, 0.000000000000000000, 0.000000000000000000 ) ) ;
#9991=CARTESIAN_POINT ( 'NONE',  ( 19.99999999999999645, -1.966014849757073968, 6.277170897746257694 ) ) ;
#9996=CARTESIAN_POINT ( 'NONE',  ( 19.99999999999999645, -6.453973581750240385, 0.7636923504068631186 ) ) ;
#9998=AXIS2_PLACEMENT_3D ( 'NONE', #7174, #9092, #11882 ) ;
#9999=DIRECTION ( 'NONE',  ( -1.121661599611125110E-30, 0.9989930665413144784, 0.04486483035051876817 ) ) ;
#10002=EDGE_LOOP ( 'NONE', ( #6034, #4966, #12212, #10764 ) ) ;
#10008=VECTOR ( 'NONE', #11586, 1000.000000000000000 ) ;
#10011=EDGE_CURVE ( 'NONE', #742, #6622, #8848, .T. ) ;
#10017=CYLINDRICAL_SURFACE ( 'NONE', #3690, 7.400000000000010125 ) ;
#10020=LINE ( 'NONE', #8234, #3191 ) ;
#10023=ORIENTED_EDGE ( 'NONE', *, *, #11447, .T. ) ;
#10025=ADVANCED_FACE ( 'NONE', ( #12013 ), #9799, .T. ) ;
#10028=AXIS2_PLACEMENT_3D ( 'NONE', #9353, #2760, #6481 ) ;
#10030=SURFACE_STYLE_USAGE ( .BOTH. , #1931 ) ;
#10032=DIRECTION ( 'NONE',  ( 0.000000000000000000, 0.000000000000000000, 1.000000000000000000 ) ) ;
#10037=DIRECTION ( 'NONE',  ( 0.000000000000000000, 0.000000000000000000, 1.000000000000000000 ) ) ;
#10039=EDGE_CURVE ( 'NONE', #5639, #802, #6183, .T. ) ;
#10042=AXIS2_PLACEMENT_3D ( 'NONE', #849, #137, #6851 ) ;
#10044=CIRCLE ( 'NONE', #3301, 2.500000000000003553 ) ;
#10049=CARTESIAN_POINT ( 'NONE',  ( 19.99999999999999645, 0.000000000000000000, 0.000000000000000000 ) ) ;
#10053=AXIS2_PLACEMENT_3D ( 'NONE', #10557, #2594, #1613 ) ;
#10054=CIRCLE ( 'NONE', #9232, 2.800000000000003375 ) ;
#10055=CARTESIAN_POINT ( 'NONE',  ( 0.000000000000000000, 0.000000000000000000, 0.000000000000000000 ) ) ;
#10058=ORIENTED_EDGE ( 'NONE', *, *, #6247, .F. ) ;
#10059=FACE_OUTER_BOUND ( 'NONE', #5307, .T. ) ;
#10060=ORIENTED_EDGE ( 'NONE', *, *, #11790, .F. ) ;
#10068=ORIENTED_EDGE ( 'NONE', *, *, #10964, .F. ) ;
#10070=DIRECTION ( 'NONE',  ( -1.000000000000000000, 1.010728034814421376E-30, 1.090846720500930387E-30 ) ) ;
#10071=DIRECTION ( 'NONE',  ( 0.000000000000000000, -0.4338837391175658365, 0.9009688679024154823 ) ) ;
#10073=AXIS2_PLACEMENT_3D ( 'NONE', #2091, #6931, #4149 ) ;
#10074=ORIENTED_EDGE ( 'NONE', *, *, #10996, .T. ) ;
#10077=ORIENTED_EDGE ( 'NONE', *, *, #7927, .F. ) ;
#10078=CARTESIAN_POINT ( 'NONE',  ( 19.99999999999999645, -3.730839900301562206, 5.321450426182494198 ) ) ;
#10083=ORIENTED_EDGE ( 'NONE', *, *, #454, .T. ) ;
#10084=DIRECTION ( 'NONE',  ( 0.000000000000000000, 0.000000000000000000, 1.000000000000000000 ) ) ;
#10087=CARTESIAN_POINT ( 'NONE',  ( 0.000000000000000000, 0.000000000000000000, 0.000000000000000000 ) ) ;
#10089=ORIENTED_EDGE ( 'NONE', *, *, #6685, .T. ) ;
#10090=CIRCLE ( 'NONE', #11759, 2.800000000000003375 ) ;
#10092=ORIENTED_EDGE ( 'NONE', *, *, #929, .T. ) ;
#10098=VECTOR ( 'NONE', #9333, 1000.000000000000000 ) ;
#10099=EDGE_CURVE ( 'NONE', #8975, #11564, #10970, .T. ) ;
#10105=LINE ( 'NONE', #3499, #12597 ) ;
#10110=CARTESIAN_POINT ( 'NONE',  ( 19.99999999999999645, -3.730839900301496925, -5.321450426182552818 ) ) ;
#10111=CYLINDRICAL_SURFACE ( 'NONE', #4471, 2.800000000000003819 ) ;
#10114=ORIENTED_EDGE ( 'NONE', *, *, #1422, .T. ) ;
#10115=CIRCLE ( 'NONE', #10951, 2.800000000000004263 ) ;
#10123=ORIENTED_EDGE ( 'NONE', *, *, #1893, .F. ) ;
#10124=CIRCLE ( 'NONE', #2767, 2.800000000000003819 ) ;
#10128=DIRECTION ( 'NONE',  ( 0.000000000000000000, -0.8805955318567323387, -0.4738686624730092944 ) ) ;
#10129=LINE ( 'NONE', #230, #9570 ) ;
#10130=DIRECTION ( 'NONE',  ( 0.000000000000000000, -0.5877852522924801315, 0.8090169943749423442 ) ) ;
#10131=CARTESIAN_POINT ( 'NONE',  ( 19.99999999999999645, -6.884685972239679153, 2.713134545806031195 ) ) ;
#10133=AXIS2_PLACEMENT_3D ( 'NONE', #2756, #5628, #1765 ) ;
#10134=CARTESIAN_POINT ( 'NONE',  ( 0.000000000000000000, -0.8135880386783354012, 6.527339685683402060 ) ) ;
#10135=EDGE_LOOP ( 'NONE', ( #2318, #491, #552, #2502 ) ) ;
#10136=ORIENTED_EDGE ( 'NONE', *, *, #4840, .F. ) ;
#10137=ORIENTED_EDGE ( 'NONE', *, *, #23, .T. ) ;
#10139=CARTESIAN_POINT ( 'NONE',  ( 19.99999999999997868, 6.146182963951668299, 2.112211157443887100 ) ) ;
#10140=CIRCLE ( 'NONE', #1925, 2.800000000000003819 ) ;
#10143=CARTESIAN_POINT ( 'NONE',  ( 0.000000000000000000, -7.399010254356644722, -0.1210258481700102196 ) ) ;
#10149=VERTEX_POINT ( 'NONE', #8391 ) ;
#10151=LINE ( 'NONE', #7409, #6215 ) ;
#10152=MANIFOLD_SOLID_BREP ( 'Bore', #4997 ) ;
#10159=AXIS2_PLACEMENT_3D ( 'NONE', #5448, #6616, #11572 ) ;
#10160=DIRECTION ( 'NONE',  ( -1.000000000000000000, 1.010728034814421376E-30, 1.090846720500930387E-30 ) ) ;
#10163=DIRECTION ( 'NONE',  ( 1.000000000000000000, -1.010728034814421376E-30, -1.090846720500930387E-30 ) ) ;
#10164=DIRECTION ( 'NONE',  ( 0.000000000000000000, 0.4338837391175525693, 0.9009688679024219216 ) ) ;
#10165=EDGE_CURVE ( 'NONE', #955, #8657, #11105, .T. ) ;
#10167=EDGE_CURVE ( 'NONE', #2096, #2020, #10044, .T. ) ;
#10171=FACE_OUTER_BOUND ( 'NONE', #7974, .T. ) ;
#10181=EDGE_LOOP ( 'NONE', ( #12242, #6298, #10348, #5342 ) ) ;
#10188=VECTOR ( 'NONE', #12726, 1000.000000000000000 ) ;
#10192=CIRCLE ( 'NONE', #12490, 2.800000000000002931 ) ;
#10194=DIRECTION ( 'NONE',  ( -1.000000000000000000, 1.010728034814421376E-30, 1.090846720500930387E-30 ) ) ;
#10199=EDGE_LOOP ( 'NONE', ( #9878, #5246, #2978, #1474 ) ) ;
#10204=ADVANCED_FACE ( 'NONE', ( #4539 ), #7556, .T. ) ;
#10205=ORIENTED_EDGE ( 'NONE', *, *, #6320, .F. ) ;
#10207=VERTEX_POINT ( 'NONE', #1627 ) ;
#10210=CIRCLE ( 'NONE', #6093, 6.499000000000008548 ) ;
#10213=ORIENTED_EDGE ( 'NONE', *, *, #9960, .F. ) ;
#10219=EDGE_CURVE ( 'NONE', #1526, #7722, #3701, .T. ) ;
#10220=CARTESIAN_POINT ( 'NONE',  ( 19.99999999999999645, -4.046291478462229030, 5.186098161460289901 ) ) ;
#10221=FACE_OUTER_BOUND ( 'NONE', #12599, .T. ) ;
#10222=DIRECTION ( 'NONE',  ( -1.000000000000000000, 1.010728034814421376E-30, 1.090846720500930387E-30 ) ) ;
#10225=DIRECTION ( 'NONE',  ( 0.000000000000000000, 0.1785568947986370392, -0.9839295885986295565 ) ) ;
#10228=DIRECTION ( 'NONE',  ( 1.140150527077241873E-30, 0.000000000000000000, -1.000000000000000000 ) ) ;
#10229=DIRECTION ( 'NONE',  ( -1.000000000000000000, 1.010728034814421376E-30, 1.090846720500930387E-30 ) ) ;
#10230=AXIS2_PLACEMENT_3D ( 'NONE', #11391, #4565, #8476 ) ;
#10232=DIRECTION ( 'NONE',  ( 0.000000000000000000, -0.3513748240813304724, -0.9362348706397417564 ) ) ;
#10238=CARTESIAN_POINT ( 'NONE',  ( 9.999999999999994671, -7.301715115245778875, 1.202063382601485042 ) ) ;
#10241=CIRCLE ( 'NONE', #10665, 2.800000000000002931 ) ;
#10245=CIRCLE ( 'NONE', #4717, 2.800000000000002487 ) ;
#10257=ORIENTED_EDGE ( 'NONE', *, *, #3994, .F. ) ;
#10258=FACE_OUTER_BOUND ( 'NONE', #12316, .T. ) ;
#10262=ORIENTED_EDGE ( 'NONE', *, *, #2067, .F. ) ;
#10264=ORIENTED_EDGE ( 'NONE', *, *, #4683, .F. ) ;
#10267=CIRCLE ( 'NONE', #3104, 2.800000000000003375 ) ;
#10273=ORIENTED_EDGE ( 'NONE', *, *, #7229, .F. ) ;
#10275=CARTESIAN_POINT ( 'NONE',  ( 19.99999999999999645, 4.494880553659021061, 4.802513683199234329 ) ) ;
#10277=LINE ( 'NONE', #7652, #4479 ) ;
#10280=VECTOR ( 'NONE', #10538, 1000.000000000000000 ) ;
#10282=FACE_OUTER_BOUND ( 'NONE', #6999, .T. ) ;
#10283=ADVANCED_FACE ( 'NONE', ( #9660 ), #10447, .T. ) ;
#10284=CARTESIAN_POINT ( 'NONE',  ( 19.99999999999999645, -4.155687294075622873, 5.098857909653524700 ) ) ;
#10286=ORIENTED_EDGE ( 'NONE', *, *, #5796, .T. ) ;
#10292=CARTESIAN_POINT ( 'NONE',  ( 0.000000000000000000, 7.164568425986757916, 1.851744925564474675 ) ) ;
#10293=CARTESIAN_POINT ( 'NONE',  ( 9.999999999999998224, -1.113123845672307155, -7.315801754025040182 ) ) ;
#10294=AXIS2_PLACEMENT_3D ( 'NONE', #7055, #2159, #3208 ) ;
#10303=CARTESIAN_POINT ( 'NONE',  ( 0.000000000000000000, -3.730839900301574197, 5.321450426182483540 ) ) ;
#10304=DIRECTION ( 'NONE',  ( 0.000000000000000000, -0.5128992774058949156, -0.8584487936018728726 ) ) ;
#10310=DIRECTION ( 'NONE',  ( -1.000000000000000000, 1.010728034814421376E-30, 1.090846720500930387E-30 ) ) ;
#10312=DIRECTION ( 'NONE',  ( -1.000000000000000000, 1.010728034814421376E-30, 1.090846720500930387E-30 ) ) ;
#10313=ORIENTED_EDGE ( 'NONE', *, *, #1226, .F. ) ;
#10318=CIRCLE ( 'NONE', #12207, 6.499000000000008548 ) ;
#10322=CYLINDRICAL_SURFACE ( 'NONE', #5723, 2.800000000000003819 ) ;
#10329=ORIENTED_EDGE ( 'NONE', *, *, #9722, .T. ) ;
#10331=CARTESIAN_POINT ( 'NONE',  ( 19.99999999999999645, 4.596015818000074304, 4.705818469689523553 ) ) ;
#10332=ORIENTED_EDGE ( 'NONE', *, *, #2405, .F. ) ;
#10333=AXIS2_PLACEMENT_3D ( 'NONE', #6293, #12103, #3230 ) ;
#10334=ORIENTED_EDGE ( 'NONE', *, *, #8637, .T. ) ;
#10341=ORIENTED_EDGE ( 'NONE', *, *, #4685, .F. ) ;
#10342=VECTOR ( 'NONE', #7441, 1000.000000000000000 ) ;
#10343=DIRECTION ( 'NONE',  ( -1.000000000000000000, 1.010728034814421376E-30, 1.090846720500930387E-30 ) ) ;
#10348=ORIENTED_EDGE ( 'NONE', *, *, #8917, .F. ) ;
#10349=AXIS2_PLACEMENT_3D ( 'NONE', #9065, #4243, #10084 ) ;
#10361=CARTESIAN_POINT ( 'NONE',  ( 19.99999999999999645, 0.000000000000000000, 0.000000000000000000 ) ) ;
#10362=DIRECTION ( 'NONE',  ( -1.000000000000000000, 1.010728034814421376E-30, 1.090846720500930387E-30 ) ) ;
#10364=CARTESIAN_POINT ( 'NONE',  ( 0.000000000000000000, -3.426907987218851481, 5.522074125465508132 ) ) ;
#10372=AXIS2_PLACEMENT_3D ( 'NONE', #6046, #11913, #7152 ) ;
#10380=VERTEX_POINT ( 'NONE', #4912 ) ;
#10381=EDGE_CURVE ( 'NONE', #291, #7883, #2267, .T. ) ;
#10382=AXIS2_PLACEMENT_3D ( 'NONE', #8906, #7585, #1050 ) ;
#10387=DIRECTION ( 'NONE',  ( -1.000000000000000000, 1.010728034814421376E-30, 1.090846720500930387E-30 ) ) ;
#10390=CARTESIAN_POINT ( 'NONE',  ( 19.99999999999999645, -5.774092856145700559, -2.982759240804946810 ) ) ;
#10392=EDGE_CURVE ( 'NONE', #9681, #11065, #2139, .T. ) ;
#10393=FACE_OUTER_BOUND ( 'NONE', #10649, .T. ) ;
#10394=AXIS2_PLACEMENT_3D ( 'NONE', #1545, #11346, #2658 ) ;
#10396=VERTEX_POINT ( 'NONE', #4976 ) ;
#10399=ORIENTED_EDGE ( 'NONE', *, *, #6391, .T. ) ;
#10409=DIRECTION ( 'NONE',  ( -1.000000000000000000, 1.010728034814421376E-30, 1.090846720500930387E-30 ) ) ;
#10410=EDGE_CURVE ( 'NONE', #10811, #825, #11935, .T. ) ;
#10414=EDGE_CURVE ( 'NONE', #7570, #8231, #9849, .T. ) ;
#10415=AXIS2_PLACEMENT_3D ( 'NONE', #9010, #4256, #8113 ) ;
#10416=CYLINDRICAL_SURFACE ( 'NONE', #831, 2.800000000000003819 ) ;
#10419=ORIENTED_EDGE ( 'NONE', *, *, #1838, .T. ) ;
#10423=EDGE_LOOP ( 'NONE', ( #3347, #6893, #1012, #1504 ) ) ;
#10427=CIRCLE ( 'NONE', #1791, 6.499000000000008548 ) ;
#10431=ORIENTED_EDGE ( 'NONE', *, *, #254, .F. ) ;
#10436=EDGE_CURVE ( 'NONE', #6015, #3764, #405, .T. ) ;
#10437=DIRECTION ( 'NONE',  ( -1.000000000000000000, 1.010728034814421376E-30, 1.090846720500930387E-30 ) ) ;
#10438=ORIENTED_EDGE ( 'NONE', *, *, #11338, .T. ) ;
#10440=DIRECTION ( 'NONE',  ( 4.606824426974262030E-31, 0.5128992774059070170, -0.8584487936018656562 ) ) ;
#10445=CARTESIAN_POINT ( 'NONE',  ( 19.99999999999999645, -5.774092856145738750, 2.982759240804856660 ) ) ;
#10446=EDGE_CURVE ( 'NONE', #4508, #5455, #7413, .T. ) ;
#10447=CYLINDRICAL_SURFACE ( 'NONE', #3095, 2.800000000000003819 ) ;
#10452=EDGE_LOOP ( 'NONE', ( #685, #2400 ) ) ;
#10455=CARTESIAN_POINT ( 'NONE',  ( 19.99999999999999645, -4.999339924971576643, 4.274890546383965706 ) ) ;
#10457=DIRECTION ( 'NONE',  ( -1.000000000000000000, 1.010728034814421376E-30, 1.090846720500930387E-30 ) ) ;
#10458=EDGE_LOOP ( 'NONE', ( #6486, #10974, #11327, #3522 ) ) ;
#10459=CARTESIAN_POINT ( 'NONE',  ( 0.000000000000000000, -0.8732627748487655772, -7.348293143721449816 ) ) ;
#10460=VECTOR ( 'NONE', #12543, 1000.000000000000000 ) ;
#10461=CIRCLE ( 'NONE', #1216, 2.800000000000003375 ) ;
#10464=LINE ( 'NONE', #1649, #11506 ) ;
#10465=EDGE_LOOP ( 'NONE', ( #1669, #10114, #9817, #3459 ) ) ;
#10471=AXIS2_PLACEMENT_3D ( 'NONE', #12427, #2639, #4367 ) ;
#10473=EDGE_LOOP ( 'NONE', ( #410, #4137, #252, #9093 ) ) ;
#10474=DIRECTION ( 'NONE',  ( 0.000000000000000000, 0.000000000000000000, 1.000000000000000000 ) ) ;
#10476=ORIENTED_EDGE ( 'NONE', *, *, #7236, .F. ) ;
#10478=DIRECTION ( 'NONE',  ( 0.000000000000000000, 0.9989930665413144784, 0.04486483035051876817 ) ) ;
#10479=CYLINDRICAL_SURFACE ( 'NONE', #7105, 6.499000000000010324 ) ;
#10480=AXIS2_PLACEMENT_3D ( 'NONE', #1987, #11662, #5858 ) ;
#10482=CIRCLE ( 'NONE', #5151, 7.400000000000009237 ) ;
#10483=CIRCLE ( 'NONE', #7610, 2.800000000000003375 ) ;
#10488=ORIENTED_EDGE ( 'NONE', *, *, #11189, .F. ) ;
#10489=ADVANCED_FACE ( 'NONE', ( #12257 ), #330, .T. ) ;
#10492=EDGE_CURVE ( 'NONE', #7234, #11776, #1020, .T. ) ;
#10493=AXIS2_PLACEMENT_3D ( 'NONE', #5792, #67, #11919 ) ;
#10494=VECTOR ( 'NONE', #10689, 1000.000000000000000 ) ;
#10495=DIRECTION ( 'NONE',  ( -1.000000000000000000, 1.010728034814421376E-30, 1.090846720500930387E-30 ) ) ;
#10497=DIRECTION ( 'NONE',  ( 1.140150527077241873E-30, 0.000000000000000000, -1.000000000000000000 ) ) ;
#10498=VERTEX_POINT ( 'NONE', #1229 ) ;
#10501=DIRECTION ( 'NONE',  ( 0.000000000000000000, 0.000000000000000000, 1.000000000000000000 ) ) ;
#10502=EDGE_CURVE ( 'NONE', #3764, #10396, #9042, .T. ) ;
#10506=DIRECTION ( 'NONE',  ( -1.000000000000000000, 1.010728034814421376E-30, 1.090846720500930387E-30 ) ) ;
#10508=DIRECTION ( 'NONE',  ( -1.000000000000000000, 1.010728034814421376E-30, 1.090846720500930387E-30 ) ) ;
#10510=DIRECTION ( 'NONE',  ( 0.000000000000000000, 0.000000000000000000, 1.000000000000000000 ) ) ;
#10513=AXIS2_PLACEMENT_3D ( 'NONE', #8911, #2293, #9868 ) ;
#10514=EDGE_CURVE ( 'NONE', #8559, #5751, #10267, .T. ) ;
#10519=EDGE_CURVE ( 'NONE', #8354, #9064, #11937, .T. ) ;
#10525=VECTOR ( 'NONE', #2078, 1000.000000000000000 ) ;
#10528=ORIENTED_EDGE ( 'NONE', *, *, #4701, .F. ) ;
#10530=CYLINDRICAL_SURFACE ( 'NONE', #4325, 7.400000000000010125 ) ;
#10531=ORIENTED_EDGE ( 'NONE', *, *, #1305, .T. ) ;
#10534=VECTOR ( 'NONE', #9135, 1000.000000000000000 ) ;
#10538=DIRECTION ( 'NONE',  ( -1.000000000000000000, 1.010728034814421376E-30, 1.090846720500930387E-30 ) ) ;
#10539=ORIENTED_EDGE ( 'NONE', *, *, #1660, .F. ) ;
#10543=AXIS2_PLACEMENT_3D ( 'NONE', #8490, #4764, #5599 ) ;
#10544=ORIENTED_EDGE ( 'NONE', *, *, #8352, .F. ) ;
#10549=EDGE_LOOP ( 'NONE', ( #11369, #8788, #5658, #6426 ) ) ;
#10551=DIRECTION ( 'NONE',  ( -1.000000000000000000, 1.010728034814421376E-30, 1.090846720500930387E-30 ) ) ;
#10554=AXIS2_PLACEMENT_3D ( 'NONE', #337, #2474, #10440 ) ;
#10555=DIRECTION ( 'NONE',  ( -1.000000000000000000, 1.010728034814421376E-30, 1.090846720500930387E-30 ) ) ;
#10556=ORIENTED_EDGE ( 'NONE', *, *, #6206, .T. ) ;
#10557=CARTESIAN_POINT ( 'NONE',  ( 19.99999999999999645, 0.000000000000000000, 0.000000000000000000 ) ) ;
#10558=EDGE_LOOP ( 'NONE', ( #4242, #10763, #6117, #6955 ) ) ;
#10561=DIRECTION ( 'NONE',  ( 1.000000000000000000, -1.010728034814421376E-30, -1.090846720500930387E-30 ) ) ;
#10562=AXIS2_PLACEMENT_3D ( 'NONE', #2742, #8645, #8937 ) ;
#10564=CYLINDRICAL_SURFACE ( 'NONE', #5022, 2.800000000000003819 ) ;
#10565=CARTESIAN_POINT ( 'NONE',  ( 0.000000000000000000, 0.000000000000000000, 0.000000000000000000 ) ) ;
#10568=AXIS2_PLACEMENT_3D ( 'NONE', #723, #1815, #12462 ) ;
#10575=CARTESIAN_POINT ( 'NONE',  ( 19.99999999999999645, 1.834336845376711933, 6.234758161925244124 ) ) ;
#10576=VERTEX_POINT ( 'NONE', #12388 ) ;
#10577=CIRCLE ( 'NONE', #7100, 6.499000000000008548 ) ;
#10578=EDGE_CURVE ( 'NONE', #8686, #2242, #5347, .T. ) ;
#10580=CIRCLE ( 'NONE', #2376, 6.499000000000009436 ) ;
#10581=ORIENTED_EDGE ( 'NONE', *, *, #12698, .T. ) ;
#10583=CARTESIAN_POINT ( 'NONE',  ( 19.99999999999999645, 0.000000000000000000, 0.000000000000000000 ) ) ;
#10587=DIRECTION ( 'NONE',  ( 1.000000000000000000, -1.010728034814421376E-30, -1.090846720500930387E-30 ) ) ;
#10588=CARTESIAN_POINT ( 'NONE',  ( 19.99999999999999645, 0.000000000000000000, 0.000000000000000000 ) ) ;
#10589=ORIENTED_EDGE ( 'NONE', *, *, #3792, .F. ) ;
#10590=CIRCLE ( 'NONE', #9963, 2.800000000000002487 ) ;
#10594=ORIENTED_EDGE ( 'NONE', *, *, #9225, .F. ) ;
#10596=DIRECTION ( 'NONE',  ( 0.000000000000000000, -0.8345732537213080837, 0.5508969814520944253 ) ) ;
#10599=EDGE_CURVE ( 'NONE', #6992, #10576, #8015, .T. ) ;
#10600=DIRECTION ( 'NONE',  ( 0.000000000000000000, 0.6579387259397136978, -0.7530714660036098573 ) ) ;
#10601=VERTEX_POINT ( 'NONE', #1806 ) ;
#10605=ORIENTED_EDGE ( 'NONE', *, *, #3927, .T. ) ;
#10606=ADVANCED_FACE ( 'NONE', ( #4649 ), #5668, .T. ) ;
#10607=EDGE_CURVE ( 'NONE', #11603, #1459, #10482, .T. ) ;
#10620=CARTESIAN_POINT ( 'NONE',  ( 0.000000000000000000, 0.000000000000000000, 0.000000000000000000 ) ) ;
#10621=VERTEX_POINT ( 'NONE', #10364 ) ;
#10623=ORIENTED_EDGE ( 'NONE', *, *, #11189, .T. ) ;
#10624=CARTESIAN_POINT ( 'NONE',  ( 0.000000000000000000, 0.000000000000000000, 0.000000000000000000 ) ) ;
#10628=CARTESIAN_POINT ( 'NONE',  ( 0.000000000000000000, 0.000000000000000000, 0.000000000000000000 ) ) ;
#10629=FACE_OUTER_BOUND ( 'NONE', #7396, .T. ) ;
#10630=DIRECTION ( 'NONE',  ( -1.000000000000000000, 1.010728034814421376E-30, 1.090846720500930387E-30 ) ) ;
#10634=DIRECTION ( 'NONE',  ( 0.000000000000000000, 0.000000000000000000, 1.000000000000000000 ) ) ;
#10638=EDGE_LOOP ( 'NONE', ( #4202, #3613, #3346, #12499 ) ) ;
#10640=EDGE_CURVE ( 'NONE', #12228, #10862, #1230, .T. ) ;
#10643=DIRECTION ( 'NONE',  ( -1.000000000000000000, 1.010728034814421376E-30, 1.090846720500930387E-30 ) ) ;
#10644=EDGE_CURVE ( 'NONE', #6820, #4793, #3560, .T. ) ;
#10649=EDGE_LOOP ( 'NONE', ( #3902, #4678, #675, #12701 ) ) ;
#10650=CARTESIAN_POINT ( 'NONE',  ( 9.999999999999994671, -5.651611091574781476, -4.776954267060657955 ) ) ;
#10653=ORIENTED_EDGE ( 'NONE', *, *, #4771, .T. ) ;
#10655=EDGE_LOOP ( 'NONE', ( #4635, #9240, #178, #6949 ) ) ;
#10657=CARTESIAN_POINT ( 'NONE',  ( 19.99999999999999645, -2.720702104307051172, 5.902099716170436494 ) ) ;
#10659=EDGE_CURVE ( 'NONE', #10716, #479, #1221, .T. ) ;
#10662=AXIS2_PLACEMENT_3D ( 'NONE', #3525, #7758, #26 ) ;
#10663=ORIENTED_EDGE ( 'NONE', *, *, #11790, .T. ) ;
#10665=AXIS2_PLACEMENT_3D ( 'NONE', #9821, #1017, #4110 ) ;
#10672=EDGE_CURVE ( 'NONE', #9285, #6460, #9439, .T. ) ;
#10673=CARTESIAN_POINT ( 'NONE',  ( 0.000000000000000000, -5.682309657208367781, 3.313524683561968942 ) ) ;
#10676=AXIS2_PLACEMENT_3D ( 'NONE', #5949, #988, #11886 ) ;
#10681=ORIENTED_EDGE ( 'NONE', *, *, #978, .F. ) ;
#10682=DIRECTION ( 'NONE',  ( 0.000000000000000000, 0.000000000000000000, 1.000000000000000000 ) ) ;
#10683=ORIENTED_EDGE ( 'NONE', *, *, #6410, .T. ) ;
#10685=AXIS2_PLACEMENT_3D ( 'NONE', #6347, #10194, #3592 ) ;
#10688=AXIS2_PLACEMENT_3D ( 'NONE', #1998, #6844, #10878 ) ;
#10689=DIRECTION ( 'NONE',  ( -1.000000000000000000, 1.010728034814421376E-30, 1.090846720500930387E-30 ) ) ;
#10690=CARTESIAN_POINT ( 'NONE',  ( 0.000000000000000000, -0.8732627748488687169, 7.348293143721422283 ) ) ;
#10691=DIRECTION ( 'NONE',  ( 1.368180632492690774E-30, -0.8805955318567323387, -0.4738686624730094610 ) ) ;
#10692=DIRECTION ( 'NONE',  ( -1.000000000000000000, 1.010728034814421376E-30, 1.090846720500930387E-30 ) ) ;
#10694=DIRECTION ( 'NONE',  ( 1.000000000000000000, -1.010728034814421376E-30, -1.090846720500930387E-30 ) ) ;
#10696=CARTESIAN_POINT ( 'NONE',  ( 19.99999999999997868, -1.623118704078857499, -6.293050665016890477 ) ) ;
#10701=ORIENTED_EDGE ( 'NONE', *, *, #12123, .T. ) ;
#10704=FACE_OUTER_BOUND ( 'NONE', #4166, .T. ) ;
#10707=ORIENTED_EDGE ( 'NONE', *, *, #12598, .F. ) ;
#10710=AXIS2_PLACEMENT_3D ( 'NONE', #8201, #3394, #4540 ) ;
#10713=ORIENTED_EDGE ( 'NONE', *, *, #11802, .F. ) ;
#10715=CARTESIAN_POINT ( 'NONE',  ( 19.99999999999997868, 6.359534927042317598, 1.339147681075194996 ) ) ;
#10716=VERTEX_POINT ( 'NONE', #2733 ) ;
#10717=ORIENTED_EDGE ( 'NONE', *, *, #9401, .T. ) ;
#10720=CIRCLE ( 'NONE', #7647, 2.800000000000003819 ) ;
#10724=ORIENTED_EDGE ( 'NONE', *, *, #5884, .F. ) ;
#10725=DIRECTION ( 'NONE',  ( -1.000000000000000000, 1.010728034814421376E-30, 1.090846720500930387E-30 ) ) ;
#10726=CARTESIAN_POINT ( 'NONE',  ( 19.99999999999999645, -5.610543508060415796, -3.433640984893324699 ) ) ;
#10732=ORIENTED_EDGE ( 'NONE', *, *, #4787, .T. ) ;
#10734=ORIENTED_EDGE ( 'NONE', *, *, #10167, .F. ) ;
#10740=DIRECTION ( 'NONE',  ( -1.000000000000000000, 1.010728034814421376E-30, 1.090846720500930387E-30 ) ) ;
#10741=DIRECTION ( 'NONE',  ( -1.000000000000000000, 1.010728034814421376E-30, 1.090846720500930387E-30 ) ) ;
#10745=ORIENTED_EDGE ( 'NONE', *, *, #9565, .T. ) ;
#10746=CYLINDRICAL_SURFACE ( 'NONE', #8052, 6.499000000000010324 ) ;
#10750=CARTESIAN_POINT ( 'NONE',  ( 19.99999999999999645, -6.413745496774076571, -3.691052519622334938 ) ) ;
#10752=AXIS2_PLACEMENT_3D ( 'NONE', #7815, #12723, #3888 ) ;
#10755=LINE ( 'NONE', #9657, #2578 ) ;
#10756=CARTESIAN_POINT ( 'NONE',  ( 0.000000000000000000, 0.000000000000000000, 0.000000000000000000 ) ) ;
#10761=VECTOR ( 'NONE', #12456, 1000.000000000000000 ) ;
#10763=ORIENTED_EDGE ( 'NONE', *, *, #4895, .T. ) ;
#10764=ORIENTED_EDGE ( 'NONE', *, *, #6176, .T. ) ;
#10765=DIRECTION ( 'NONE',  ( 1.000000000000000000, -1.010728034814421376E-30, -1.090846720500930387E-30 ) ) ;
#10775=ORIENTED_EDGE ( 'NONE', *, *, #9441, .F. ) ;
#10777=CARTESIAN_POINT ( 'NONE',  ( 0.000000000000000000, 6.496448636052932990, -0.1820882179769771347 ) ) ;
#10783=ADVANCED_FACE ( 'NONE', ( #1154 ), #1928, .T. ) ;
#10785=VERTEX_POINT ( 'NONE', #7975 ) ;
#10786=CARTESIAN_POINT ( 'NONE',  ( 19.99999999999999645, 4.494880553659021061, 4.802513683199234329 ) ) ;
#10787=EDGE_CURVE ( 'NONE', #7571, #10785, #6959, .T. ) ;
#10793=EDGE_LOOP ( 'NONE', ( #10531, #1386, #5644, #10842 ) ) ;
#10796=ADVANCED_FACE ( 'NONE', ( #9898 ), #6840, .T. ) ;
#10801=DIRECTION ( 'NONE',  ( -1.000000000000000000, 1.010728034814421376E-30, 1.090846720500930387E-30 ) ) ;
#10804=ADVANCED_FACE ( 'NONE', ( #10940 ), #901, .T. ) ;
#10806=FACE_OUTER_BOUND ( 'NONE', #442, .T. ) ;
#10811=VERTEX_POINT ( 'NONE', #11729 ) ;
#10812=FACE_OUTER_BOUND ( 'NONE', #6683, .T. ) ;
#10813=CYLINDRICAL_SURFACE ( 'NONE', #7414, 2.800000000000003819 ) ;
#10815=CARTESIAN_POINT ( 'NONE',  ( 9.999999999999994671, 3.019282868015081611, 6.756029230465990132 ) ) ;
#10816=AXIS2_PLACEMENT_3D ( 'NONE', #10897, #2083, #12602 ) ;
#10817=CARTESIAN_POINT ( 'NONE',  ( 9.999999999999994671, 0.4528593230174703388, 7.386130139224206026 ) ) ;
#10818=PRODUCT_DEFINITION ( 'UNKNOWN', '', #11667, #4881 ) ;
#10821=LINE ( 'NONE', #12713, #11710 ) ;
#10822=DIRECTION ( 'NONE',  ( -1.000000000000000000, 1.010728034814421376E-30, 1.090846720500930387E-30 ) ) ;
#10824=AXIS2_PLACEMENT_3D ( 'NONE', #6071, #6325, #10232 ) ;
#10826=ADVANCED_FACE ( 'NONE', ( #190 ), #1025, .T. ) ;
#10828=CYLINDRICAL_SURFACE ( 'NONE', #11788, 2.800000000000003819 ) ;
#10833=CIRCLE ( 'NONE', #5498, 2.800000000000003375 ) ;
#10835=LINE ( 'NONE', #11754, #8765 ) ;
#10842=ORIENTED_EDGE ( 'NONE', *, *, #8454, .T. ) ;
#10849=CARTESIAN_POINT ( 'NONE',  ( 20.00000000000000000, 5.510332127717284397E-15, -2.499999999999999556 ) ) ;
#10851=CARTESIAN_POINT ( 'NONE',  ( 19.99999999999997868, -0.8732627748487620245, -7.348293143721449816 ) ) ;
#10854=FACE_OUTER_BOUND ( 'NONE', #2009, .T. ) ;
#10857=ORIENTED_EDGE ( 'NONE', *, *, #10644, .T. ) ;
#10859=ORIENTED_EDGE ( 'NONE', *, *, #6410, .F. ) ;
#10860=CARTESIAN_POINT ( 'NONE',  ( 0.000000000000000000, -1.966014849756989147, -6.277170897746302991 ) ) ;
#10862=VERTEX_POINT ( 'NONE', #5216 ) ;
#10864=AXIS2_PLACEMENT_3D ( 'NONE', #6732, #2945, #3890 ) ;
#10866=DIRECTION ( 'NONE',  ( 0.000000000000000000, 0.000000000000000000, 1.000000000000000000 ) ) ;
#10868=AXIS2_PLACEMENT_3D ( 'NONE', #244, #4175, #8096 ) ;
#10871=AXIS2_PLACEMENT_3D ( 'NONE', #10786, #5770, #9875 ) ;
#10872=DIRECTION ( 'NONE',  ( 1.000000000000000000, -1.010728034814421376E-30, -1.090846720500930387E-30 ) ) ;
#10873=EDGE_LOOP ( 'NONE', ( #10998, #999, #6353, #4022 ) ) ;
#10874=DIRECTION ( 'NONE',  ( -1.000000000000000000, 1.010728034814421376E-30, 1.090846720500930387E-30 ) ) ;
#10878=DIRECTION ( 'NONE',  ( 0.000000000000000000, 0.7818314824680310249, -0.6234898018587319291 ) ) ;
#10879=CIRCLE ( 'NONE', #1628, 2.800000000000003819 ) ;
#10881=CIRCLE ( 'NONE', #7810, 6.499000000000009436 ) ;
#10882=DIRECTION ( 'NONE',  ( -1.000000000000000000, 1.010728034814421376E-30, 1.090846720500930387E-30 ) ) ;
#10883=DIRECTION ( 'NONE',  ( 0.000000000000000000, 0.000000000000000000, 1.000000000000000000 ) ) ;
#10886=DIRECTION ( 'NONE',  ( 0.000000000000000000, -0.08963930890344097568, 0.9959742939952382912 ) ) ;
#10889=AXIS2_PLACEMENT_3D ( 'NONE', #12318, #3378, #7295 ) ;
#10890=AXIS2_PLACEMENT_3D ( 'NONE', #7227, #2331, #2394 ) ;
#10891=CARTESIAN_POINT ( 'NONE',  ( 19.99999999999997868, 0.2252065540230664964, -6.573992004634869879 ) ) ;
#10893=ORIENTED_EDGE ( 'NONE', *, *, #3587, .T. ) ;
#10894=ORIENTED_EDGE ( 'NONE', *, *, #2278, .T. ) ;
#10896=AXIS2_PLACEMENT_3D ( 'NONE', #10588, #677, #4615 ) ;
#10897=CARTESIAN_POINT ( 'NONE',  ( 19.99999999999999645, 0.000000000000000000, 0.000000000000000000 ) ) ;
#10899=VECTOR ( 'NONE', #1399, 1000.000000000000000 ) ;
#10900=DIRECTION ( 'NONE',  ( 0.000000000000000000, 0.000000000000000000, 1.000000000000000000 ) ) ;
#10901=VERTEX_POINT ( 'NONE', #2260 ) ;
#10906=ORIENTED_EDGE ( 'NONE', *, *, #10165, .T. ) ;
#10907=CARTESIAN_POINT ( 'NONE',  ( 0.000000000000000000, -4.999339924971534899, -4.274890546384045642 ) ) ;
#10909=VERTEX_POINT ( 'NONE', #2327 ) ;
#10911=ADVANCED_FACE ( 'NONE', ( #9133 ), #11010, .T. ) ;
#10914=ORIENTED_EDGE ( 'NONE', *, *, #11963, .T. ) ;
#10916=CARTESIAN_POINT ( 'NONE',  ( 19.99999999999999645, 0.000000000000000000, 0.000000000000000000 ) ) ;
#10917=ORIENTED_EDGE ( 'NONE', *, *, #5219, .F. ) ;
#10918=FACE_OUTER_BOUND ( 'NONE', #3474, .T. ) ;
#10923=VERTEX_POINT ( 'NONE', #8176 ) ;
#10926=CARTESIAN_POINT ( 'NONE',  ( 19.99999999999999645, 0.6915992404089836842, 6.462096524400245734 ) ) ;
#10930=ORIENTED_EDGE ( 'NONE', *, *, #12582, .T. ) ;
#10934=DIRECTION ( 'NONE',  ( 0.000000000000000000, -0.5877852522924802425, 0.8090169943749422332 ) ) ;
#10937=DIRECTION ( 'NONE',  ( 0.000000000000000000, 0.000000000000000000, 1.000000000000000000 ) ) ;
#10939=ORIENTED_EDGE ( 'NONE', *, *, #10039, .F. ) ;
#10940=FACE_OUTER_BOUND ( 'NONE', #4111, .T. ) ;
#10951=AXIS2_PLACEMENT_3D ( 'NONE', #8836, #22, #7872 ) ;
#10957=ORIENTED_EDGE ( 'NONE', *, *, #254, .T. ) ;
#10958=DIRECTION ( 'NONE',  ( -1.000000000000000000, 1.010728034814421376E-30, 1.090846720500930387E-30 ) ) ;
#10959=DIRECTION ( 'NONE',  ( -1.000000000000000000, 1.010728034814421376E-30, 1.090846720500930387E-30 ) ) ;
#10962=DIRECTION ( 'NONE',  ( -1.000000000000000000, 1.010728034814421376E-30, 1.090846720500930387E-30 ) ) ;
#10963=ORIENTED_EDGE ( 'NONE', *, *, #10165, .F. ) ;
#10964=EDGE_CURVE ( 'NONE', #2228, #6027, #10464, .T. ) ;
#10968=DIRECTION ( 'NONE',  ( 1.140150527077241873E-30, 0.000000000000000000, -1.000000000000000000 ) ) ;
#10970=LINE ( 'NONE', #6141, #5140 ) ;
#10971=VECTOR ( 'NONE', #6795, 1000.000000000000000 ) ;
#10972=ORIENTED_EDGE ( 'NONE', *, *, #4861, .T. ) ;
#10974=ORIENTED_EDGE ( 'NONE', *, *, #445, .F. ) ;
#10975=ORIENTED_EDGE ( 'NONE', *, *, #12095, .T. ) ;
#10982=DIRECTION ( 'NONE',  ( -1.000000000000000000, 1.010728034814421376E-30, 1.090846720500930387E-30 ) ) ;
#10988=LINE ( 'NONE', #8925, #1948 ) ;
#10989=EDGE_CURVE ( 'NONE', #10862, #9583, #6179, .T. ) ;
#10990=ORIENTED_EDGE ( 'NONE', *, *, #111, .T. ) ;
#10992=ORIENTED_EDGE ( 'NONE', *, *, #8152, .F. ) ;
#10994=VERTEX_POINT ( 'NONE', #1713 ) ;
#10995=CARTESIAN_POINT ( 'NONE',  ( 19.99999999999997868, 2.918117354836732513, -5.807029542149833468 ) ) ;
#10996=EDGE_CURVE ( 'NONE', #11547, #3660, #11512, .T. ) ;
#10998=ORIENTED_EDGE ( 'NONE', *, *, #12288, .T. ) ;
#11001=EDGE_LOOP ( 'NONE', ( #940, #5259, #3596, #7721 ) ) ;
#11002=CIRCLE ( 'NONE', #12655, 7.400000000000009237 ) ;
#11005=ADVANCED_FACE ( 'NONE', ( #2830 ), #867, .T. ) ;
#11006=EDGE_CURVE ( 'NONE', #12032, #6829, #3086, .T. ) ;
#11007=CARTESIAN_POINT ( 'NONE',  ( 19.99999999999999645, -5.932103089875909951, -2.654647609586772816 ) ) ;
#11010=CYLINDRICAL_SURFACE ( 'NONE', #4296, 2.800000000000003819 ) ;
#11011=AXIS2_PLACEMENT_3D ( 'NONE', #9987, #6929, #10968 ) ;
#11012=ORIENTED_EDGE ( 'NONE', *, *, #9960, .T. ) ;
#11015=SURFACE_STYLE_FILL_AREA ( #7094 ) ;
#11022=CARTESIAN_POINT ( 'NONE',  ( 19.99999999999997868, 2.180689217871956131, -6.122221454264557217 ) ) ;
#11027=AXIS2_PLACEMENT_3D ( 'NONE', #242, #11064, #1076 ) ;
#11029=DIRECTION ( 'NONE',  ( -1.000000000000000000, 1.010728034814421376E-30, 1.090846720500930387E-30 ) ) ;
#11032=DIRECTION ( 'NONE',  ( 1.232595164407829369E-30, -0.9510565162951500895, -0.3090169943749582759 ) ) ;
#11033=VERTEX_POINT ( 'NONE', #2955 ) ;
#11034=CARTESIAN_POINT ( 'NONE',  ( 0.000000000000000000, 5.200656487704269360, 5.264330166022977764 ) ) ;
#11040=DIRECTION ( 'NONE',  ( -1.000000000000000000, 1.010728034814421376E-30, 1.090846720500930387E-30 ) ) ;
#11041=ORIENTED_EDGE ( 'NONE', *, *, #11725, .T. ) ;
#11044=ADVANCED_FACE ( 'NONE', ( #9552 ), #7572, .T. ) ;
#11045=ORIENTED_EDGE ( 'NONE', *, *, #7462, .T. ) ;
#11046=DIRECTION ( 'NONE',  ( -1.000000000000000000, 1.010728034814421376E-30, 1.090846720500930387E-30 ) ) ;
#11047=ADVANCED_FACE ( 'NONE', ( #1835 ), #10530, .T. ) ;
#11049=AXIS2_PLACEMENT_3D ( 'NONE', #4657, #3757, #7682 ) ;
#11051=VECTOR ( 'NONE', #12330, 1000.000000000000000 ) ;
#11052=DIRECTION ( 'NONE',  ( 0.000000000000000000, 0.000000000000000000, 1.000000000000000000 ) ) ;
#11053=EDGE_LOOP ( 'NONE', ( #5781, #4866, #4217, #9329 ) ) ;
#11055=CARTESIAN_POINT ( 'NONE',  ( 0.000000000000000000, 0.000000000000000000, 0.000000000000000000 ) ) ;
#11058=VERTEX_POINT ( 'NONE', #10777 ) ;
#11061=EDGE_LOOP ( 'NONE', ( #82, #9823, #3705, #1073 ) ) ;
#11064=DIRECTION ( 'NONE',  ( -1.000000000000000000, 1.010728034814421376E-30, 1.090846720500930387E-30 ) ) ;
#11065=VERTEX_POINT ( 'NONE', #11577 ) ;
#11067=VERTEX_POINT ( 'NONE', #12674 ) ;
#11068=DIRECTION ( 'NONE',  ( 0.000000000000000000, 0.000000000000000000, 1.000000000000000000 ) ) ;
#11071=CARTESIAN_POINT ( 'NONE',  ( 0.000000000000000000, -7.258495115966587363, 1.440225208600799611 ) ) ;
#11074=VERTEX_POINT ( 'NONE', #2702 ) ;
#11075=CARTESIAN_POINT ( 'NONE',  ( 19.99999999999997868, 6.557268578288196537, 3.319920822022206952 ) ) ;
#11076=CIRCLE ( 'NONE', #1196, 2.800000000000003819 ) ;
#11078=CARTESIAN_POINT ( 'NONE',  ( 19.99999999999997868, 3.908107171477257058, -5.192658214849914522 ) ) ;
#11083=EDGE_CURVE ( 'NONE', #3794, #5369, #8537, .T. ) ;
#11085=AXIS2_PLACEMENT_3D ( 'NONE', #8738, #9683, #4028 ) ;
#11087=DIRECTION ( 'NONE',  ( -1.000000000000000000, 1.010728034814421376E-30, 1.090846720500930387E-30 ) ) ;
#11090=CIRCLE ( 'NONE', #8616, 7.400000000000009237 ) ;
#11093=AXIS2_PLACEMENT_3D ( 'NONE', #12548, #3845, #2773 ) ;
#11096=LINE ( 'NONE', #12070, #5827 ) ;
#11098=FACE_OUTER_BOUND ( 'NONE', #3550, .T. ) ;
#11099=ORIENTED_EDGE ( 'NONE', *, *, #3001, .F. ) ;
#11101=AXIS2_PLACEMENT_3D ( 'NONE', #9453, #8438, #7603 ) ;
#11105=LINE ( 'NONE', #4273, #8215 ) ;
#11107=DIRECTION ( 'NONE',  ( -1.000000000000000000, 1.010728034814421376E-30, 1.090846720500930387E-30 ) ) ;
#11108=ORIENTED_EDGE ( 'NONE', *, *, #4840, .T. ) ;
#11109=ORIENTED_EDGE ( 'NONE', *, *, #8325, .T. ) ;
#11116=CARTESIAN_POINT ( 'NONE',  ( 19.99999999999997868, 2.520781513113738548, -6.075668640744172677 ) ) ;
#11117=DIRECTION ( 'NONE',  ( -1.000000000000000000, 1.010728034814421376E-30, 1.090846720500930387E-30 ) ) ;
#11119=DIRECTION ( 'NONE',  ( -1.000000000000000000, 1.010728034814421376E-30, 1.090846720500930387E-30 ) ) ;
#11126=EDGE_LOOP ( 'NONE', ( #6557, #1390, #5045, #2701 ) ) ;
#11127=EDGE_LOOP ( 'NONE', ( #6607, #10313, #10963, #2851 ) ) ;
#11134=DIRECTION ( 'NONE',  ( 1.000000000000000000, -1.010728034814421376E-30, -1.090846720500930387E-30 ) ) ;
#11136=DIRECTION ( 'NONE',  ( 0.000000000000000000, -0.4338837391175658365, 0.9009688679024154823 ) ) ;
#11139=CARTESIAN_POINT ( 'NONE',  ( 3.054370817402604524E-30, 6.544726022087268724, 2.140719964816360399 ) ) ;
#11140=ORIENTED_EDGE ( 'NONE', *, *, #3359, .F. ) ;
#11141=CIRCLE ( 'NONE', #6827, 6.499000000000006771 ) ;
#11143=ORIENTED_EDGE ( 'NONE', *, *, #3531, .F. ) ;
#11154=VERTEX_POINT ( 'NONE', #1121 ) ;
#11155=DIRECTION ( 'NONE',  ( -1.000000000000000000, 1.010728034814421376E-30, 1.090846720500930387E-30 ) ) ;
#11158=ADVANCED_FACE ( 'NONE', ( #4993 ), #9036, .T. ) ;
#11166=AXIS2_PLACEMENT_3D ( 'NONE', #11653, #5475, #9379 ) ;
#11167=ADVANCED_FACE ( 'NONE', ( #10059 ), #3017, .T. ) ;
#11168=CARTESIAN_POINT ( 'NONE',  ( 0.000000000000000000, 2.918117354836734290, -5.807029542149833468 ) ) ;
#11171=ORIENTED_EDGE ( 'NONE', *, *, #9031, .T. ) ;
#11174=AXIS2_PLACEMENT_3D ( 'NONE', #3463, #9476, #547 ) ;
#11177=DIRECTION ( 'NONE',  ( 0.000000000000000000, -0.3513748240813304724, -0.9362348706397417564 ) ) ;
#11178=LINE ( 'NONE', #1382, #1711 ) ;
#11179=CARTESIAN_POINT ( 'NONE',  ( 3.054370817402604524E-30, 6.557268578288196537, 3.319920822022213613 ) ) ;
#11184=EDGE_CURVE ( 'NONE', #5073, #9626, #3343, .T. ) ;
#11188=ORIENTED_EDGE ( 'NONE', *, *, #2925, .T. ) ;
#11189=EDGE_CURVE ( 'NONE', #4626, #5504, #443, .T. ) ;
#11193=EDGE_CURVE ( 'NONE', #10862, #8204, #5991, .T. ) ;
#11194=AXIS2_PLACEMENT_3D ( 'NONE', #3385, #6261, #10304 ) ;
#11196=ORIENTED_EDGE ( 'NONE', *, *, #6225, .F. ) ;
#11197=CARTESIAN_POINT ( 'NONE',  ( 19.99999999999999645, -5.148708580507647348, -3.965829163366334953 ) ) ;
#11198=EDGE_LOOP ( 'NONE', ( #9506, #3458, #8016, #3295 ) ) ;
#11202=DIRECTION ( 'NONE',  ( -1.000000000000000000, 1.010728034814421376E-30, 1.090846720500930387E-30 ) ) ;
#11204=EDGE_CURVE ( 'NONE', #9165, #8354, #9069, .T. ) ;
#11207=ORIENTED_EDGE ( 'NONE', *, *, #3878, .F. ) ;
#11208=DIRECTION ( 'NONE',  ( -1.000000000000000000, 1.010728034814421376E-30, 1.090846720500930387E-30 ) ) ;
#11211=ADVANCED_FACE ( 'NONE', ( #12017 ), #7884, .T. ) ;
#11213=EDGE_CURVE ( 'NONE', #35, #6322, #11347, .T. ) ;
#11214=DIRECTION ( 'NONE',  ( -1.000000000000000000, 1.010728034814421376E-30, 1.090846720500930387E-30 ) ) ;
#11217=CARTESIAN_POINT ( 'NONE',  ( 9.999999999999998224, 5.914787828628609745, -4.446941076999683773 ) ) ;
#11219=AXIS2_PLACEMENT_3D ( 'NONE', #4115, #8238, #1210 ) ;
#11221=CARTESIAN_POINT ( 'NONE',  ( 19.99999999999999645, 5.280167904461726458, 3.922743398397384063 ) ) ;
#11222=ORIENTED_EDGE ( 'NONE', *, *, #978, .T. ) ;
#11223=CARTESIAN_POINT ( 'NONE',  ( 0.000000000000000000, 4.494880553659021061, 4.802513683199234329 ) ) ;
#11224=DIRECTION ( 'NONE',  ( -1.000000000000000000, 1.010728034814421376E-30, 1.090846720500930387E-30 ) ) ;
#11226=ORIENTED_EDGE ( 'NONE', *, *, #6814, .T. ) ;
#11231=CARTESIAN_POINT ( 'NONE',  ( 19.99999999999997868, -2.720702104306968572, -5.902099716170495114 ) ) ;
#11233=DIRECTION ( 'NONE',  ( -1.392832535780847042E-30, 0.8345732537212999791, 0.5508969814521064157 ) ) ;
#11235=FILL_AREA_STYLE_COLOUR ( '', #12133 ) ;
#11236=ORIENTED_EDGE ( 'NONE', *, *, #3565, .F. ) ;
#11238=ORIENTED_EDGE ( 'NONE', *, *, #8206, .F. ) ;
#11241=EDGE_CURVE ( 'NONE', #4279, #7331, #1051, .T. ) ;
#11246=VECTOR ( 'NONE', #6094, 1000.000000000000000 ) ;
#11258=AXIS2_PLACEMENT_3D ( 'NONE', #7745, #1690, #2869 ) ;
#11263=ORIENTED_EDGE ( 'NONE', *, *, #11204, .F. ) ;
#11266=DIRECTION ( 'NONE',  ( 1.140150527077241873E-30, 0.000000000000000000, -1.000000000000000000 ) ) ;
#11268=AXIS2_PLACEMENT_3D ( 'NONE', #4287, #1135, #10071 ) ;
#11269=DIRECTION ( 'NONE',  ( -1.000000000000000000, 1.010728034814421376E-30, 1.090846720500930387E-30 ) ) ;
#11271=ORIENTED_EDGE ( 'NONE', *, *, #7433, .F. ) ;
#11282=DIRECTION ( 'NONE',  ( 4.606824426974262030E-31, 0.5128992774059070170, -0.8584487936018656562 ) ) ;
#11285=ORIENTED_EDGE ( 'NONE', *, *, #7036, .T. ) ;
#11289=CYLINDRICAL_SURFACE ( 'NONE', #11670, 2.800000000000003819 ) ;
#11291=LINE ( 'NONE', #3573, #1547 ) ;
#11292=DIRECTION ( 'NONE',  ( -1.000000000000000000, 1.010728034814421376E-30, 1.090846720500930387E-30 ) ) ;
#11301=EDGE_LOOP ( 'NONE', ( #6953, #9820, #10556, #7522 ) ) ;
#11304=ORIENTED_EDGE ( 'NONE', *, *, #2979, .T. ) ;
#11310=CIRCLE ( 'NONE', #12551, 2.800000000000002931 ) ;
#11311=CARTESIAN_POINT ( 'NONE',  ( 19.99999999999997868, 6.057062246029579100, -4.251117141143414990 ) ) ;
#11313=CARTESIAN_POINT ( 'NONE',  ( 0.000000000000000000, 5.012092988313943565, 4.137139697483554812 ) ) ;
#11314=AXIS2_PLACEMENT_3D ( 'NONE', #6153, #12094, #10130 ) ;
#11315=EDGE_CURVE ( 'NONE', #11905, #9583, #11141, .T. ) ;
#11316=CARTESIAN_POINT ( 'NONE',  ( 19.99999999999999645, 0.000000000000000000, 0.000000000000000000 ) ) ;
#11317=ORIENTED_EDGE ( 'NONE', *, *, #9642, .T. ) ;
#11319=ORIENTED_EDGE ( 'NONE', *, *, #7277, .F. ) ;
#11322=AXIS2_PLACEMENT_3D ( 'NONE', #12416, #4290, #8219 ) ;
#11325=VECTOR ( 'NONE', #1809, 1000.000000000000000 ) ;
#11327=ORIENTED_EDGE ( 'NONE', *, *, #8531, .T. ) ;
#11329=DIRECTION ( 'NONE',  ( 1.000000000000000000, -1.010728034814421376E-30, -1.090846720500930387E-30 ) ) ;
#11334=VECTOR ( 'NONE', #11953, 1000.000000000000000 ) ;
#11335=DIRECTION ( 'NONE',  ( -1.000000000000000000, 1.010728034814421376E-30, 1.090846720500930387E-30 ) ) ;
#11336=ADVANCED_FACE ( 'NONE', ( #543 ), #4342, .T. ) ;
#11338=EDGE_CURVE ( 'NONE', #5523, #7377, #1568, .T. ) ;
#11339=EDGE_LOOP ( 'NONE', ( #1056, #6418, #5704, #885 ) ) ;
#11340=VERTEX_POINT ( 'NONE', #7313 ) ;
#11345=CARTESIAN_POINT ( 'NONE',  ( 0.000000000000000000, -6.577476285968332448, 0.06996125000490599488 ) ) ;
#11346=DIRECTION ( 'NONE',  ( -1.000000000000000000, 1.010728034814421376E-30, 1.090846720500930387E-30 ) ) ;
#11347=CIRCLE ( 'NONE', #2730, 7.400000000000011902 ) ;
#11349=EDGE_LOOP ( 'NONE', ( #12576, #7311, #1375, #5813 ) ) ;
#11351=DIRECTION ( 'NONE',  ( -1.000000000000000000, 1.010728034814421376E-30, 1.090846720500930387E-30 ) ) ;
#11355=DIRECTION ( 'NONE',  ( 1.000000000000000000, -1.010728034814421376E-30, -1.090846720500930387E-30 ) ) ;
#11359=CARTESIAN_POINT ( 'NONE',  ( 0.000000000000000000, 0.000000000000000000, 0.000000000000000000 ) ) ;
#11361=CARTESIAN_POINT ( 'NONE',  ( 0.000000000000000000, -3.055252325922142020, -5.825248672282193674 ) ) ;
#11362=CARTESIAN_POINT ( 'NONE',  ( 0.000000000000000000, -4.155687294075552707, -5.098857909653597531 ) ) ;
#11363=DIRECTION ( 'NONE',  ( 1.140150527077241873E-30, 0.000000000000000000, -1.000000000000000000 ) ) ;
#11369=ORIENTED_EDGE ( 'NONE', *, *, #9913, .F. ) ;
#11371=AXIS2_PLACEMENT_3D ( 'NONE', #6461, #9337, #8385 ) ;
#11373=DIRECTION ( 'NONE',  ( -1.000000000000000000, 1.010728034814421376E-30, 1.090846720500930387E-30 ) ) ;
#11375=DIRECTION ( 'NONE',  ( 0.000000000000000000, 0.000000000000000000, 1.000000000000000000 ) ) ;
#11378=LINE ( 'NONE', #1642, #2191 ) ;
#11379=EDGE_LOOP ( 'NONE', ( #2557, #4744, #9196, #10023 ) ) ;
#11380=CARTESIAN_POINT ( 'NONE',  ( 19.99999999999997868, 6.146182963951697609, -2.112211157443803611 ) ) ;
#11383=AXIS2_PLACEMENT_3D ( 'NONE', #12090, #2031, #4089 ) ;
#11388=VERTEX_POINT ( 'NONE', #7625 ) ;
#11390=ORIENTED_EDGE ( 'NONE', *, *, #10167, .T. ) ;
#11391=CARTESIAN_POINT ( 'NONE',  ( 19.99999999999999645, -6.459281472512932609, -1.243290685169442966 ) ) ;
#11394=AXIS2_PLACEMENT_3D ( 'NONE', #1429, #10229, #7428 ) ;
#11395=EDGE_CURVE ( 'NONE', #12687, #2961, #11561, .T. ) ;
#11400=DIRECTION ( 'NONE',  ( -1.000000000000000000, 1.010728034814421376E-30, 1.090846720500930387E-30 ) ) ;
#11401=EDGE_CURVE ( 'NONE', #7234, #2472, #2090, .T. ) ;
#11402=ORIENTED_EDGE ( 'NONE', *, *, #10219, .T. ) ;
#11404=ORIENTED_EDGE ( 'NONE', *, *, #11963, .F. ) ;
#11408=EDGE_CURVE ( 'NONE', #4169, #87, #1884, .T. ) ;
#11410=CYLINDRICAL_SURFACE ( 'NONE', #7309, 2.800000000000003819 ) ;
#11411=EDGE_CURVE ( 'NONE', #6027, #4169, #10090, .T. ) ;
#11412=VECTOR ( 'NONE', #7836, 1000.000000000000000 ) ;
#11413=DIRECTION ( 'NONE',  ( 1.000000000000000000, -1.010728034814421376E-30, -1.090846720500930387E-30 ) ) ;
#11416=DIRECTION ( 'NONE',  ( -1.000000000000000000, 1.010728034814421376E-30, 1.090846720500930387E-30 ) ) ;
#11417=CIRCLE ( 'NONE', #8135, 2.800000000000003819 ) ;
#11420=DIRECTION ( 'NONE',  ( -1.000000000000000000, 1.010728034814421376E-30, 1.090846720500930387E-30 ) ) ;
#11424=VECTOR ( 'NONE', #9766, 1000.000000000000000 ) ;
#11425=CARTESIAN_POINT ( 'NONE',  ( 0.000000000000000000, 2.649444137877682515, -6.020675595748679498 ) ) ;
#11429=DIRECTION ( 'NONE',  ( 1.503766100577550951E-30, -0.7818314824680222541, -0.6234898018587429203 ) ) ;
#11431=DIRECTION ( 'NONE',  ( 0.000000000000000000, 0.000000000000000000, 1.000000000000000000 ) ) ;
#11440=DIRECTION ( 'NONE',  ( -1.000000000000000000, 1.010728034814421376E-30, 1.090846720500930387E-30 ) ) ;
#11446=EDGE_LOOP ( 'NONE', ( #4819, #11041, #637, #7787 ) ) ;
#11447=EDGE_CURVE ( 'NONE', #8175, #9943, #7846, .T. ) ;
#11449=ORIENTED_EDGE ( 'NONE', *, *, #3742, .T. ) ;
#11451=ORIENTED_EDGE ( 'NONE', *, *, #3043, .F. ) ;
#11455=CIRCLE ( 'NONE', #6725, 7.400000000000011902 ) ;
#11458=FACE_OUTER_BOUND ( 'NONE', #2364, .T. ) ;
#11461=DIRECTION ( 'NONE',  ( -1.000000000000000000, 1.010728034814421376E-30, 1.090846720500930387E-30 ) ) ;
#11465=VECTOR ( 'NONE', #7488, 1000.000000000000000 ) ;
#11467=EDGE_CURVE ( 'NONE', #4885, #156, #664, .T. ) ;
#11469=ORIENTED_EDGE ( 'NONE', *, *, #4914, .F. ) ;
#11470=LINE ( 'NONE', #9444, #12614 ) ;
#11472=ORIENTED_EDGE ( 'NONE', *, *, #2076, .F. ) ;
#11473=CARTESIAN_POINT ( 'NONE',  ( 19.99999999999997868, 6.544726022087268724, 2.140719964816360399 ) ) ;
#11475=CARTESIAN_POINT ( 'NONE',  ( 19.99999999999999645, 0.000000000000000000, 0.000000000000000000 ) ) ;
#11476=FACE_OUTER_BOUND ( 'NONE', #1324, .T. ) ;
#11477=DIRECTION ( 'NONE',  ( -1.140150527077241873E-30, 0.000000000000000000, 1.000000000000000000 ) ) ;
#11478=VERTEX_POINT ( 'NONE', #8654 ) ;
#11482=EDGE_CURVE ( 'NONE', #6132, #12737, #12654, .T. ) ;
#11488=CARTESIAN_POINT ( 'NONE',  ( 19.99999999999999645, 4.596015818000074304, 4.705818469689523553 ) ) ;
#11489=DIRECTION ( 'NONE',  ( -1.000000000000000000, 1.010728034814421376E-30, 1.090846720500930387E-30 ) ) ;
#11491=CARTESIAN_POINT ( 'NONE',  ( 0.000000000000000000, -5.148708580507658006, -3.965829163366345167 ) ) ;
#11496=ORIENTED_EDGE ( 'NONE', *, *, #10989, .T. ) ;
#11499=ORIENTED_EDGE ( 'NONE', *, *, #317, .T. ) ;
#11500=CYLINDRICAL_SURFACE ( 'NONE', #8709, 2.800000000000003819 ) ;
#11501=DIRECTION ( 'NONE',  ( 0.000000000000000000, 0.9195277725514489076, 0.3930250316539277144 ) ) ;
#11503=DIRECTION ( 'NONE',  ( -1.000000000000000000, 1.010728034814421376E-30, 1.090846720500930387E-30 ) ) ;
#11506=VECTOR ( 'NONE', #1278, 1000.000000000000000 ) ;
#11508=AXIS2_PLACEMENT_3D ( 'NONE', #6088, #11964, #9166 ) ;
#11511=ORIENTED_EDGE ( 'NONE', *, *, #11006, .F. ) ;
#11512=LINE ( 'NONE', #10650, #8840 ) ;
#11516=CARTESIAN_POINT ( 'NONE',  ( 0.000000000000000000, -5.651611091574845425, 4.776954267060575354 ) ) ;
#11519=AXIS2_PLACEMENT_3D ( 'NONE', #2812, #8715, #12593 ) ;
#11520=ORIENTED_EDGE ( 'NONE', *, *, #12558, .F. ) ;
#11521=CARTESIAN_POINT ( 'NONE',  ( 19.99999999999999645, 6.718789039999943924, 3.101269713516811688 ) ) ;
#11524=AXIS2_PLACEMENT_3D ( 'NONE', #12160, #6414, #9049 ) ;
#11526=CARTESIAN_POINT ( 'NONE',  ( 19.99999999999997868, 7.100173756228451261, -2.085073771204482007 ) ) ;
#11531=EDGE_LOOP ( 'NONE', ( #10262, #6483, #21, #2892 ) ) ;
#11536=CARTESIAN_POINT ( 'NONE',  ( 19.99999999999999645, 0.000000000000000000, 0.000000000000000000 ) ) ;
#11537=AXIS2_PLACEMENT_3D ( 'NONE', #5700, #11574, #8595 ) ;
#11545=DIRECTION ( 'NONE',  ( -1.000000000000000000, 1.010728034814421376E-30, 1.090846720500930387E-30 ) ) ;
#11546=CARTESIAN_POINT ( 'NONE',  ( 0.000000000000000000, 0.000000000000000000, 0.000000000000000000 ) ) ;
#11547=VERTEX_POINT ( 'NONE', #5042 ) ;
#11548=CARTESIAN_POINT ( 'NONE',  ( 0.000000000000000000, 0.000000000000000000, 0.000000000000000000 ) ) ;
#11549=ORIENTED_EDGE ( 'NONE', *, *, #23, .F. ) ;
#11552=FACE_OUTER_BOUND ( 'NONE', #6434, .T. ) ;
#11557=CARTESIAN_POINT ( 'NONE',  ( 9.999999999999998224, 1.528443194675510153, -7.240432404259457222 ) ) ;
#11561=LINE ( 'NONE', #10575, #7437 ) ;
#11562=EDGE_LOOP ( 'NONE', ( #4818, #5093, #9899, #6689 ) ) ;
#11564=VERTEX_POINT ( 'NONE', #206 ) ;
#11566=DIRECTION ( 'NONE',  ( -1.000000000000000000, 1.010728034814421376E-30, 1.090846720500930387E-30 ) ) ;
#11572=DIRECTION ( 'NONE',  ( 0.000000000000000000, 0.000000000000000000, 1.000000000000000000 ) ) ;
#11574=DIRECTION ( 'NONE',  ( -1.000000000000000000, 1.010728034814421376E-30, 1.090846720500930387E-30 ) ) ;
#11575=VERTEX_POINT ( 'NONE', #8051 ) ;
#11576=VERTEX_POINT ( 'NONE', #3122 ) ;
#11577=CARTESIAN_POINT ( 'NONE',  ( 19.99999999999999645, -4.518585619147920340, 5.860237538055056206 ) ) ;
#11578=ORIENTED_EDGE ( 'NONE', *, *, #6057, .T. ) ;
#11579=ORIENTED_EDGE ( 'NONE', *, *, #2999, .T. ) ;
#11581=CARTESIAN_POINT ( 'NONE',  ( 19.99999999999999645, 2.649444137877595473, 6.020675595748703479 ) ) ;
#11584=FACE_OUTER_BOUND ( 'NONE', #8010, .T. ) ;
#11586=DIRECTION ( 'NONE',  ( 1.000000000000000000, -1.010728034814421376E-30, -1.090846720500930387E-30 ) ) ;
#11589=AXIS2_PLACEMENT_3D ( 'NONE', #8808, #9887, #54 ) ;
#11590=ADVANCED_FACE ( 'NONE', ( #19 ), #11939, .T. ) ;
#11592=ORIENTED_EDGE ( 'NONE', *, *, #2278, .F. ) ;
#11595=ORIENTED_EDGE ( 'NONE', *, *, #10410, .F. ) ;
#11596=DIRECTION ( 'NONE',  ( -1.000000000000000000, 1.010728034814421376E-30, 1.090846720500930387E-30 ) ) ;
#11597=DIRECTION ( 'NONE',  ( 1.000000000000000000, -1.010728034814421376E-30, -1.090846720500930387E-30 ) ) ;
#11598=CARTESIAN_POINT ( 'NONE',  ( 0.000000000000000000, 7.380072687735805381, 0.5427035320837054755 ) ) ;
#11599=VECTOR ( 'NONE', #4462, 1000.000000000000000 ) ;
#11603=VERTEX_POINT ( 'NONE', #2141 ) ;
#11606=EDGE_CURVE ( 'NONE', #5369, #5504, #6637, .T. ) ;
#11607=DIRECTION ( 'NONE',  ( -1.000000000000000000, 1.010728034814421376E-30, 1.090846720500930387E-30 ) ) ;
#11608=CIRCLE ( 'NONE', #3988, 2.800000000000004263 ) ;
#11609=DIRECTION ( 'NONE',  ( 0.000000000000000000, 0.000000000000000000, 1.000000000000000000 ) ) ;
#11610=CARTESIAN_POINT ( 'NONE',  ( 19.99999999999997868, 6.544726022087254513, 0.6592800351837256878 ) ) ;
#11613=CARTESIAN_POINT ( 'NONE',  ( 19.99999999999997868, -1.113123845672304491, -7.315801754025040182 ) ) ;
#11619=EDGE_CURVE ( 'NONE', #12630, #4356, #5933, .T. ) ;
#11620=AXIS2_PLACEMENT_3D ( 'NONE', #1803, #10740, #8755 ) ;
#11624=CARTESIAN_POINT ( 'NONE',  ( 19.99999999999999645, 7.164568425986759692, 1.851744925564481559 ) ) ;
#11628=ORIENTED_EDGE ( 'NONE', *, *, #9441, .T. ) ;
#11631=ORIENTED_EDGE ( 'NONE', *, *, #8723, .T. ) ;
#11633=VECTOR ( 'NONE', #6344, 1000.000000000000000 ) ;
#11636=VERTEX_POINT ( 'NONE', #1102 ) ;
#11637=ORIENTED_EDGE ( 'NONE', *, *, #1159, .T. ) ;
#11638=EDGE_CURVE ( 'NONE', #10601, #7844, #7032, .T. ) ;
#11640=DIRECTION ( 'NONE',  ( -1.000000000000000000, 1.010728034814421376E-30, 1.090846720500930387E-30 ) ) ;
#11643=CARTESIAN_POINT ( 'NONE',  ( 19.99999999999999645, 6.018220532833773007, 2.453165835849278942 ) ) ;
#11644=VERTEX_POINT ( 'NONE', #6064 ) ;
#11645=CIRCLE ( 'NONE', #320, 2.800000000000002931 ) ;
#11648=DIRECTION ( 'NONE',  ( -1.000000000000000000, 1.010728034814421376E-30, 1.090846720500930387E-30 ) ) ;
#11649=VERTEX_POINT ( 'NONE', #9084 ) ;
#11651=ORIENTED_EDGE ( 'NONE', *, *, #3792, .T. ) ;
#11652=AXIS2_PLACEMENT_3D ( 'NONE', #1066, #8083, #11969 ) ;
#11653=CARTESIAN_POINT ( 'NONE',  ( 19.99999999999999645, -4.907279493584704610, -4.380262188593404105 ) ) ;
#11656=VERTEX_POINT ( 'NONE', #3060 ) ;
#11657=DIRECTION ( 'NONE',  ( -1.140150527077241873E-30, 0.000000000000000000, 1.000000000000000000 ) ) ;
#11659=DIRECTION ( 'NONE',  ( 0.000000000000000000, 0.000000000000000000, 1.000000000000000000 ) ) ;
#11662=DIRECTION ( 'NONE',  ( -1.000000000000000000, 1.010728034814421376E-30, 1.090846720500930387E-30 ) ) ;
#11663=VERTEX_POINT ( 'NONE', #8894 ) ;
#11666=DIRECTION ( 'NONE',  ( -1.000000000000000000, 1.010728034814421376E-30, 1.090846720500930387E-30 ) ) ;
#11667=PRODUCT_DEFINITION_FORMATION_WITH_SPECIFIED_SOURCE ( 'ANY', '', #4427, .NOT_KNOWN. ) ;
#11670=AXIS2_PLACEMENT_3D ( 'NONE', #6531, #11489, #1430 ) ;
#11678=CARTESIAN_POINT ( 'NONE',  ( 0.000000000000000000, 0.000000000000000000, 0.000000000000000000 ) ) ;
#11682=ORIENTED_EDGE ( 'NONE', *, *, #929, .F. ) ;
#11683=EDGE_LOOP ( 'NONE', ( #10589, #8718, #10975, #1507 ) ) ;
#11684=LINE ( 'NONE', #2879, #10971 ) ;
#11685=CARTESIAN_POINT ( 'NONE',  ( 0.000000000000000000, -4.907279493584765895, 4.380262188593320616 ) ) ;
#11686=CARTESIAN_POINT ( 'NONE',  ( 0.000000000000000000, -6.486618105788061861, -0.4009819817180140800 ) ) ;
#11691=CARTESIAN_POINT ( 'NONE',  ( 0.000000000000000000, 0.000000000000000000, 0.000000000000000000 ) ) ;
#11693=ORIENTED_EDGE ( 'NONE', *, *, #7517, .T. ) ;
#11697=DIRECTION ( 'NONE',  ( -9.614242282381069117E-31, -0.08963930890344097568, 0.9959742939952382912 ) ) ;
#11698=VERTEX_POINT ( 'NONE', #8381 ) ;
#11710=VECTOR ( 'NONE', #2006, 1000.000000000000000 ) ;
#11714=CARTESIAN_POINT ( 'NONE',  ( 19.99999999999999645, -6.310777386698718239, 1.552768423021305022 ) ) ;
#11715=EDGE_CURVE ( 'NONE', #4507, #7155, #8877, .T. ) ;
#11718=LINE ( 'NONE', #5850, #9828 ) ;
#11719=VERTEX_POINT ( 'NONE', #7360 ) ;
#11720=DIRECTION ( 'NONE',  ( -1.000000000000000000, 1.010728034814421376E-30, 1.090846720500930387E-30 ) ) ;
#11723=AXIS2_PLACEMENT_3D ( 'NONE', #1780, #2834, #8605 ) ;
#11725=EDGE_CURVE ( 'NONE', #3477, #3794, #3351, .T. ) ;
#11727=DIRECTION ( 'NONE',  ( -1.000000000000000000, 1.010728034814421376E-30, 1.090846720500930387E-30 ) ) ;
#11728=ORIENTED_EDGE ( 'NONE', *, *, #12198, .F. ) ;
#11729=CARTESIAN_POINT ( 'NONE',  ( 19.99999999999997868, 4.772487208025196992, -4.411390579991299354 ) ) ;
#11730=VERTEX_POINT ( 'NONE', #3257 ) ;
#11731=DIRECTION ( 'NONE',  ( 0.000000000000000000, 0.000000000000000000, 1.000000000000000000 ) ) ;
#11736=LINE ( 'NONE', #73, #883 ) ;
#11737=EDGE_CURVE ( 'NONE', #1778, #10994, #5486, .T. ) ;
#11742=CIRCLE ( 'NONE', #3520, 7.400000000000009237 ) ;
#11743=CARTESIAN_POINT ( 'NONE',  ( 19.99999999999997868, 4.596015818000145359, -4.705818469689468486 ) ) ;
#11744=ADVANCED_FACE ( 'NONE', ( #6193 ), #525, .T. ) ;
#11747=EDGE_CURVE ( 'NONE', #7883, #5688, #10105, .T. ) ;
#11750=FACE_OUTER_BOUND ( 'NONE', #1983, .T. ) ;
#11752=DIRECTION ( 'NONE',  ( 1.000000000000000000, -1.010728034814421376E-30, -1.090846720500930387E-30 ) ) ;
#11754=CARTESIAN_POINT ( 'NONE',  ( 19.99999999999997868, 6.018220532833812975, -2.453165835849195453 ) ) ;
#11757=EDGE_CURVE ( 'NONE', #3985, #11478, #2314, .T. ) ;
#11759=AXIS2_PLACEMENT_3D ( 'NONE', #6666, #1631, #4789 ) ;
#11763=DIRECTION ( 'NONE',  ( 1.000000000000000000, -1.010728034814421376E-30, -1.090846720500930387E-30 ) ) ;
#11765=VERTEX_POINT ( 'NONE', #585 ) ;
#11769=ADVANCED_FACE ( 'NONE', ( #8186 ), #6388, .T. ) ;
#11772=DIRECTION ( 'NONE',  ( 0.000000000000000000, -0.9195277725514543476, 0.3930250316539148359 ) ) ;
#11775=AXIS2_PLACEMENT_3D ( 'NONE', #7297, #2402, #10164 ) ;
#11776=VERTEX_POINT ( 'NONE', #5292 ) ;
#11778=DIRECTION ( 'NONE',  ( -1.000000000000000000, 1.010728034814421376E-30, 1.090846720500930387E-30 ) ) ;
#11784=EDGE_CURVE ( 'NONE', #11388, #8069, #4327, .T. ) ;
#11785=ORIENTED_EDGE ( 'NONE', *, *, #6490, .T. ) ;
#11787=ORIENTED_EDGE ( 'NONE', *, *, #2814, .F. ) ;
#11788=AXIS2_PLACEMENT_3D ( 'NONE', #2010, #2215, #8259 ) ;
#11790=EDGE_CURVE ( 'NONE', #8854, #8657, #5998, .T. ) ;
#11795=DIRECTION ( 'NONE',  ( 0.000000000000000000, 0.000000000000000000, 1.000000000000000000 ) ) ;
#11798=ORIENTED_EDGE ( 'NONE', *, *, #1757, .F. ) ;
#11799=DIRECTION ( 'NONE',  ( -1.000000000000000000, 1.010728034814421376E-30, 1.090846720500930387E-30 ) ) ;
#11801=CARTESIAN_POINT ( 'NONE',  ( 0.000000000000000000, 3.238809497145205718, 5.634457741540171760 ) ) ;
#11802=EDGE_CURVE ( 'NONE', #10901, #8587, #9284, .T. ) ;
#11814=DIRECTION ( 'NONE',  ( -1.000000000000000000, 1.010728034814421376E-30, 1.090846720500930387E-30 ) ) ;
#11817=DIRECTION ( 'NONE',  ( -1.000000000000000000, 1.010728034814421376E-30, 1.090846720500930387E-30 ) ) ;
#11828=VERTEX_POINT ( 'NONE', #839 ) ;
#11829=AXIS2_PLACEMENT_3D ( 'NONE', #3317, #2398, #6189 ) ;
#11830=ORIENTED_EDGE ( 'NONE', *, *, #11757, .F. ) ;
#11841=VECTOR ( 'NONE', #4613, 1000.000000000000000 ) ;
#11844=ORIENTED_EDGE ( 'NONE', *, *, #5796, .F. ) ;
#11846=EDGE_LOOP ( 'NONE', ( #8632, #6943, #1902, #12291 ) ) ;
#11849=AXIS2_PLACEMENT_3D ( 'NONE', #6008, #1047, #7049 ) ;
#11851=ORIENTED_EDGE ( 'NONE', *, *, #3972, .T. ) ;
#11852=CARTESIAN_POINT ( 'NONE',  ( 19.99999999999999645, -6.213893036447794671, -1.903820982021606989 ) ) ;
#11853=EDGE_CURVE ( 'NONE', #5639, #3589, #1682, .T. ) ;
#11856=VERTEX_POINT ( 'NONE', #7739 ) ;
#11860=( NAMED_UNIT ( * ) PLANE_ANGLE_UNIT ( ) SI_UNIT ( $, .RADIAN. ) );
#11862=CIRCLE ( 'NONE', #5080, 7.400000000000009237 ) ;
#11866=CARTESIAN_POINT ( 'NONE',  ( 19.99999999999999645, 0.000000000000000000, 0.000000000000000000 ) ) ;
#11869=EDGE_CURVE ( 'NONE', #3731, #5073, #8572, .T. ) ;
#11870=DIRECTION ( 'NONE',  ( -1.140150527077241873E-30, 0.000000000000000000, 1.000000000000000000 ) ) ;
#11874=AXIS2_PLACEMENT_3D ( 'NONE', #1365, #9399, #8511 ) ;
#11875=AXIS2_PLACEMENT_3D ( 'NONE', #3130, #7045, #5110 ) ;
#11878=EDGE_LOOP ( 'NONE', ( #8976, #5893, #2817, #4365 ) ) ;
#11879=VERTEX_POINT ( 'NONE', #12451 ) ;
#11881=FACE_OUTER_BOUND ( 'NONE', #2622, .T. ) ;
#11882=DIRECTION ( 'NONE',  ( 0.000000000000000000, -0.3513748240813304724, -0.9362348706397417564 ) ) ;
#11886=DIRECTION ( 'NONE',  ( 0.000000000000000000, 0.6579387259397138088, -0.7530714660036099684 ) ) ;
#11890=DIRECTION ( 'NONE',  ( 0.000000000000000000, 0.7227948638273881121, 0.6910626489868684219 ) ) ;
#11891=ORIENTED_EDGE ( 'NONE', *, *, #11903, .F. ) ;
#11892=ORIENTED_EDGE ( 'NONE', *, *, #11411, .T. ) ;
#11895=ORIENTED_EDGE ( 'NONE', *, *, #2979, .F. ) ;
#11896=FACE_OUTER_BOUND ( 'NONE', #10002, .T. ) ;
#11903=EDGE_CURVE ( 'NONE', #1526, #7064, #2799, .T. ) ;
#11905=VERTEX_POINT ( 'NONE', #3810 ) ;
#11906=DIRECTION ( 'NONE',  ( -2.126226658603505316E-31, 0.7818314824680310249, -0.6234898018587319291 ) ) ;
#11913=DIRECTION ( 'NONE',  ( -1.000000000000000000, 1.010728034814421376E-30, 1.090846720500930387E-30 ) ) ;
#11914=AXIS2_PLACEMENT_3D ( 'NONE', #11678, #4785, #11870 ) ;
#11916=CARTESIAN_POINT ( 'NONE',  ( 0.000000000000000000, 5.280167904461778861, -3.922743398397307679 ) ) ;
#11918=AXIS2_PLACEMENT_3D ( 'NONE', #686, #8675, #9367 ) ;
#11919=DIRECTION ( 'NONE',  ( 0.000000000000000000, 0.000000000000000000, 1.000000000000000000 ) ) ;
#11920=VERTEX_POINT ( 'NONE', #7607 ) ;
#11925=AXIS2_PLACEMENT_3D ( 'NONE', #9972, #9014, #10037 ) ;
#11926=EDGE_CURVE ( 'NONE', #3630, #8559, #6845, .T. ) ;
#11928=AXIS2_PLACEMENT_3D ( 'NONE', #9106, #5962, #8856 ) ;
#11929=DIRECTION ( 'NONE',  ( 0.000000000000000000, 0.000000000000000000, 1.000000000000000000 ) ) ;
#11931=AXIS2_PLACEMENT_3D ( 'NONE', #2857, #11720, #1863 ) ;
#11934=DIRECTION ( 'NONE',  ( -1.000000000000000000, 1.010728034814421376E-30, 1.090846720500930387E-30 ) ) ;
#11935=LINE ( 'NONE', #6916, #12144 ) ;
#11937=CIRCLE ( 'NONE', #8225, 2.800000000000004263 ) ;
#11939=CYLINDRICAL_SURFACE ( 'NONE', #4575, 2.800000000000003819 ) ;
#11941=CARTESIAN_POINT ( 'NONE',  ( 19.99999999999999645, 0.3649881613860001539, 6.567714405409708078 ) ) ;
#11944=CIRCLE ( 'NONE', #8649, 2.800000000000002931 ) ;
#11945=FACE_OUTER_BOUND ( 'NONE', #6669, .T. ) ;
#11947=CIRCLE ( 'NONE', #7589, 6.499000000000008548 ) ;
#11948=CARTESIAN_POINT ( 'NONE',  ( 19.99999999999999645, 0.000000000000000000, 0.000000000000000000 ) ) ;
#11949=ORIENTED_EDGE ( 'NONE', *, *, #5186, .F. ) ;
#11953=DIRECTION ( 'NONE',  ( -1.000000000000000000, 1.010728034814421376E-30, 1.090846720500930387E-30 ) ) ;
#11954=ORIENTED_EDGE ( 'NONE', *, *, #4136, .F. ) ;
#11956=DIRECTION ( 'NONE',  ( -1.140150527077241873E-30, 0.000000000000000000, 1.000000000000000000 ) ) ;
#11957=VERTEX_POINT ( 'NONE', #6521 ) ;
#11960=SHAPE_DEFINITION_REPRESENTATION ( #8112, #891 ) ;
#11961=DIRECTION ( 'NONE',  ( -1.000000000000000000, 1.010728034814421376E-30, 1.090846720500930387E-30 ) ) ;
#11962=ORIENTED_EDGE ( 'NONE', *, *, #1226, .T. ) ;
#11963=EDGE_CURVE ( 'NONE', #568, #4499, #6429, .T. ) ;
#11964=DIRECTION ( 'NONE',  ( -1.000000000000000000, 1.010728034814421376E-30, 1.090846720500930387E-30 ) ) ;
#11966=CARTESIAN_POINT ( 'NONE',  ( 19.99999999999999645, 0.000000000000000000, 0.000000000000000000 ) ) ;
#11967=ORIENTED_EDGE ( 'NONE', *, *, #8367, .T. ) ;
#11969=DIRECTION ( 'NONE',  ( 0.000000000000000000, 0.2660368455666687337, 0.9639628606958550172 ) ) ;
#11972=ORIENTED_EDGE ( 'NONE', *, *, #6391, .F. ) ;
#11976=AXIS2_PLACEMENT_3D ( 'NONE', #3313, #7228, #11929 ) ;
#11982=DIRECTION ( 'NONE',  ( -1.000000000000000000, 1.010728034814421376E-30, 1.090846720500930387E-30 ) ) ;
#11984=DIRECTION ( 'NONE',  ( -1.000000000000000000, 1.010728034814421376E-30, 1.090846720500930387E-30 ) ) ;
#11985=DIRECTION ( 'NONE',  ( -1.000000000000000000, 1.010728034814421376E-30, 1.090846720500930387E-30 ) ) ;
#11988=ORIENTED_EDGE ( 'NONE', *, *, #59, .F. ) ;
#11991=CARTESIAN_POINT ( 'NONE',  ( 0.000000000000000000, 7.164568425986778344, -1.851744925564384525 ) ) ;
#11997=AXIS2_PLACEMENT_3D ( 'NONE', #1748, #5867, #11609 ) ;
#11998=ADVANCED_FACE ( 'NONE', ( #5094 ), #6905, .T. ) ;
#12001=EDGE_CURVE ( 'NONE', #41, #3305, #6961, .T. ) ;
#12006=LINE ( 'NONE', #1041, #74 ) ;
#12007=CARTESIAN_POINT ( 'NONE',  ( 19.99999999999997868, 2.918117354836732513, -5.807029542149833468 ) ) ;
#12008=DIRECTION ( 'NONE',  ( -1.000000000000000000, 1.010728034814421376E-30, 1.090846720500930387E-30 ) ) ;
#12010=DIRECTION ( 'NONE',  ( -1.140150527077241873E-30, 0.000000000000000000, 1.000000000000000000 ) ) ;
#12012=DIRECTION ( 'NONE',  ( 0.000000000000000000, -0.9195277725514543476, 0.3930250316539147248 ) ) ;
#12013=FACE_OUTER_BOUND ( 'NONE', #11126, .T. ) ;
#12015=EDGE_CURVE ( 'NONE', #9489, #7883, #8683, .T. ) ;
#12016=ORIENTED_EDGE ( 'NONE', *, *, #11853, .F. ) ;
#12017=FACE_OUTER_BOUND ( 'NONE', #5516, .T. ) ;
#12018=ORIENTED_EDGE ( 'NONE', *, *, #11193, .T. ) ;
#12019=ORIENTED_EDGE ( 'NONE', *, *, #2441, .T. ) ;
#12021=DIRECTION ( 'NONE',  ( 0.000000000000000000, -0.9989930665413151445, 0.04486483035050449486 ) ) ;
#12023=AXIS2_PLACEMENT_3D ( 'NONE', #657, #4537, #10634 ) ;
#12025=FACE_OUTER_BOUND ( 'NONE', #9370, .T. ) ;
#12026=ORIENTED_EDGE ( 'NONE', *, *, #8298, .T. ) ;
#12032=VERTEX_POINT ( 'NONE', #5864 ) ;
#12034=EDGE_CURVE ( 'NONE', #2488, #12043, #2113, .T. ) ;
#12035=CIRCLE ( 'NONE', #9137, 7.400000000000011902 ) ;
#12036=ORIENTED_EDGE ( 'NONE', *, *, #9108, .F. ) ;
#12037=ORIENTED_EDGE ( 'NONE', *, *, #6007, .T. ) ;
#12043=VERTEX_POINT ( 'NONE', #6052 ) ;
#12048=AXIS2_PLACEMENT_3D ( 'NONE', #1387, #5316, #12224 ) ;
#12049=DIRECTION ( 'NONE',  ( -1.000000000000000000, 1.010728034814421376E-30, 1.090846720500930387E-30 ) ) ;
#12052=ORIENTED_EDGE ( 'NONE', *, *, #10578, .T. ) ;
#12059=CARTESIAN_POINT ( 'NONE',  ( 19.99999999999999645, -4.357840574720558635, -4.821434073522041786 ) ) ;
#12060=DIRECTION ( 'NONE',  ( 0.000000000000000000, -0.9510565162951500895, -0.3090169943749582759 ) ) ;
#12062=CARTESIAN_POINT ( 'NONE',  ( 19.99999999999997868, 5.200656487704349296, -5.264330166022921809 ) ) ;
#12065=CIRCLE ( 'NONE', #7751, 2.800000000000002931 ) ;
#12067=VERTEX_POINT ( 'NONE', #3179 ) ;
#12069=ADVANCED_FACE ( 'NONE', ( #1027 ), #10746, .T. ) ;
#12070=CARTESIAN_POINT ( 'NONE',  ( 9.999999999999998224, -4.707829255731169837, -5.709320773864598131 ) ) ;
#12073=ORIENTED_EDGE ( 'NONE', *, *, #5075, .F. ) ;
#12074=DIRECTION ( 'NONE',  ( -1.000000000000000000, 1.010728034814421376E-30, 1.090846720500930387E-30 ) ) ;
#12077=AXIS2_PLACEMENT_3D ( 'NONE', #10455, #6672, #11501 ) ;
#12078=( NAMED_UNIT ( * ) PLANE_ANGLE_UNIT ( ) SI_UNIT ( $, .RADIAN. ) );
#12084=CARTESIAN_POINT ( 'NONE',  ( 19.99999999999997868, -3.178467454237100309, -5.758943784352606343 ) ) ;
#12085=ORIENTED_EDGE ( 'NONE', *, *, #8845, .T. ) ;
#12086=CIRCLE ( 'NONE', #5290, 2.800000000000003819 ) ;
#12087=DIRECTION ( 'NONE',  ( -1.000000000000000000, 1.010728034814421376E-30, 1.090846720500930387E-30 ) ) ;
#12088=VECTOR ( 'NONE', #3053, 1000.000000000000000 ) ;
#12090=CARTESIAN_POINT ( 'NONE',  ( 19.99999999999997868, 1.395418990828298567, -6.428133065596409068 ) ) ;
#12093=LINE ( 'NONE', #293, #5490 ) ;
#12094=DIRECTION ( 'NONE',  ( -1.000000000000000000, 1.010728034814421376E-30, 1.090846720500930387E-30 ) ) ;
#12095=EDGE_CURVE ( 'NONE', #9218, #2245, #12607, .T. ) ;
#12103=DIRECTION ( 'NONE',  ( -1.000000000000000000, 1.010728034814421376E-30, 1.090846720500930387E-30 ) ) ;
#12107=LINE ( 'NONE', #11197, #10899 ) ;
#12110=CARTESIAN_POINT ( 'NONE',  ( 19.99999999999997868, 0.3649881613860929686, -6.567714405409704526 ) ) ;
#12111=FACE_OUTER_BOUND ( 'NONE', #3663, .T. ) ;
#12113=ADVANCED_FACE ( 'NONE', ( #3111 ), #1219, .T. ) ;
#12116=ORIENTED_EDGE ( 'NONE', *, *, #11213, .T. ) ;
#12118=AXIS2_PLACEMENT_3D ( 'NONE', #11685, #983, #8901 ) ;
#12120=CARTESIAN_POINT ( 'NONE',  ( 19.99999999999997868, 2.180689217871956131, -6.122221454264557217 ) ) ;
#12121=ADVANCED_FACE ( 'NONE', ( #10812 ), #7915, .T. ) ;
#12123=EDGE_CURVE ( 'NONE', #2378, #4490, #5194, .T. ) ;
#12126=CARTESIAN_POINT ( 'NONE',  ( 9.999999999999998224, 5.200656487704351960, -5.264330166022921809 ) ) ;
#12127=DIRECTION ( 'NONE',  ( -1.000000000000000000, 1.010728034814421376E-30, 1.090846720500930387E-30 ) ) ;
#12130=CIRCLE ( 'NONE', #5336, 7.400000000000011902 ) ;
#12131=AXIS2_PLACEMENT_3D ( 'NONE', #9309, #498, #4430 ) ;
#12133=COLOUR_RGB ( '', 0.31764706, 0.68627451, 0.89019608) ;
#12134=EDGE_CURVE ( 'NONE', #8459, #4118, #6181, .T. ) ;
#12138=CARTESIAN_POINT ( 'NONE',  ( 19.99999999999999645, -3.730839900301496925, -5.321450426182552818 ) ) ;
#12144=VECTOR ( 'NONE', #10822, 1000.000000000000000 ) ;
#12147=EDGE_CURVE ( 'NONE', #2245, #2575, #3306, .T. ) ;
#12148=CARTESIAN_POINT ( 'NONE',  ( 20.00000000000000000, 0.000000000000000000, 0.000000000000000000 ) ) ;
#12152=ORIENTED_EDGE ( 'NONE', *, *, #9954, .T. ) ;
#12155=ORIENTED_EDGE ( 'NONE', *, *, #8915, .T. ) ;
#12156=CIRCLE ( 'NONE', #1029, 2.800000000000002931 ) ;
#12157=CARTESIAN_POINT ( 'NONE',  ( 19.99999999999997868, 4.494880553659097444, -4.802513683199186367 ) ) ;
#12158=CARTESIAN_POINT ( 'NONE',  ( 0.000000000000000000, 0.000000000000000000, 0.000000000000000000 ) ) ;
#12159=CARTESIAN_POINT ( 'NONE',  ( 0.000000000000000000, -0.9522442067291368994, 6.508557431545707317 ) ) ;
#12160=CARTESIAN_POINT ( 'NONE',  ( 19.99999999999999645, -5.682309657208315379, -3.313524683562055984 ) ) ;
#12168=EDGE_CURVE ( 'NONE', #701, #3305, #3760, .T. ) ;
#12171=VERTEX_POINT ( 'NONE', #11075 ) ;
#12172=CARTESIAN_POINT ( 'NONE',  ( 19.99999999999999645, 1.834336845376711933, 6.234758161925244124 ) ) ;
#12173=CARTESIAN_POINT ( 'NONE',  ( 19.99999999999997868, -7.301715115245777099, 1.202063382601481489 ) ) ;
#12175=CARTESIAN_POINT ( 'NONE',  ( -10.00000000000000178, 0.000000000000000000, 0.000000000000000000 ) ) ;
#12176=ORIENTED_EDGE ( 'NONE', *, *, #12742, .F. ) ;
#12179=CARTESIAN_POINT ( 'NONE',  ( 19.99999999999999645, -6.577476285968329783, 0.06996125000489905599 ) ) ;
#12184=ORIENTED_EDGE ( 'NONE', *, *, #12486, .F. ) ;
#12187=DIRECTION ( 'NONE',  ( 0.000000000000000000, 0.8805955318567392220, -0.4738686624729964159 ) ) ;
#12190=DIRECTION ( 'NONE',  ( -4.683861624749750588E-31, -0.4338837391175658365, 0.9009688679024154823 ) ) ;
#12192=FACE_OUTER_BOUND ( 'NONE', #11446, .T. ) ;
#12193=EDGE_LOOP ( 'NONE', ( #12073, #7540, #7961, #4826 ) ) ;
#12198=EDGE_CURVE ( 'NONE', #11765, #7155, #10151, .T. ) ;
#12202=LINE ( 'NONE', #1106, #3766 ) ;
#12204=CARTESIAN_POINT ( 'NONE',  ( 19.99999999999999645, -6.310777386698697811, -1.552768423021409161 ) ) ;
#12205=CARTESIAN_POINT ( 'NONE',  ( 19.99999999999997868, 1.531833341630222112, -6.396997380212695816 ) ) ;
#12207=AXIS2_PLACEMENT_3D ( 'NONE', #4138, #8055, #6197 ) ;
#12208=CARTESIAN_POINT ( 'NONE',  ( 19.99999999999997868, 6.359534927042319374, -1.339147681075104845 ) ) ;
#12209=VECTOR ( 'NONE', #9948, 1000.000000000000000 ) ;
#12210=DIRECTION ( 'NONE',  ( 0.000000000000000000, 0.000000000000000000, 1.000000000000000000 ) ) ;
#12212=ORIENTED_EDGE ( 'NONE', *, *, #9176, .T. ) ;
#12224=DIRECTION ( 'NONE',  ( 0.000000000000000000, 0.9749279121818227312, 0.2225209339563182509 ) ) ;
#12228=VERTEX_POINT ( 'NONE', #1408 ) ;
#12229=ORIENTED_EDGE ( 'NONE', *, *, #12561, .F. ) ;
#12231=DIRECTION ( 'NONE',  ( -1.000000000000000000, 1.010728034814421376E-30, 1.090846720500930387E-30 ) ) ;
#12236=ORIENTED_EDGE ( 'NONE', *, *, #8133, .F. ) ;
#12237=LINE ( 'NONE', #3422, #1104 ) ;
#12239=DIRECTION ( 'NONE',  ( 1.000000000000000000, -1.010728034814421376E-30, -1.090846720500930387E-30 ) ) ;
#12242=ORIENTED_EDGE ( 'NONE', *, *, #3740, .F. ) ;
#12244=DIRECTION ( 'NONE',  ( -1.000000000000000000, 1.010728034814421376E-30, 1.090846720500930387E-30 ) ) ;
#12245=VECTOR ( 'NONE', #7789, 1000.000000000000000 ) ;
#12255=CYLINDRICAL_SURFACE ( 'NONE', #11925, 2.800000000000003819 ) ;
#12257=FACE_OUTER_BOUND ( 'NONE', #4743, .T. ) ;
#12258=CARTESIAN_POINT ( 'NONE',  ( 19.99999999999999645, 0.000000000000000000, 0.000000000000000000 ) ) ;
#12260=ORIENTED_EDGE ( 'NONE', *, *, #2838, .F. ) ;
#12262=DIRECTION ( 'NONE',  ( 0.000000000000000000, 0.000000000000000000, 1.000000000000000000 ) ) ;
#12263=CARTESIAN_POINT ( 'NONE',  ( 19.99999999999997868, -3.426907987218776874, -5.522074125465566752 ) ) ;
#12266=CARTESIAN_POINT ( 'NONE',  ( 0.000000000000000000, -0.1095571986795065844, 6.498076501567022767 ) ) ;
#12269=DIRECTION ( 'NONE',  ( -1.000000000000000000, 1.010728034814421376E-30, 1.090846720500930387E-30 ) ) ;
#12273=ADVANCED_FACE ( 'NONE', ( #7529 ), #6700, .T. ) ;
#12279=ORIENTED_EDGE ( 'NONE', *, *, #12598, .T. ) ;
#12280=CARTESIAN_POINT ( 'NONE',  ( 0.000000000000000000, -6.459281472512942379, -1.243290685169453402 ) ) ;
#12281=DIRECTION ( 'NONE',  ( -1.000000000000000000, 1.010728034814421376E-30, 1.090846720500930387E-30 ) ) ;
#12285=CARTESIAN_POINT ( 'NONE',  ( 0.000000000000000000, 5.025702764809159895, -5.431603052487340655 ) ) ;
#12288=EDGE_CURVE ( 'NONE', #9180, #3594, #11470, .T. ) ;
#12291=ORIENTED_EDGE ( 'NONE', *, *, #4561, .T. ) ;
#12295=CIRCLE ( 'NONE', #9998, 2.800000000000003819 ) ;
#12297=CIRCLE ( 'NONE', #6736, 2.800000000000002931 ) ;
#12299=LINE ( 'NONE', #7397, #6578 ) ;
#12302=LINE ( 'NONE', #12371, #3608 ) ;
#12303=EDGE_CURVE ( 'NONE', #2371, #9180, #7050, .T. ) ;
#12304=DIRECTION ( 'NONE',  ( 0.000000000000000000, 0.000000000000000000, 1.000000000000000000 ) ) ;
#12312=FACE_OUTER_BOUND ( 'NONE', #12498, .T. ) ;
#12314=DIRECTION ( 'NONE',  ( -1.000000000000000000, 1.010728034814421376E-30, 1.090846720500930387E-30 ) ) ;
#12316=EDGE_LOOP ( 'NONE', ( #5076, #2422, #226, #3141 ) ) ;
#12317=CIRCLE ( 'NONE', #11524, 2.800000000000003375 ) ;
#12318=CARTESIAN_POINT ( 'NONE',  ( 19.99999999999999645, 0.000000000000000000, 0.000000000000000000 ) ) ;
#12319=CARTESIAN_POINT ( 'NONE',  ( 0.000000000000000000, 6.321830586517956263, -1.817291089601262621 ) ) ;
#12321=EDGE_CURVE ( 'NONE', #6259, #10923, #9505, .T. ) ;
#12325=CARTESIAN_POINT ( 'NONE',  ( 0.000000000000000000, -2.385831757338500836, -6.045230171438896072 ) ) ;
#12327=FACE_OUTER_BOUND ( 'NONE', #10423, .T. ) ;
#12330=DIRECTION ( 'NONE',  ( -1.000000000000000000, 1.010728034814421376E-30, 1.090846720500930387E-30 ) ) ;
#12331=DIRECTION ( 'NONE',  ( 1.000000000000000000, -1.010728034814421376E-30, -1.090846720500930387E-30 ) ) ;
#12333=CARTESIAN_POINT ( 'NONE',  ( 0.000000000000000000, -7.301715115245786869, 1.202063382601481489 ) ) ;
#12337=DIRECTION ( 'NONE',  ( -1.000000000000000000, 1.010728034814421376E-30, 1.090846720500930387E-30 ) ) ;
#12340=ADVANCED_FACE ( 'NONE', ( #3674 ), #1733, .T. ) ;
#12345=AXIS2_PLACEMENT_3D ( 'NONE', #123, #10741, #7790 ) ;
#12346=CARTESIAN_POINT ( 'NONE',  ( 19.99999999999999645, -5.774092856145700559, -2.982759240804946810 ) ) ;
#12349=VECTOR ( 'NONE', #3274, 1000.000000000000000 ) ;
#12355=ORIENTED_EDGE ( 'NONE', *, *, #4147, .T. ) ;
#12356=ORIENTED_EDGE ( 'NONE', *, *, #714, .T. ) ;
#12358=ORIENTED_EDGE ( 'NONE', *, *, #5694, .T. ) ;
#12360=ORIENTED_EDGE ( 'NONE', *, *, #414, .T. ) ;
#12361=AXIS2_PLACEMENT_3D ( 'NONE', #1681, #7541, #7670 ) ;
#12362=AXIS2_PLACEMENT_3D ( 'NONE', #6447, #1605, #5476 ) ;
#12366=ORIENTED_EDGE ( 'NONE', *, *, #2864, .T. ) ;
#12368=CARTESIAN_POINT ( 'NONE',  ( 0.000000000000000000, 0.3649881613859949914, 6.567714405409693867 ) ) ;
#12371=CARTESIAN_POINT ( 'NONE',  ( 19.99999999999999645, -6.310777386698718239, 1.552768423021305022 ) ) ;
#12375=DIRECTION ( 'NONE',  ( -1.140150527077241873E-30, 0.000000000000000000, 1.000000000000000000 ) ) ;
#12377=ORIENTED_EDGE ( 'NONE', *, *, #2569, .T. ) ;
#12382=DIRECTION ( 'NONE',  ( -1.000000000000000000, 1.010728034814421376E-30, 1.090846720500930387E-30 ) ) ;
#12383=ADVANCED_FACE ( 'NONE', ( #4695 ), #8619, .T. ) ;
#12384=DIRECTION ( 'NONE',  ( -1.140150527077241873E-30, 0.000000000000000000, 1.000000000000000000 ) ) ;
#12385=VECTOR ( 'NONE', #2749, 1000.000000000000000 ) ;
#12388=CARTESIAN_POINT ( 'NONE',  ( 0.000000000000000000, 5.914787828628547572, 4.446941076999753051 ) ) ;
#12391=CARTESIAN_POINT ( 'NONE',  ( 19.99999999999999645, -6.459281472512932609, -1.243290685169442966 ) ) ;
#12394=CARTESIAN_POINT ( 'NONE',  ( 0.000000000000000000, 0.000000000000000000, 0.000000000000000000 ) ) ;
#12400=EDGE_CURVE ( 'NONE', #6000, #6900, #6440, .T. ) ;
#12402=VECTOR ( 'NONE', #5670, 1000.000000000000000 ) ;
#12405=ORIENTED_EDGE ( 'NONE', *, *, #12095, .F. ) ;
#12406=EDGE_LOOP ( 'NONE', ( #6699, #2288, #7671, #1988 ) ) ;
#12408=DIRECTION ( 'NONE',  ( -1.000000000000000000, 1.010728034814421376E-30, 1.090846720500930387E-30 ) ) ;
#12410=CARTESIAN_POINT ( 'NONE',  ( 19.99999999999999645, 0.2252065540229667429, 6.573992004634855668 ) ) ;
#12416=CARTESIAN_POINT ( 'NONE',  ( 0.000000000000000000, 0.000000000000000000, 0.000000000000000000 ) ) ;
#12419=ORIENTED_EDGE ( 'NONE', *, *, #10514, .F. ) ;
#12421=VERTEX_POINT ( 'NONE', #7014 ) ;
#12422=AXIS2_PLACEMENT_3D ( 'NONE', #5707, #7392, #6428 ) ;
#12423=EDGE_LOOP ( 'NONE', ( #1965, #9163, #2281, #7590 ) ) ;
#12425=EDGE_LOOP ( 'NONE', ( #11728, #2627, #892, #5570 ) ) ;
#12427=CARTESIAN_POINT ( 'NONE',  ( 19.99999999999999645, 0.000000000000000000, 0.000000000000000000 ) ) ;
#12429=DIRECTION ( 'NONE',  ( -1.000000000000000000, 1.010728034814421376E-30, 1.090846720500930387E-30 ) ) ;
#12431=EDGE_CURVE ( 'NONE', #6622, #6552, #6654, .T. ) ;
#12436=AXIS2_PLACEMENT_3D ( 'NONE', #3755, #3102, #3632 ) ;
#12437=VERTEX_POINT ( 'NONE', #10926 ) ;
#12438=DIRECTION ( 'NONE',  ( -1.000000000000000000, 1.010728034814421376E-30, 1.090846720500930387E-30 ) ) ;
#12441=ORIENTED_EDGE ( 'NONE', *, *, #5960, .T. ) ;
#12442=CARTESIAN_POINT ( 'NONE',  ( -10.00000000000000178, 0.000000000000000000, 0.000000000000000000 ) ) ;
#12444=CARTESIAN_POINT ( 'NONE',  ( 19.99999999999999645, 3.908107171477180675, 5.192658214849959819 ) ) ;
#12447=ORIENTED_EDGE ( 'NONE', *, *, #2169, .F. ) ;
#12451=CARTESIAN_POINT ( 'NONE',  ( 19.99999999999999645, -6.486618105788068966, 0.4009819817179238743 ) ) ;
#12452=( LENGTH_UNIT ( ) NAMED_UNIT ( * ) SI_UNIT ( .MILLI., .METRE. ) );
#12453=DIRECTION ( 'NONE',  ( -1.000000000000000000, 1.010728034814421376E-30, 1.090846720500930387E-30 ) ) ;
#12454=ORIENTED_EDGE ( 'NONE', *, *, #5398, .F. ) ;
#12456=DIRECTION ( 'NONE',  ( -1.000000000000000000, 1.010728034814421376E-30, 1.090846720500930387E-30 ) ) ;
#12460=AXIS2_PLACEMENT_3D ( 'NONE', #5577, #2625, #7447 ) ;
#12462=DIRECTION ( 'NONE',  ( 7.272311470006191196E-31, 0.3513748240813434620, -0.9362348706397368714 ) ) ;
#12464=CARTESIAN_POINT ( 'NONE',  ( 0.000000000000000000, 0.000000000000000000, 0.000000000000000000 ) ) ;
#12465=ORIENTED_EDGE ( 'NONE', *, *, #5652, .T. ) ;
#12467=EDGE_LOOP ( 'NONE', ( #10734, #493 ) ) ;
#12471=CARTESIAN_POINT ( 'NONE',  ( 19.99999999999999645, 2.520781513113643513, 6.075668640744193105 ) ) ;
#12473=ORIENTED_EDGE ( 'NONE', *, *, #1159, .F. ) ;
#12479=DIRECTION ( 'NONE',  ( -1.000000000000000000, 1.010728034814421376E-30, 1.090846720500930387E-30 ) ) ;
#12483=EDGE_CURVE ( 'NONE', #825, #276, #6853, .T. ) ;
#12486=EDGE_CURVE ( 'NONE', #6460, #8908, #5848, .T. ) ;
#12488=CIRCLE ( 'NONE', #4245, 6.499000000000009436 ) ;
#12489=DIRECTION ( 'NONE',  ( -1.000000000000000000, 1.010728034814421376E-30, 1.090846720500930387E-30 ) ) ;
#12490=AXIS2_PLACEMENT_3D ( 'NONE', #12410, #7442, #6480 ) ;
#12493=CARTESIAN_POINT ( 'NONE',  ( 0.000000000000000000, -6.453973581750236832, -0.7636923504069602631 ) ) ;
#12494=CARTESIAN_POINT ( 'NONE',  ( 0.000000000000000000, -3.730839900301502254, -5.321450426182545712 ) ) ;
#12495=DIRECTION ( 'NONE',  ( -1.000000000000000000, 1.010728034814421376E-30, 1.090846720500930387E-30 ) ) ;
#12497=AXIS2_PLACEMENT_3D ( 'NONE', #4399, #8321, #9527 ) ;
#12498=EDGE_LOOP ( 'NONE', ( #8816, #1328, #668, #12676 ) ) ;
#12499=ORIENTED_EDGE ( 'NONE', *, *, #2055, .T. ) ;
#12502=ORIENTED_EDGE ( 'NONE', *, *, #9496, .F. ) ;
#12503=DIRECTION ( 'NONE',  ( -1.000000000000000000, 1.010728034814421376E-30, 1.090846720500930387E-30 ) ) ;
#12507=EDGE_CURVE ( 'NONE', #2472, #9566, #7868, .T. ) ;
#12511=DIRECTION ( 'NONE',  ( -1.000000000000000000, 1.010728034814421376E-30, 1.090846720500930387E-30 ) ) ;
#12513=CARTESIAN_POINT ( 'NONE',  ( 19.99999999999999645, -6.459281472512932609, 1.556709314830560853 ) ) ;
#12515=EDGE_CURVE ( 'NONE', #11656, #4011, #470, .T. ) ;
#12516=CARTESIAN_POINT ( 'NONE',  ( 20.00000000000000000, 0.000000000000000000, 2.500000000000003553 ) ) ;
#12521=FACE_OUTER_BOUND ( 'NONE', #11339, .T. ) ;
#12527=VERTEX_POINT ( 'NONE', #11714 ) ;
#12529=CIRCLE ( 'NONE', #12118, 2.800000000000003819 ) ;
#12531=ORIENTED_EDGE ( 'NONE', *, *, #3163, .F. ) ;
#12533=CARTESIAN_POINT ( 'NONE',  ( 19.99999999999999645, -5.362766118793823367, -3.671204237728701969 ) ) ;
#12543=DIRECTION ( 'NONE',  ( -1.000000000000000000, 1.010728034814421376E-30, 1.090846720500930387E-30 ) ) ;
#12547=CIRCLE ( 'NONE', #186, 2.800000000000002931 ) ;
#12548=CARTESIAN_POINT ( 'NONE',  ( 19.99999999999999645, 5.956456411769392112, 2.790827096699012522 ) ) ;
#12551=AXIS2_PLACEMENT_3D ( 'NONE', #12391, #11607, #8505 ) ;
#12554=DIRECTION ( 'NONE',  ( 0.000000000000000000, 0.000000000000000000, 1.000000000000000000 ) ) ;
#12557=CARTESIAN_POINT ( 'NONE',  ( 19.99999999999997868, 6.557268578288196537, 0.5199208220222073518 ) ) ;
#12558=EDGE_CURVE ( 'NONE', #11033, #10811, #9699, .T. ) ;
#12559=CIRCLE ( 'NONE', #10480, 7.400000000000009237 ) ;
#12561=EDGE_CURVE ( 'NONE', #8658, #2488, #8994, .T. ) ;
#12562=AXIS2_PLACEMENT_3D ( 'NONE', #11223, #10163, #7357 ) ;
#12564=ORIENTED_EDGE ( 'NONE', *, *, #9642, .F. ) ;
#12566=CARTESIAN_POINT ( 'NONE',  ( 19.99999999999999645, -6.459281472512945932, 1.243290685169349485 ) ) ;
#12572=DIRECTION ( 'NONE',  ( 1.140150527077241873E-30, 0.000000000000000000, -1.000000000000000000 ) ) ;
#12574=EDGE_CURVE ( 'NONE', #9626, #229, #4039, .T. ) ;
#12576=ORIENTED_EDGE ( 'NONE', *, *, #4151, .T. ) ;
#12577=COLOUR_RGB ( '', 0.31764706, 0.68627451, 0.89019608) ;
#12579=ORIENTED_EDGE ( 'NONE', *, *, #8949, .F. ) ;
#12580=DIRECTION ( 'NONE',  ( 1.140150527077241873E-30, 0.000000000000000000, -1.000000000000000000 ) ) ;
#12582=EDGE_CURVE ( 'NONE', #8069, #5127, #1489, .T. ) ;
#12583=DIRECTION ( 'NONE',  ( -1.140150527077241873E-30, 0.000000000000000000, 1.000000000000000000 ) ) ;
#12587=CARTESIAN_POINT ( 'NONE',  ( 9.999999999999994671, -6.884685972239686258, 2.713134545806031195 ) ) ;
#12592=ADVANCED_FACE ( 'NONE', ( #6354 ), #8092, .T. ) ;
#12593=DIRECTION ( 'NONE',  ( 0.000000000000000000, 0.000000000000000000, 1.000000000000000000 ) ) ;
#12596=ORIENTED_EDGE ( 'NONE', *, *, #12123, .F. ) ;
#12597=VECTOR ( 'NONE', #2536, 1000.000000000000000 ) ;
#12598=EDGE_CURVE ( 'NONE', #1263, #1849, #8691, .T. ) ;
#12599=EDGE_LOOP ( 'NONE', ( #6223, #7701, #4823, #4345 ) ) ;
#12602=DIRECTION ( 'NONE',  ( 0.000000000000000000, 0.000000000000000000, 1.000000000000000000 ) ) ;
#12603=DIRECTION ( 'NONE',  ( -1.000000000000000000, 1.010728034814421376E-30, 1.090846720500930387E-30 ) ) ;
#12607=CIRCLE ( 'NONE', #8275, 6.499000000000006771 ) ;
#12610=EDGE_LOOP ( 'NONE', ( #10438, #4704, #10136, #8870 ) ) ;
#12613=ORIENTED_EDGE ( 'NONE', *, *, #8383, .F. ) ;
#12614=VECTOR ( 'NONE', #2653, 1000.000000000000000 ) ;
#12622=AXIS2_PLACEMENT_3D ( 'NONE', #1572, #9351, #670 ) ;
#12627=CARTESIAN_POINT ( 'NONE',  ( -10.00000000000000178, 0.000000000000000000, 0.000000000000000000 ) ) ;
#12630=VERTEX_POINT ( 'NONE', #7076 ) ;
#12633=CYLINDRICAL_SURFACE ( 'NONE', #3503, 7.400000000000010125 ) ;
#12636=ORIENTED_EDGE ( 'NONE', *, *, #6883, .F. ) ;
#12638=ORIENTED_EDGE ( 'NONE', *, *, #2404, .T. ) ;
#12641=AXIS2_PLACEMENT_3D ( 'NONE', #10055, #4402, #8326 ) ;
#12643=EDGE_CURVE ( 'NONE', #9694, #2472, #495, .T. ) ;
#12644=AXIS2_PLACEMENT_3D ( 'NONE', #5086, #3236, #7214 ) ;
#12647=CARTESIAN_POINT ( 'NONE',  ( 19.99999999999997868, -2.720702104306968572, -5.902099716170495114 ) ) ;
#12649=LINE ( 'NONE', #6850, #944 ) ;
#12651=AXIS2_PLACEMENT_3D ( 'NONE', #49, #12686, #8023 ) ;
#12652=DIRECTION ( 'NONE',  ( 1.000000000000000000, -1.010728034814421376E-30, -1.090846720500930387E-30 ) ) ;
#12653=CARTESIAN_POINT ( 'NONE',  ( 19.99999999999997868, 6.359055127044386246, 1.682410996215993881 ) ) ;
#12654=LINE ( 'NONE', #7686, #5589 ) ;
#12655=AXIS2_PLACEMENT_3D ( 'NONE', #248, #4182, #3360 ) ;
#12656=VERTEX_POINT ( 'NONE', #10995 ) ;
#12658=AXIS2_PLACEMENT_3D ( 'NONE', #5198, #9235, #4165 ) ;
#12664=DIRECTION ( 'NONE',  ( -1.000000000000000000, 1.010728034814421376E-30, 1.090846720500930387E-30 ) ) ;
#12667=FACE_OUTER_BOUND ( 'NONE', #9608, .T. ) ;
#12669=DIRECTION ( 'NONE',  ( 0.000000000000000000, 0.000000000000000000, 1.000000000000000000 ) ) ;
#12670=ORIENTED_EDGE ( 'NONE', *, *, #916, .T. ) ;
#12671=AXIS2_PLACEMENT_3D ( 'NONE', #2718, #4078, #3137 ) ;
#12674=CARTESIAN_POINT ( 'NONE',  ( 0.000000000000000000, 2.180689217871857100, 6.122221454264574092 ) ) ;
#12676=ORIENTED_EDGE ( 'NONE', *, *, #7433, .T. ) ;
#12677=DIRECTION ( 'NONE',  ( -1.000000000000000000, 1.010728034814421376E-30, 1.090846720500930387E-30 ) ) ;
#12679=EDGE_CURVE ( 'NONE', #1327, #9789, #4590, .T. ) ;
#12681=ADVANCED_FACE ( 'NONE', ( #5388 ), #2440, .T. ) ;
#12686=DIRECTION ( 'NONE',  ( -1.000000000000000000, 1.010728034814421376E-30, 1.090846720500930387E-30 ) ) ;
#12687=VERTEX_POINT ( 'NONE', #12172 ) ;
#12689=EDGE_LOOP ( 'NONE', ( #8189, #3367, #162, #6933 ) ) ;
#12690=VECTOR ( 'NONE', #5575, 1000.000000000000000 ) ;
#12691=DIRECTION ( 'NONE',  ( -1.000000000000000000, 1.010728034814421376E-30, 1.090846720500930387E-30 ) ) ;
#12695=ORIENTED_EDGE ( 'NONE', *, *, #7561, .F. ) ;
#12698=EDGE_CURVE ( 'NONE', #6291, #245, #1461, .T. ) ;
#12700=CYLINDRICAL_SURFACE ( 'NONE', #1433, 2.800000000000003819 ) ;
#12701=ORIENTED_EDGE ( 'NONE', *, *, #3549, .T. ) ;
#12702=CARTESIAN_POINT ( 'NONE',  ( 9.999999999999994671, -2.171317488608541346, 7.074275960383700657 ) ) ;
#12703=ORIENTED_EDGE ( 'NONE', *, *, #5856, .T. ) ;
#12710=DIRECTION ( 'NONE',  ( -1.000000000000000000, 1.010728034814421376E-30, 1.090846720500930387E-30 ) ) ;
#12711=LINE ( 'NONE', #3877, #5280 ) ;
#12713=CARTESIAN_POINT ( 'NONE',  ( 9.999999999999998224, 0.4528593230175856910, -7.386130139224213131 ) ) ;
#12714=AXIS2_PLACEMENT_3D ( 'NONE', #2576, #5527, #630 ) ;
#12720=DIRECTION ( 'NONE',  ( -1.000000000000000000, 1.010728034814421376E-30, 1.090846720500930387E-30 ) ) ;
#12722=ORIENTED_EDGE ( 'NONE', *, *, #9722, .F. ) ;
#12723=DIRECTION ( 'NONE',  ( -1.000000000000000000, 1.010728034814421376E-30, 1.090846720500930387E-30 ) ) ;
#12726=DIRECTION ( 'NONE',  ( -1.000000000000000000, 1.010728034814421376E-30, 1.090846720500930387E-30 ) ) ;
#12734=DIRECTION ( 'NONE',  ( 0.000000000000000000, 0.000000000000000000, 1.000000000000000000 ) ) ;
#12735=ORIENTED_EDGE ( 'NONE', *, *, #111, .F. ) ;
#12737=VERTEX_POINT ( 'NONE', #11516 ) ;
#12739=CYLINDRICAL_SURFACE ( 'NONE', #7802, 2.800000000000003819 ) ;
#12740=EDGE_LOOP ( 'NONE', ( #9567, #3215, #6159, #5137 ) ) ;
#12742=EDGE_CURVE ( 'NONE', #7844, #5973, #9105, .T. ) ;
#12743=CARTESIAN_POINT ( 'NONE',  ( 19.99999999999997868, -0.4733669331951446679, -6.481737787550303942 ) ) ;
#12746=AXIS2_PLACEMENT_3D ( 'NONE', #7857, #5920, #9833 ) ;
#12747=CARTESIAN_POINT ( 'NONE',  ( 0.000000000000000000, 1.528443194675400019, 7.240432404259460775 ) ) ;
ENDSEC;
END-ISO-10303-21;
